ISO-10303-21;
HEADER;
/* Generated by software containing ST-Developer
 * from STEP Tools, Inc. (www.steptools.com) 
 */

FILE_DESCRIPTION(
/* description */ ('CAx-IF Rec.Pracs.---Representation and Presentation of Product Manufa
cturing Information (PMI)---4.0---2014-10-13'),
/* implementation_level */ '2;1');

FILE_NAME(
/* name */ 'Screw.step',
/* time_stamp */ '2026-10-24T15:08:39-07:00',
/* author */ (''),
/* organization */ (''),
/* preprocessor_version */ 'ST-DEVELOPER v20.2',
/* originating_system */ 'Autodesk Translation Framework v15.17.0.0',
/* authorisation */ '');

FILE_SCHEMA (('AP242_MANAGED_MODEL_BASED_3D_ENGINEERING_MIM_LF { 1 0 10303 442 2 1 4 }'));
ENDSEC;

DATA;
#10=MECHANICAL_DESIGN_GEOMETRIC_PRESENTATION_REPRESENTATION('',(#836),#50081);
#91=(
BOUNDED_SURFACE()
B_SPLINE_SURFACE(1,2,((#48380,#48381,#48382,#48383,#48384,#48385,#48386,
#48387,#48388,#48389,#48390,#48391,#48392,#48393,#48394,#48395,#48396,#48397,
#48398,#48399,#48400,#48401,#48402,#48403,#48404,#48405,#48406,#48407,#48408,
#48409,#48410,#48411,#48412,#48413,#48414,#48415,#48416,#48417,#48418,#48419,
#48420,#48421,#48422,#48423,#48424,#48425,#48426,#48427,#48428,#48429,#48430,
#48431,#48432,#48433,#48434,#48435,#48436,#48437,#48438,#48439,#48440,#48441,
#48442,#48443,#48444,#48445,#48446,#48447,#48448,#48449,#48450,#48451,#48452,
#48453,#48454,#48455,#48456,#48457,#48458,#48459,#48460,#48461,#48462,#48463,
#48464,#48465,#48466,#48467,#48468,#48469,#48470,#48471,#48472,#48473,#48474,
#48475,#48476,#48477,#48478,#48479,#48480,#48481,#48482,#48483,#48484,#48485,
#48486,#48487,#48488,#48489,#48490,#48491,#48492,#48493,#48494,#48495,#48496,
#48497,#48498,#48499,#48500,#48501,#48502,#48503,#48504,#48505,#48506,#48507,
#48508,#48509,#48510,#48511,#48512,#48513,#48514,#48515,#48516,#48517,#48518,
#48519,#48520,#48521,#48522,#48523,#48524,#48525,#48526,#48527,#48528,#48529,
#48530,#48531,#48532,#48533,#48534,#48535,#48536,#48537,#48538,#48539,#48540,
#48541,#48542,#48543,#48544,#48545,#48546,#48547,#48548,#48549,#48550,#48551,
#48552,#48553,#48554,#48555,#48556,#48557,#48558,#48559,#48560,#48561,#48562,
#48563,#48564,#48565,#48566,#48567,#48568,#48569,#48570,#48571,#48572,#48573,
#48574,#48575,#48576,#48577,#48578),(#48579,#48580,#48581,#48582,#48583,
#48584,#48585,#48586,#48587,#48588,#48589,#48590,#48591,#48592,#48593,#48594,
#48595,#48596,#48597,#48598,#48599,#48600,#48601,#48602,#48603,#48604,#48605,
#48606,#48607,#48608,#48609,#48610,#48611,#48612,#48613,#48614,#48615,#48616,
#48617,#48618,#48619,#48620,#48621,#48622,#48623,#48624,#48625,#48626,#48627,
#48628,#48629,#48630,#48631,#48632,#48633,#48634,#48635,#48636,#48637,#48638,
#48639,#48640,#48641,#48642,#48643,#48644,#48645,#48646,#48647,#48648,#48649,
#48650,#48651,#48652,#48653,#48654,#48655,#48656,#48657,#48658,#48659,#48660,
#48661,#48662,#48663,#48664,#48665,#48666,#48667,#48668,#48669,#48670,#48671,
#48672,#48673,#48674,#48675,#48676,#48677,#48678,#48679,#48680,#48681,#48682,
#48683,#48684,#48685,#48686,#48687,#48688,#48689,#48690,#48691,#48692,#48693,
#48694,#48695,#48696,#48697,#48698,#48699,#48700,#48701,#48702,#48703,#48704,
#48705,#48706,#48707,#48708,#48709,#48710,#48711,#48712,#48713,#48714,#48715,
#48716,#48717,#48718,#48719,#48720,#48721,#48722,#48723,#48724,#48725,#48726,
#48727,#48728,#48729,#48730,#48731,#48732,#48733,#48734,#48735,#48736,#48737,
#48738,#48739,#48740,#48741,#48742,#48743,#48744,#48745,#48746,#48747,#48748,
#48749,#48750,#48751,#48752,#48753,#48754,#48755,#48756,#48757,#48758,#48759,
#48760,#48761,#48762,#48763,#48764,#48765,#48766,#48767,#48768,#48769,#48770,
#48771,#48772,#48773,#48774,#48775,#48776,#48777)),.UNSPECIFIED.,.F.,.F.,
 .F.)
B_SPLINE_SURFACE_WITH_KNOTS((2,2),(3,2,2,2,2,2,2,2,2,2,2,2,2,2,2,2,2,2,
2,2,2,2,2,2,2,2,2,2,2,2,2,2,2,2,2,2,2,2,2,2,2,2,2,2,2,2,2,2,2,2,2,2,2,2,
2,2,2,2,2,2,2,2,2,2,2,2,2,2,2,2,2,2,2,2,2,2,2,2,2,2,2,2,2,2,2,2,2,2,2,2,
2,2,2,2,2,2,2,2,2,3),(0.,1.00004093151987),(0.0295122414599334,0.0392156862745098,
0.0490196078431373,0.0588235294117647,0.0686274509803922,0.0784313725490196,
0.0882352941176471,0.0980392156862745,0.107843137254902,0.117647058823529,
0.127450980392157,0.137254901960784,0.147058823529412,0.156862745098039,
0.166666666666667,0.176470588235294,0.186274509803922,0.196078431372549,
0.205882352941176,0.215686274509804,0.225490196078431,0.235294117647059,
0.245098039215686,0.254901960784314,0.264705882352941,0.274509803921569,
0.284313725490196,0.294117647058824,0.303921568627451,0.313725490196078,
0.323529411764706,0.333333333333333,0.343137254901961,0.352941176470588,
0.362745098039216,0.372549019607843,0.382352941176471,0.392156862745098,
0.401960784313726,0.411764705882353,0.42156862745098,0.431372549019608,
0.441176470588235,0.450980392156863,0.46078431372549,0.470588235294118,
0.480392156862745,0.490196078431373,0.5,0.509803921568627,0.519607843137255,
0.529411764705882,0.53921568627451,0.549019607843137,0.558823529411765,
0.568627450980392,0.57843137254902,0.588235294117647,0.598039215686274,
0.607843137254902,0.617647058823529,0.627450980392157,0.637254901960784,
0.647058823529412,0.656862745098039,0.666666666666667,0.676470588235294,
0.686274509803922,0.696078431372549,0.705882352941177,0.715686274509804,
0.725490196078431,0.735294117647059,0.745098039215686,0.754901960784314,
0.764705882352941,0.774509803921569,0.784313725490196,0.794117647058823,
0.803921568627451,0.813725490196078,0.823529411764706,0.833333333333333,
0.843137254901961,0.852941176470588,0.862745098039216,0.872549019607843,
0.882352941176471,0.892156862745098,0.901960784313726,0.911764705882353,
0.92156862745098,0.931372549019608,0.941176470588235,0.950980392156863,
0.96078431372549,0.970588235294118,0.980392156862745,0.990196078431373,
0.998519452012734),.UNSPECIFIED.)
GEOMETRIC_REPRESENTATION_ITEM()
RATIONAL_B_SPLINE_SURFACE(((0.997282032040392,0.867398459704848,1.,0.866025403784439,
1.,0.866025403784439,1.,0.866025403784439,1.,0.866025403784439,1.,0.866025403784439,
1.,0.866025403784439,1.,0.866025403784439,1.,0.866025403784439,1.,0.866025403784439,
1.,0.866025403784439,1.,0.866025403784439,1.,0.866025403784439,1.,0.866025403784439,
1.,0.866025403784439,1.,0.866025403784439,1.,0.866025403784439,1.,0.866025403784439,
1.,0.866025403784439,1.,0.866025403784439,1.,0.866025403784439,1.,0.866025403784439,
1.,0.866025403784439,1.,0.866025403784439,1.,0.866025403784439,1.,0.866025403784439,
1.,0.866025403784439,1.,0.866025403784439,1.,0.866025403784439,1.,0.866025403784439,
1.,0.866025403784439,1.,0.866025403784439,1.,0.866025403784439,1.,0.866025403784439,
1.,0.866025403784439,1.,0.866025403784439,1.,0.866025403784439,1.,0.866025403784439,
1.,0.866025403784439,1.,0.866025403784439,1.,0.866025403784439,1.,0.866025403784439,
1.,0.866025403784439,1.,0.866025403784439,1.,0.866025403784439,1.,0.866025403784439,
1.,0.866025403784439,1.,0.866025403784439,1.,0.866025403784439,1.,0.866025403784439,
1.,0.866025403784439,1.,0.866025403784439,1.,0.866025403784439,1.,0.866025403784439,
1.,0.866025403784439,1.,0.866025403784439,1.,0.866025403784439,1.,0.866025403784439,
1.,0.866025403784439,1.,0.866025403784439,1.,0.866025403784439,1.,0.866025403784439,
1.,0.866025403784439,1.,0.866025403784439,1.,0.866025403784439,1.,0.866025403784439,
1.,0.866025403784439,1.,0.866025403784439,1.,0.866025403784439,1.,0.866025403784439,
1.,0.866025403784439,1.,0.866025403784439,1.,0.866025403784439,1.,0.866025403784439,
1.,0.866025403784439,1.,0.866025403784439,1.,0.866025403784439,1.,0.866025403784439,
1.,0.866025403784439,1.,0.866025403784439,1.,0.866025403784439,1.,0.866025403784439,
1.,0.866025403784439,1.,0.866025403784439,1.,0.866025403784439,1.,0.866025403784439,
1.,0.866025403784439,1.,0.866025403784439,1.,0.866025403784439,1.,0.866025403784439,
1.,0.866025403784439,1.,0.866025403784439,1.,0.866025403784439,1.,0.866025403784439,
1.,0.866025403784439,1.,0.866025403784439,1.,0.866025403784439,1.,0.866025403784439,
1.,0.886257697299162,0.965646208784519),(0.997282032040392,0.867398459704848,
1.,0.866025403784439,1.,0.866025403784439,1.,0.866025403784439,1.,0.866025403784439,
1.,0.866025403784439,1.,0.866025403784439,1.,0.866025403784439,1.,0.866025403784439,
1.,0.866025403784439,1.,0.866025403784439,1.,0.866025403784439,1.,0.866025403784439,
1.,0.866025403784439,1.,0.866025403784439,1.,0.866025403784439,1.,0.866025403784439,
1.,0.866025403784439,1.,0.866025403784439,1.,0.866025403784439,1.,0.866025403784439,
1.,0.866025403784439,1.,0.866025403784439,1.,0.866025403784439,1.,0.866025403784439,
1.,0.866025403784439,1.,0.866025403784439,1.,0.866025403784439,1.,0.866025403784439,
1.,0.866025403784439,1.,0.866025403784439,1.,0.866025403784439,1.,0.866025403784439,
1.,0.866025403784439,1.,0.866025403784439,1.,0.866025403784439,1.,0.866025403784439,
1.,0.866025403784439,1.,0.866025403784439,1.,0.866025403784439,1.,0.866025403784439,
1.,0.866025403784439,1.,0.866025403784439,1.,0.866025403784439,1.,0.866025403784439,
1.,0.866025403784439,1.,0.866025403784439,1.,0.866025403784439,1.,0.866025403784439,
1.,0.866025403784439,1.,0.866025403784439,1.,0.866025403784439,1.,0.866025403784439,
1.,0.866025403784439,1.,0.866025403784439,1.,0.866025403784439,1.,0.866025403784439,
1.,0.866025403784439,1.,0.866025403784439,1.,0.866025403784439,1.,0.866025403784439,
1.,0.866025403784439,1.,0.866025403784439,1.,0.866025403784439,1.,0.866025403784439,
1.,0.866025403784439,1.,0.866025403784439,1.,0.866025403784439,1.,0.866025403784439,
1.,0.866025403784439,1.,0.866025403784439,1.,0.866025403784439,1.,0.866025403784439,
1.,0.866025403784439,1.,0.866025403784439,1.,0.866025403784439,1.,0.866025403784439,
1.,0.866025403784439,1.,0.866025403784439,1.,0.866025403784439,1.,0.866025403784439,
1.,0.866025403784439,1.,0.866025403784439,1.,0.866025403784439,1.,0.866025403784439,
1.,0.866025403784439,1.,0.866025403784439,1.,0.866025403784439,1.,0.866025403784439,
1.,0.866025403784439,1.,0.866025403784439,1.,0.866025403784439,1.,0.866025403784439,
1.,0.866025403784439,1.,0.866025403784439,1.,0.866025403784439,1.,0.866025403784439,
1.,0.866025403784439,1.,0.886257697299162,0.965646208784519)))
REPRESENTATION_ITEM('')
SURFACE()
);
#92=(
BOUNDED_SURFACE()
B_SPLINE_SURFACE(1,2,((#48794,#48795,#48796,#48797,#48798,#48799,#48800,
#48801,#48802,#48803,#48804,#48805,#48806,#48807,#48808,#48809,#48810,#48811,
#48812,#48813,#48814,#48815,#48816,#48817,#48818,#48819,#48820,#48821,#48822,
#48823,#48824,#48825,#48826,#48827,#48828,#48829,#48830,#48831,#48832,#48833,
#48834,#48835,#48836,#48837,#48838,#48839,#48840,#48841,#48842,#48843,#48844,
#48845,#48846,#48847,#48848,#48849,#48850,#48851,#48852,#48853,#48854,#48855,
#48856,#48857,#48858,#48859,#48860,#48861,#48862,#48863,#48864,#48865,#48866,
#48867,#48868,#48869,#48870,#48871,#48872,#48873,#48874,#48875,#48876,#48877,
#48878,#48879,#48880,#48881,#48882,#48883,#48884,#48885,#48886,#48887,#48888,
#48889,#48890,#48891,#48892,#48893,#48894,#48895,#48896,#48897,#48898,#48899,
#48900,#48901,#48902,#48903,#48904,#48905,#48906,#48907,#48908,#48909,#48910,
#48911,#48912,#48913,#48914,#48915,#48916,#48917,#48918,#48919,#48920,#48921,
#48922,#48923,#48924,#48925,#48926,#48927,#48928,#48929,#48930,#48931,#48932,
#48933,#48934,#48935,#48936,#48937,#48938,#48939,#48940,#48941,#48942,#48943,
#48944,#48945,#48946,#48947,#48948,#48949,#48950,#48951,#48952,#48953,#48954,
#48955,#48956,#48957,#48958,#48959,#48960,#48961,#48962,#48963,#48964,#48965,
#48966,#48967,#48968,#48969,#48970,#48971,#48972,#48973,#48974,#48975,#48976,
#48977,#48978,#48979,#48980,#48981,#48982,#48983,#48984,#48985,#48986,#48987,
#48988),(#48989,#48990,#48991,#48992,#48993,#48994,#48995,#48996,#48997,
#48998,#48999,#49000,#49001,#49002,#49003,#49004,#49005,#49006,#49007,#49008,
#49009,#49010,#49011,#49012,#49013,#49014,#49015,#49016,#49017,#49018,#49019,
#49020,#49021,#49022,#49023,#49024,#49025,#49026,#49027,#49028,#49029,#49030,
#49031,#49032,#49033,#49034,#49035,#49036,#49037,#49038,#49039,#49040,#49041,
#49042,#49043,#49044,#49045,#49046,#49047,#49048,#49049,#49050,#49051,#49052,
#49053,#49054,#49055,#49056,#49057,#49058,#49059,#49060,#49061,#49062,#49063,
#49064,#49065,#49066,#49067,#49068,#49069,#49070,#49071,#49072,#49073,#49074,
#49075,#49076,#49077,#49078,#49079,#49080,#49081,#49082,#49083,#49084,#49085,
#49086,#49087,#49088,#49089,#49090,#49091,#49092,#49093,#49094,#49095,#49096,
#49097,#49098,#49099,#49100,#49101,#49102,#49103,#49104,#49105,#49106,#49107,
#49108,#49109,#49110,#49111,#49112,#49113,#49114,#49115,#49116,#49117,#49118,
#49119,#49120,#49121,#49122,#49123,#49124,#49125,#49126,#49127,#49128,#49129,
#49130,#49131,#49132,#49133,#49134,#49135,#49136,#49137,#49138,#49139,#49140,
#49141,#49142,#49143,#49144,#49145,#49146,#49147,#49148,#49149,#49150,#49151,
#49152,#49153,#49154,#49155,#49156,#49157,#49158,#49159,#49160,#49161,#49162,
#49163,#49164,#49165,#49166,#49167,#49168,#49169,#49170,#49171,#49172,#49173,
#49174,#49175,#49176,#49177,#49178,#49179,#49180,#49181,#49182,#49183)),
 .UNSPECIFIED.,.F.,.F.,.F.)
B_SPLINE_SURFACE_WITH_KNOTS((2,2),(3,2,2,2,2,2,2,2,2,2,2,2,2,2,2,2,2,2,
2,2,2,2,2,2,2,2,2,2,2,2,2,2,2,2,2,2,2,2,2,2,2,2,2,2,2,2,2,2,2,2,2,2,2,2,
2,2,2,2,2,2,2,2,2,2,2,2,2,2,2,2,2,2,2,2,2,2,2,2,2,2,2,2,2,2,2,2,2,2,2,2,
2,2,2,2,2,2,2,3),(-4.46693850465293E-5,1.00004466937728),(0.0222318908269079,
0.0294117647058824,0.0392156862745098,0.0490196078431373,0.0588235294117647,
0.0686274509803922,0.0784313725490196,0.0882352941176471,0.0980392156862745,
0.107843137254902,0.117647058823529,0.127450980392157,0.137254901960784,
0.147058823529412,0.156862745098039,0.166666666666667,0.176470588235294,
0.186274509803922,0.196078431372549,0.205882352941176,0.215686274509804,
0.225490196078431,0.235294117647059,0.245098039215686,0.254901960784314,
0.264705882352941,0.274509803921569,0.284313725490196,0.294117647058824,
0.303921568627451,0.313725490196078,0.323529411764706,0.333333333333333,
0.343137254901961,0.352941176470588,0.362745098039216,0.372549019607843,
0.382352941176471,0.392156862745098,0.401960784313726,0.411764705882353,
0.42156862745098,0.431372549019608,0.441176470588235,0.450980392156863,
0.46078431372549,0.470588235294118,0.480392156862745,0.490196078431373,
0.5,0.509803921568627,0.519607843137255,0.529411764705882,0.53921568627451,
0.549019607843137,0.558823529411765,0.568627450980392,0.57843137254902,
0.588235294117647,0.598039215686274,0.607843137254902,0.617647058823529,
0.627450980392157,0.637254901960784,0.647058823529412,0.656862745098039,
0.666666666666667,0.676470588235294,0.686274509803922,0.696078431372549,
0.705882352941177,0.715686274509804,0.725490196078431,0.735294117647059,
0.745098039215686,0.754901960784314,0.764705882352941,0.774509803921569,
0.784313725490196,0.794117647058823,0.803921568627451,0.813725490196078,
0.823529411764706,0.833333333333333,0.843137254901961,0.852941176470588,
0.862745098039216,0.872549019607843,0.882352941176471,0.892156862745098,
0.901960784313726,0.911764705882353,0.92156862745098,0.931372549019608,
0.941176470588235,0.950980392156863,0.96078431372549,0.968975690801275),
 .UNSPECIFIED.)
GEOMETRIC_REPRESENTATION_ITEM()
RATIONAL_B_SPLINE_SURFACE(((0.947477990343754,0.901884088210946,1.,0.866025403784439,
1.,0.866025403784439,1.,0.866025403784439,1.,0.866025403784439,1.,0.866025403784439,
1.,0.866025403784439,1.,0.866025403784439,1.,0.866025403784439,1.,0.866025403784439,
1.,0.866025403784439,1.,0.866025403784439,1.,0.866025403784439,1.,0.866025403784439,
1.,0.866025403784439,1.,0.866025403784439,1.,0.866025403784439,1.,0.866025403784439,
1.,0.866025403784439,1.,0.866025403784439,1.,0.866025403784439,1.,0.866025403784439,
1.,0.866025403784439,1.,0.866025403784439,1.,0.866025403784439,1.,0.866025403784439,
1.,0.866025403784439,1.,0.866025403784439,1.,0.866025403784439,1.,0.866025403784439,
1.,0.866025403784439,1.,0.866025403784439,1.,0.866025403784439,1.,0.866025403784439,
1.,0.866025403784439,1.,0.866025403784439,1.,0.866025403784439,1.,0.866025403784439,
1.,0.866025403784439,1.,0.866025403784439,1.,0.866025403784439,1.,0.866025403784439,
1.,0.866025403784439,1.,0.866025403784439,1.,0.866025403784439,1.,0.866025403784439,
1.,0.866025403784439,1.,0.866025403784439,1.,0.866025403784439,1.,0.866025403784439,
1.,0.866025403784439,1.,0.866025403784439,1.,0.866025403784439,1.,0.866025403784439,
1.,0.866025403784439,1.,0.866025403784439,1.,0.866025403784439,1.,0.866025403784439,
1.,0.866025403784439,1.,0.866025403784439,1.,0.866025403784439,1.,0.866025403784439,
1.,0.866025403784439,1.,0.866025403784439,1.,0.866025403784439,1.,0.866025403784439,
1.,0.866025403784439,1.,0.866025403784439,1.,0.866025403784439,1.,0.866025403784439,
1.,0.866025403784439,1.,0.866025403784439,1.,0.866025403784439,1.,0.866025403784439,
1.,0.866025403784439,1.,0.866025403784439,1.,0.866025403784439,1.,0.866025403784439,
1.,0.866025403784439,1.,0.866025403784439,1.,0.866025403784439,1.,0.866025403784439,
1.,0.866025403784439,1.,0.866025403784439,1.,0.866025403784439,1.,0.866025403784439,
1.,0.866025403784439,1.,0.866025403784439,1.,0.866025403784439,1.,0.866025403784439,
1.,0.866025403784439,1.,0.866025403784439,1.,0.866025403784439,1.,0.866025403784439,
1.,0.866025403784439,1.,0.866025403784439,1.,0.888061483509882,0.963176808986156),
(0.947477990343754,0.901884088210946,1.,0.866025403784439,1.,0.866025403784439,
1.,0.866025403784439,1.,0.866025403784439,1.,0.866025403784439,1.,0.866025403784439,
1.,0.866025403784439,1.,0.866025403784439,1.,0.866025403784439,1.,0.866025403784439,
1.,0.866025403784439,1.,0.866025403784439,1.,0.866025403784439,1.,0.866025403784439,
1.,0.866025403784439,1.,0.866025403784439,1.,0.866025403784439,1.,0.866025403784439,
1.,0.866025403784439,1.,0.866025403784439,1.,0.866025403784439,1.,0.866025403784439,
1.,0.866025403784439,1.,0.866025403784439,1.,0.866025403784439,1.,0.866025403784439,
1.,0.866025403784439,1.,0.866025403784439,1.,0.866025403784439,1.,0.866025403784439,
1.,0.866025403784439,1.,0.866025403784439,1.,0.866025403784439,1.,0.866025403784439,
1.,0.866025403784439,1.,0.866025403784439,1.,0.866025403784439,1.,0.866025403784439,
1.,0.866025403784439,1.,0.866025403784439,1.,0.866025403784439,1.,0.866025403784439,
1.,0.866025403784439,1.,0.866025403784439,1.,0.866025403784439,1.,0.866025403784439,
1.,0.866025403784439,1.,0.866025403784439,1.,0.866025403784439,1.,0.866025403784439,
1.,0.866025403784439,1.,0.866025403784439,1.,0.866025403784439,1.,0.866025403784439,
1.,0.866025403784439,1.,0.866025403784439,1.,0.866025403784439,1.,0.866025403784439,
1.,0.866025403784439,1.,0.866025403784439,1.,0.866025403784439,1.,0.866025403784439,
1.,0.866025403784439,1.,0.866025403784439,1.,0.866025403784439,1.,0.866025403784439,
1.,0.866025403784439,1.,0.866025403784439,1.,0.866025403784439,1.,0.866025403784439,
1.,0.866025403784439,1.,0.866025403784439,1.,0.866025403784439,1.,0.866025403784439,
1.,0.866025403784439,1.,0.866025403784439,1.,0.866025403784439,1.,0.866025403784439,
1.,0.866025403784439,1.,0.866025403784439,1.,0.866025403784439,1.,0.866025403784439,
1.,0.866025403784439,1.,0.866025403784439,1.,0.866025403784439,1.,0.866025403784439,
1.,0.866025403784439,1.,0.866025403784439,1.,0.866025403784439,1.,0.866025403784439,
1.,0.866025403784439,1.,0.866025403784439,1.,0.866025403784439,1.,0.866025403784439,
1.,0.866025403784439,1.,0.888061483509882,0.963176808986156)))
REPRESENTATION_ITEM('')
SURFACE()
);
#93=SPHERICAL_SURFACE('',#10942,0.00317192226735973);
#517=B_SPLINE_CURVE_WITH_KNOTS('',3,(#45891,#45892,#45893,#45894,#45895,
#45896,#45897,#45898,#45899,#45900,#45901,#45902,#45903,#45904,#45905,#45906,
#45907,#45908,#45909,#45910),.UNSPECIFIED.,.F.,.F.,(4,2,2,2,2,2,2,2,2,4),
(-0.472680489487021,-0.421857921558036,-0.362870895179553,-0.305901838025028,
-0.246237725257386,-0.187898332264809,-0.130441066174416,-0.0704976060355538,
-0.0346474857024549,-9.9999999542133E-7),.UNSPECIFIED.);
#518=B_SPLINE_CURVE_WITH_KNOTS('',3,(#45913,#45914,#45915,#45916,#45917,
#45918,#45919,#45920,#45921,#45922,#45923,#45924,#45925,#45926,#45927,#45928),
 .UNSPECIFIED.,.F.,.F.,(4,2,2,2,2,2,2,4),(-14.4370592734888,-14.4037012578129,
-14.3709495751806,-14.3127127045736,-14.2529421093177,-14.1958485449995,
-14.1369603965429,-14.0806259388301),.UNSPECIFIED.);
#519=B_SPLINE_CURVE_WITH_KNOTS('',3,(#45933,#45934,#45935,#45936,#45937,
#45938,#45939,#45940,#45941,#45942,#45943,#45944,#45945,#45946,#45947,#45948,
#45949,#45950,#45951,#45952,#45953,#45954,#45955,#45956,#45957,#45958,#45959,
#45960,#45961,#45962,#45963,#45964,#45965,#45966,#45967,#45968,#45969,#45970),
 .UNSPECIFIED.,.F.,.F.,(4,2,2,2,2,2,2,2,2,2,2,2,2,2,2,2,2,2,4),(-1.41859832691229,
-1.41822527997428,-1.35855760366901,-1.29985891312466,-1.24273727568412,
-1.18301408218039,-1.12496822443588,-1.06682478961775,-1.00721544324156,
-0.949844979558046,-0.89017629567726,-0.831344294177192,-0.77434923288016,
-0.714670672924963,-0.656488509400857,-0.598748590473465,-0.538981330577316,
-0.481470031543986,-0.472680489487021),.UNSPECIFIED.);
#520=B_SPLINE_CURVE_WITH_KNOTS('',3,(#45971,#45972,#45973,#45974,#45975,
#45976,#45977,#45978,#45979,#45980,#45981,#45982,#45983,#45984,#45985,#45986,
#45987,#45988,#45989,#45990,#45991,#45992,#45993,#45994,#45995,#45996,#45997,
#45998,#45999,#46000,#46001,#46002,#46003,#46004,#46005,#46006,#46007,#46008),
 .UNSPECIFIED.,.F.,.F.,(4,2,2,2,2,2,2,2,2,2,2,2,2,2,2,2,2,2,4),(-14.0806259388301,
-14.0772027728482,-14.0197752809982,-13.9601089034145,-13.9017860811062,
-13.843680755693,-13.7832574713262,-13.7260330550825,-13.6672514254089,
-13.6074849557429,-13.5502487242808,-13.4908237302309,-13.432144117751,
-13.3742545460729,-13.3140698205319,-13.2567467237662,-13.198184782689,
-13.1384608998608,-13.133357359287),.UNSPECIFIED.);
#521=B_SPLINE_CURVE_WITH_KNOTS('',3,(#46013,#46014,#46015,#46016,#46017,
#46018,#46019,#46020,#46021,#46022,#46023,#46024,#46025,#46026,#46027,#46028,
#46029,#46030,#46031,#46032,#46033,#46034,#46035,#46036,#46037,#46038,#46039,
#46040,#46041,#46042,#46043,#46044,#46045,#46046,#46047,#46048),
 .UNSPECIFIED.,.F.,.F.,(4,2,2,2,2,2,2,2,2,2,2,2,2,2,2,2,2,4),(-2.36357121621961,
-2.35439216466225,-2.29478381910495,-2.23649866694068,-2.17909549669189,
-2.11920774560853,-2.06159204897073,-2.00258816172034,-1.94346622679962,
-1.8864802795193,-1.82685774819307,-1.76838058281947,-1.71116885123677,
-1.65107017816501,-1.59326446777019,-1.53472012633121,-1.47537944090739,
-1.41859832691229),.UNSPECIFIED.);
#522=B_SPLINE_CURVE_WITH_KNOTS('',3,(#46049,#46050,#46051,#46052,#46053,
#46054,#46055,#46056,#46057,#46058,#46059,#46060,#46061,#46062,#46063,#46064,
#46065,#46066,#46067,#46068,#46069,#46070,#46071,#46072,#46073,#46074,#46075,
#46076,#46077,#46078,#46079,#46080,#46081,#46082,#46083,#46084),
 .UNSPECIFIED.,.F.,.F.,(4,2,2,2,2,2,2,2,2,2,2,2,2,2,2,2,2,4),(-13.133357359287,
-13.081385357797,-13.0221773281264,-12.9630288925176,-12.905327227556,-12.8453511553982,
-12.7878283622088,-12.729456125551,-12.6697440428986,-12.6127306500945,
-12.5537100886643,-12.4940029413133,-12.4364567758814,-12.3766541658974,
-12.3188421358561,-12.2606243760745,-12.2008957709647,-12.1870122249769),
 .UNSPECIFIED.);
#523=B_SPLINE_CURVE_WITH_KNOTS('',3,(#46089,#46090,#46091,#46092,#46093,
#46094,#46095,#46096,#46097,#46098,#46099,#46100,#46101,#46102,#46103,#46104,
#46105,#46106,#46107,#46108,#46109,#46110,#46111,#46112,#46113,#46114,#46115,
#46116,#46117,#46118,#46119,#46120,#46121,#46122,#46123,#46124),
 .UNSPECIFIED.,.F.,.F.,(4,2,2,2,2,2,2,2,2,2,2,2,2,2,2,2,2,4),(-3.30848554402564,
-3.29034972008339,-3.23068257001005,-3.1726908982952,-3.11460265690008,
-3.05504892530917,-2.99773200432777,-2.93811923868514,-2.8793421277137,
-2.82240057354888,-2.76277796537348,-2.70465007979412,-2.64696477699234,
-2.58725324895101,-2.52979559565241,-2.47024018500225,-2.41130800830289,
-2.36357121621961),.UNSPECIFIED.);
#524=B_SPLINE_CURVE_WITH_KNOTS('',3,(#46125,#46126,#46127,#46128,#46129,
#46130,#46131,#46132,#46133,#46134,#46135,#46136,#46137,#46138,#46139,#46140,
#46141,#46142,#46143,#46144,#46145,#46146,#46147,#46148,#46149,#46150,#46151,
#46152,#46153,#46154,#46155,#46156,#46157,#46158,#46159,#46160),
 .UNSPECIFIED.,.F.,.F.,(4,2,2,2,2,2,2,2,2,2,2,2,2,2,2,2,2,4),(-12.1870122249769,
-12.1438492432235,-12.0849809374751,-12.0246571711172,-11.9672296348607,
-11.9075603623266,-11.8493922713876,-11.7912891282832,-11.731517449561,
-11.6743561420471,-11.6155998003076,-11.5558844962949,-11.4986749070985,
-11.4392762960987,-11.3807140133877,-11.3228531755694,-11.2626963209889,
-11.2404440616607),.UNSPECIFIED.);
#525=B_SPLINE_CURVE_WITH_KNOTS('',3,(#46165,#46166,#46167,#46168,#46169,
#46170,#46171,#46172,#46173,#46174,#46175,#46176,#46177,#46178,#46179,#46180,
#46181,#46182,#46183,#46184,#46185,#46186,#46187,#46188,#46189,#46190,#46191,
#46192,#46193,#46194,#46195,#46196,#46197,#46198,#46199,#46200),
 .UNSPECIFIED.,.F.,.F.,(4,2,2,2,2,2,2,2,2,2,2,2,2,2,2,2,2,4),(-4.2528209750252,
-4.2258289954172,-4.16599723540487,-4.10843542684453,-4.04948791774649,
-3.99042123507979,-3.93348867864914,-3.87392217476687,-3.81549965097264,
-3.75834197483301,-3.69829943582703,-3.64054774097401,-3.58205916445528,
-3.52277389154611,-3.46567311490864,-3.4060614524971,-3.34741756521746,
-3.30848554402564),.UNSPECIFIED.);
#526=B_SPLINE_CURVE_WITH_KNOTS('',3,(#46201,#46202,#46203,#46204,#46205,
#46206,#46207,#46208,#46209,#46210,#46211,#46212,#46213,#46214,#46215,#46216,
#46217,#46218,#46219,#46220,#46221,#46222,#46223,#46224,#46225,#46226,#46227,
#46228,#46229,#46230,#46231,#46232,#46233,#46234,#46235,#46236),
 .UNSPECIFIED.,.F.,.F.,(4,2,2,2,2,2,2,2,2,2,2,2,2,2,2,2,2,4),(-11.2404440616607,
-11.2054512613555,-11.1469182749413,-11.0872501668356,-11.0302148159706,
-10.9710367406564,-10.9120211179477,-10.854352265994,-10.7944084679723,
-10.7369779084177,-10.6786390615402,-10.6189869936286,-10.5620279497738,
-10.5030417379351,-10.4434790671637,-10.3859704970566,-10.3262053607749,
-10.2949578972094),.UNSPECIFIED.);
#527=B_SPLINE_CURVE_WITH_KNOTS('',3,(#46241,#46242,#46243,#46244,#46245,
#46246,#46247,#46248,#46249,#46250,#46251,#46252,#46253,#46254,#46255,#46256,
#46257,#46258,#46259,#46260,#46261,#46262,#46263,#46264,#46265,#46266,#46267,
#46268,#46269,#46270,#46271,#46272,#46273,#46274,#46275,#46276),
 .UNSPECIFIED.,.F.,.F.,(4,2,2,2,2,2,2,2,2,2,2,2,2,2,2,2,2,4),(-5.19675137828244,
-5.16045616765585,-5.10095821008514,-5.04369498598246,-4.98413831157424,
-4.92541624835806,-4.86852837157201,-4.80896188953764,-4.75088843704952,
-4.6932579452808,-4.63360230711379,-4.57619845256742,-4.5167000729659,-4.4578230250715,
-4.40096067746688,-4.34140839720388,-4.28317776156472,-4.2528209750252),
 .UNSPECIFIED.);
#528=B_SPLINE_CURVE_WITH_KNOTS('',3,(#46277,#46278,#46279,#46280,#46281,
#46282,#46283,#46284,#46285,#46286,#46287,#46288,#46289,#46290,#46291,#46292,
#46293,#46294,#46295,#46296,#46297,#46298,#46299,#46300,#46301,#46302,#46303,
#46304,#46305,#46306,#46307,#46308,#46309,#46310,#46311,#46312),
 .UNSPECIFIED.,.F.,.F.,(4,2,2,2,2,2,2,2,2,2,2,2,2,2,2,2,2,4),(-10.2949578972094,
-10.2684975889558,-10.2103184315637,-10.1506537980798,-10.0936746957517,
-10.0348459812853,-9.97467345304288,-9.91728892738338,-9.85766301371066,
-9.79960748007447,-9.74154877508422,-9.68184483516709,-9.62476165993561,
-9.56605083144069,-9.50636878850725,-9.44910648683061,-9.38961853093635,
-9.34899662094938),.UNSPECIFIED.);
#529=B_SPLINE_CURVE_WITH_KNOTS('',3,(#46317,#46318,#46319,#46320,#46321,
#46322,#46323,#46324,#46325,#46326,#46327,#46328,#46329,#46330,#46331,#46332,
#46333,#46334,#46335,#46336,#46337,#46338,#46339,#46340,#46341,#46342,#46343,
#46344,#46345,#46346,#46347,#46348,#46349,#46350,#46351,#46352),
 .UNSPECIFIED.,.F.,.F.,(4,2,2,2,2,2,2,2,2,2,2,2,2,2,2,2,2,4),(-6.14044228887836,
-6.09446054161853,-6.03544927417801,-5.97857027285831,-5.91905997766185,
-5.86069225619341,-5.80358882530382,-5.74360258432422,-5.68590506399478,
-5.62747247135089,-5.56824277211902,-5.51119553553071,-5.4516400653047,
-5.39305114016943,-5.33603726706465,-5.27642633763462,-5.21848900864112,
-5.19675137828244),.UNSPECIFIED.);
#530=B_SPLINE_CURVE_WITH_KNOTS('',3,(#46353,#46354,#46355,#46356,#46357,
#46358,#46359,#46360,#46361,#46362,#46363,#46364,#46365,#46366,#46367,#46368,
#46369,#46370,#46371,#46372,#46373,#46374,#46375,#46376,#46377,#46378,#46379,
#46380,#46381,#46382,#46383,#46384,#46385,#46386,#46387,#46388),
 .UNSPECIFIED.,.F.,.F.,(4,2,2,2,2,2,2,2,2,2,2,2,2,2,2,2,2,4),(-9.34899662094938,
-9.33105074122771,-9.2731055957996,-9.21285922380668,-9.15557513902431,
-9.09695672998933,-9.03722574734233,-8.98011691943174,-8.92085312448608,
-8.86184579512779,-8.80409668210845,-8.74406773839571,-8.6866111034004,
-8.62819119904668,-8.56848024689387,-8.51146096604764,-8.45239334999859,
-8.40244442487571),.UNSPECIFIED.);
#531=B_SPLINE_CURVE_WITH_KNOTS('',3,(#46393,#46394,#46395,#46396,#46397,
#46398,#46399,#46400,#46401,#46402,#46403,#46404,#46405,#46406,#46407,#46408,
#46409,#46410,#46411,#46412,#46413,#46414,#46415,#46416,#46417,#46418,#46419,
#46420,#46421,#46422,#46423,#46424,#46425,#46426,#46427,#46428),
 .UNSPECIFIED.,.F.,.F.,(4,2,2,2,2,2,2,2,2,2,2,2,2,2,2,2,2,4),(-7.08338076536595,
-7.02822732374101,-6.96956047673802,-6.91272645955143,-6.85321629033566,
-6.79519743717148,-6.73762196486497,-6.67802238589634,-6.62067249405759,
-6.5612313850799,-6.50240963138312,-6.44560095327405,-6.38610492232616,
-6.32792896640202,-6.27063480406051,-6.21085920145596,-6.15335144217075,
-6.14044228887836),.UNSPECIFIED.);
#532=B_SPLINE_CURVE_WITH_KNOTS('',3,(#46429,#46430,#46431,#46432,#46433,
#46434,#46435,#46436,#46437,#46438,#46439,#46440,#46441,#46442,#46443,#46444,
#46445,#46446,#46447,#46448,#46449,#46450,#46451,#46452,#46453,#46454,#46455,
#46456,#46457,#46458,#46459,#46460,#46461,#46462,#46463,#46464),
 .UNSPECIFIED.,.F.,.F.,(4,2,2,2,2,2,2,2,2,2,2,2,2,2,2,2,2,4),(-8.40244442487571,
-8.39284926891096,-8.33526507147472,-8.2754198338689,-8.21769694693658,
-8.15944175694345,-8.09972190021169,-8.04269482223153,-7.98378974191723,
-7.92364153499131,-7.86618654884418,-7.80648615931792,-7.74842299103831,
-7.69029380781885,-7.63053806985166,-7.57341695923763,-7.51463538863381,
-7.45587725387744),.UNSPECIFIED.);
#533=B_SPLINE_CURVE_WITH_KNOTS('',3,(#46469,#46470,#46471,#46472,#46473,
#46474,#46475,#46476,#46477,#46478,#46479,#46480,#46481,#46482,#46483,#46484,
#46485,#46486,#46487,#46488,#46489,#46490,#46491,#46492,#46493,#46494,#46495,
#46496,#46497,#46498,#46499,#46500,#46501,#46502,#46503,#46504,#46505,#46506),
 .UNSPECIFIED.,.F.,.F.,(4,2,2,2,2,2,2,2,2,2,2,2,2,2,2,2,2,2,4),(-8.02645494637709,
-8.02062061883662,-7.96340867156997,-7.903960246378,-7.84617097437453,-7.78828802935107,
-7.72879472313259,-7.67192938925804,-7.6133970541528,-7.55392347512622,
-7.4968374534328,-7.43753093954167,-7.3792524025024,-7.32148761472472,-7.26142618244933,
-7.20437909686838,-7.14493708373042,-7.08772772168777,-7.08338076536595),
 .UNSPECIFIED.);
#534=B_SPLINE_CURVE_WITH_KNOTS('',3,(#46507,#46508,#46509,#46510,#46511,
#46512,#46513,#46514,#46515,#46516,#46517,#46518,#46519,#46520,#46521,#46522,
#46523,#46524,#46525,#46526,#46527,#46528,#46529,#46530,#46531,#46532,#46533,
#46534,#46535,#46536,#46537,#46538,#46539,#46540,#46541,#46542,#46543,#46544),
 .UNSPECIFIED.,.F.,.F.,(4,2,2,2,2,2,2,2,2,2,2,2,2,2,2,2,2,2,4),(-7.45587725387744,
-7.45490013693559,-7.39757036603791,-7.33801115408158,-7.27944992870555,
-7.22143789013388,-7.16324228872916,-7.10513370792117,-7.04536440843998,
-6.98784351644384,-6.92765908972021,-6.86868506825907,-6.81159972067067,
-6.75181742847008,-6.69349388764354,-6.63572323919473,-6.57580712348971,
-6.51815521566034,-6.50836887295495),.UNSPECIFIED.);
#535=B_SPLINE_CURVE_WITH_KNOTS('',3,(#46549,#46550,#46551,#46552,#46553,
#46554,#46555,#46556,#46557,#46558,#46559,#46560,#46561,#46562,#46563,#46564,
#46565,#46566,#46567,#46568,#46569,#46570,#46571,#46572,#46573,#46574,#46575,
#46576,#46577,#46578,#46579,#46580,#46581,#46582,#46583,#46584),
 .UNSPECIFIED.,.F.,.F.,(4,2,2,2,2,2,2,2,2,2,2,2,2,2,2,2,2,4),(-8.96867340698881,
-8.954726041388,-8.89721705486442,-8.83743694489446,-8.7802428260537,-8.72206588455876,
-8.66261397449903,-8.6058398735651,-8.54701816312532,-8.48776662644217,
-8.43042380514485,-8.37082874094838,-8.31337464233727,-8.2553638382111,
-8.195904708086,-8.13912837602821,-8.08047063786001,-8.02645494637709),
 .UNSPECIFIED.);
#536=B_SPLINE_CURVE_WITH_KNOTS('',3,(#46585,#46586,#46587,#46588,#46589,
#46590,#46591,#46592,#46593,#46594,#46595,#46596,#46597,#46598,#46599,#46600,
#46601,#46602,#46603,#46604,#46605,#46606,#46607,#46608,#46609,#46610,#46611,
#46612,#46613,#46614,#46615,#46616,#46617,#46618,#46619,#46620),
 .UNSPECIFIED.,.F.,.F.,(4,2,2,2,2,2,2,2,2,2,2,2,2,2,2,2,2,4),(-6.50836887295495,
-6.45857330656199,-6.39943496988036,-6.34235328727518,-6.28257867687266,
-6.2240886431033,-6.16658070395808,-6.10647908395784,-6.0486606110832,-5.98961229240173,
-5.93027621485651,-5.87310049918669,-5.81330450149875,-5.75461438102413,
-5.69727475870434,-5.63695411223535,-5.57893812995217,-5.56079052540277),
 .UNSPECIFIED.);
#537=B_SPLINE_CURVE_WITH_KNOTS('',3,(#46625,#46626,#46627,#46628,#46629,
#46630,#46631,#46632,#46633,#46634,#46635,#46636,#46637,#46638,#46639,#46640,
#46641,#46642,#46643,#46644,#46645,#46646,#46647,#46648,#46649,#46650,#46651,
#46652,#46653,#46654,#46655,#46656,#46657,#46658,#46659,#46660),
 .UNSPECIFIED.,.F.,.F.,(4,2,2,2,2,2,2,2,2,2,2,2,2,2,2,2,2,4),(-9.91116502693244,
-9.88848172659285,-9.83066113567844,-9.77121178531178,-9.71437759038781,
-9.65590780022673,-9.59647959088436,-9.53945310607522,-9.48020958718447,
-9.42191865790845,-9.36421279874568,-9.30421438211681,-9.24718616399223,
-9.18880975199588,-9.12933611442946,-9.07246699404788,-9.01344815245977,
-8.96867340698881),.UNSPECIFIED.);
#538=B_SPLINE_CURVE_WITH_KNOTS('',3,(#46661,#46662,#46663,#46664,#46665,
#46666,#46667,#46668,#46669,#46670,#46671,#46672,#46673,#46674,#46675,#46676,
#46677,#46678,#46679,#46680,#46681,#46682,#46683,#46684,#46685,#46686,#46687,
#46688,#46689,#46690,#46691,#46692,#46693,#46694,#46695,#46696),
 .UNSPECIFIED.,.F.,.F.,(4,2,2,2,2,2,2,2,2,2,2,2,2,2,2,2,2,4),(-5.56079052540277,
-5.52032499325248,-5.46076339888321,-5.40343060697284,-5.34368112976859,
-5.28489746921949,-5.22775446056634,-5.16798355663942,-5.10985264323955,
-5.05174717925448,-4.99204636464476,-4.93459018081613,-4.8743772890817,
-4.815473646124,-4.75843127614468,-4.6986984995855,-4.64044506045571,-4.61376150694468),
 .UNSPECIFIED.);
#539=B_SPLINE_CURVE_WITH_KNOTS('',3,(#46701,#46702,#46703,#46704,#46705,
#46706,#46707,#46708,#46709,#46710,#46711,#46712,#46713,#46714,#46715,#46716,
#46717,#46718,#46719,#46720,#46721,#46722,#46723,#46724,#46725,#46726,#46727,
#46728,#46729,#46730,#46731,#46732,#46733,#46734,#46735,#46736),
 .UNSPECIFIED.,.F.,.F.,(4,2,2,2,2,2,2,2,2,2,2,2,2,2,2,2,2,4),(-10.8526636518455,
-10.8218563382694,-10.763751898801,-10.7043508376338,-10.6476297274538,
-10.5888807841235,-10.5296053803888,-10.4723299070045,-10.4128063061383,
-10.3553612254831,-10.2974181137557,-10.2380062710185,-10.1812709618512,
-10.1226811718715,-10.0628013902258,-10.0056518305266,-9.94626946773807,
-9.91116502693244),.UNSPECIFIED.);
#540=B_SPLINE_CURVE_WITH_KNOTS('',3,(#46737,#46738,#46739,#46740,#46741,
#46742,#46743,#46744,#46745,#46746,#46747,#46748,#46749,#46750,#46751,#46752,
#46753,#46754,#46755,#46756,#46757,#46758,#46759,#46760,#46761,#46762,#46763,
#46764,#46765,#46766,#46767,#46768,#46769,#46770,#46771,#46772),
 .UNSPECIFIED.,.F.,.F.,(4,2,2,2,2,2,2,2,2,2,2,2,2,2,2,2,2,4),(-4.61376150694468,
-4.58268504394349,-4.52284289180626,-4.46526072397115,-4.40565622753905,
-4.34659316243956,-4.28956654669504,-4.22984505241611,-4.17143000304458,
-4.11394358291504,-4.05392082544131,-3.99617659372884,-3.93711600484904,
-3.87785937905479,-3.82075170408198,-3.76101274778027,-3.7024018430971,
-3.66716520277466),.UNSPECIFIED.);
#541=B_SPLINE_CURVE_WITH_KNOTS('',3,(#46777,#46778,#46779,#46780,#46781,
#46782,#46783,#46784,#46785,#46786,#46787,#46788,#46789,#46790,#46791,#46792,
#46793,#46794,#46795,#46796,#46797,#46798,#46799,#46800,#46801,#46802,#46803,
#46804,#46805,#46806,#46807,#46808,#46809,#46810,#46811,#46812),
 .UNSPECIFIED.,.F.,.F.,(4,2,2,2,2,2,2,2,2,2,2,2,2,2,2,2,2,4),(-11.7943289504834,
-11.7550760696795,-11.6966860285444,-11.6373196802076,-11.5803693805583,
-11.5212061909831,-11.4629152278514,-11.4052850124585,-11.345367052905,
-11.2883712953563,-11.2300715499567,-11.1706526443042,-11.1138493310695,
-11.0549073697268,-10.9961716612307,-10.9387344559412,-10.8790306340246,
-10.8526636518455),.UNSPECIFIED.);
#542=B_SPLINE_CURVE_WITH_KNOTS('',3,(#46813,#46814,#46815,#46816,#46817,
#46818,#46819,#46820,#46821,#46822,#46823,#46824,#46825,#46826,#46827,#46828,
#46829,#46830,#46831,#46832,#46833,#46834,#46835,#46836,#46837,#46838,#46839,
#46840,#46841,#46842,#46843,#46844,#46845,#46846,#46847,#46848),
 .UNSPECIFIED.,.F.,.F.,(4,2,2,2,2,2,2,2,2,2,2,2,2,2,2,2,2,4),(-3.66716520277466,
-3.64509650595974,-3.58485895842258,-3.52692114130706,-3.46830941132696,
-3.40883077564351,-3.35157668733905,-3.29189146511806,-3.23319016450654,
-3.17609457994864,-3.11638652761123,-3.05833760937658,-3.00024818247934,
-2.94063377994132,-2.8832595066928,-2.82302963638987,-2.76421431619143,
-2.72088258416467),.UNSPECIFIED.);
#543=B_SPLINE_CURVE_WITH_KNOTS('',3,(#46853,#46854,#46855,#46856,#46857,
#46858,#46859,#46860,#46861,#46862,#46863,#46864,#46865,#46866,#46867,#46868,
#46869,#46870,#46871,#46872,#46873,#46874,#46875,#46876,#46877,#46878,#46879,
#46880,#46881,#46882,#46883,#46884,#46885,#46886,#46887,#46888),
 .UNSPECIFIED.,.F.,.F.,(4,2,2,2,2,2,2,2,2,2,2,2,2,2,2,2,2,4),(-12.7348788498405,
-12.6874188698587,-12.6287608191211,-12.5694727238362,-12.512281974616,
-12.4528479617241,-12.3954247373668,-12.337566819066,-12.2782189630685,
-12.2215392485701,-12.1630350707807,-12.1031371006023,-12.0460668731077,
-11.986768228256,-11.9289949150521,-11.8712537287554,-11.8118648425648,
-11.7943289504834),.UNSPECIFIED.);
#544=B_SPLINE_CURVE_WITH_KNOTS('',3,(#46889,#46890,#46891,#46892,#46893,
#46894,#46895,#46896,#46897,#46898,#46899,#46900,#46901,#46902,#46903,#46904,
#46905,#46906,#46907,#46908,#46909,#46910,#46911,#46912,#46913,#46914,#46915,
#46916,#46917,#46918,#46919,#46920,#46921,#46922,#46923,#46924),
 .UNSPECIFIED.,.F.,.F.,(4,2,2,2,2,2,2,2,2,2,2,2,2,2,2,2,2,4),(-2.72088258416467,
-2.70722964809425,-2.64756329476097,-2.58939773754221,-2.53166122802283,
-2.47191145895106,-2.41441668652848,-2.3548006927746,-2.29583132696041,
-2.23887512009193,-2.17922386530305,-2.12090205431747,-2.06345033675333,
-2.00352534511469,-1.94587345157856,-1.88681170049432,-1.82765340162895,
-1.77549971424008),.UNSPECIFIED.);
#545=B_SPLINE_CURVE_WITH_KNOTS('',3,(#46929,#46930,#46931,#46932,#46933,
#46934,#46935,#46936,#46937,#46938,#46939,#46940,#46941,#46942,#46943,#46944,
#46945,#46946,#46947,#46948,#46949,#46950,#46951,#46952,#46953,#46954,#46955,
#46956,#46957,#46958,#46959,#46960,#46961,#46962,#46963,#46964),
 .UNSPECIFIED.,.F.,.F.,(4,2,2,2,2,2,2,2,2,2,2,2,2,2,2,2,2,4),(-13.6754849562843,
-13.6190227092761,-13.5599587753475,-13.5016793981831,-13.4441430123469,
-13.3843245242679,-13.3273749651957,-13.269170262857,-13.2098232086566,
-13.1531017200101,-13.0942551920742,-13.0355170596057,-12.978169433214,
-12.9185604858425,-12.8614191319234,-12.8034051476152,-12.7440718372722,
-12.7348788498405),.UNSPECIFIED.);
#546=B_SPLINE_CURVE_WITH_KNOTS('',3,(#46965,#46966,#46967,#46968,#46969,
#46970,#46971,#46972,#46973,#46974,#46975,#46976,#46977,#46978,#46979,#46980,
#46981,#46982,#46983,#46984,#46985,#46986,#46987,#46988,#46989,#46990,#46991,
#46992,#46993,#46994,#46995,#46996,#46997,#46998,#46999,#47000,#47001,#47002),
 .UNSPECIFIED.,.F.,.F.,(4,2,2,2,2,2,2,2,2,2,2,2,2,2,2,2,2,2,4),(-1.77549971424008,
-1.77063002140922,-1.71096546150082,-1.65245246961115,-1.59519526069461,
-1.53506016305706,-1.4772190143837,-1.41862028356561,-1.35924387185229,
-1.30205503267682,-1.2423462699575,-1.18361240910777,-1.12644846804497,
-1.06607365316599,-1.00801565210581,-0.949767234086745,-0.890148542862124,
-0.832767419266973,-0.829142789718882),.UNSPECIFIED.);
#547=B_SPLINE_CURVE_WITH_KNOTS('',3,(#47008,#47009,#47010,#47011,#47012,
#47013,#47014,#47015,#47016,#47017,#47018,#47019,#47020,#47021,#47022,#47023,
#47024,#47025,#47026,#47027),.UNSPECIFIED.,.F.,.F.,(4,2,2,2,2,2,2,2,2,4),
(11.4063709592788,11.4483123767435,11.4945291489478,11.5392425816036,11.5860765085847,
11.6317930050088,11.6770207952941,11.723975630726,11.7607854872426,11.7962920971555),
 .UNSPECIFIED.);
#548=B_SPLINE_CURVE_WITH_KNOTS('',3,(#47030,#47031,#47032,#47033,#47034,
#47035,#47036,#47037,#47038,#47039,#47040,#47041,#47042,#47043,#47044,#47045,
#47046,#47047),.UNSPECIFIED.,.F.,.F.,(4,2,2,2,2,2,2,2,4),(0.,0.0289335200264656,
0.0567950287426251,0.102031362436064,0.149040124071446,0.194408682186974,
0.240180552923466,0.287104886295882,0.297239095913451),.UNSPECIFIED.);
#549=B_SPLINE_CURVE_WITH_KNOTS('',3,(#47052,#47053,#47054,#47055,#47056,
#47057,#47058,#47059,#47060,#47061,#47062,#47063,#47064,#47065,#47066,#47067,
#47068,#47069,#47070,#47071,#47072,#47073,#47074,#47075,#47076,#47077,#47078,
#47079,#47080,#47081,#47082,#47083,#47084,#47085,#47086,#47087,#47088,#47089),
 .UNSPECIFIED.,.F.,.F.,(4,2,2,2,2,2,2,2,2,2,2,2,2,2,2,2,2,2,4),(10.6639140416271,
10.6650947082322,10.7119817347136,10.7580804193876,10.8029993273581,10.8503734008782,
10.8959427839672,10.9417692986129,10.9885470228329,11.0335695774763,11.0804254452447,
11.1265643813013,11.1713443335741,11.218213374293,11.2638454555082,11.3093155266254,
11.3561724820038,11.4012663166318,11.4063709592788),.UNSPECIFIED.);
#550=B_SPLINE_CURVE_WITH_KNOTS('',3,(#47090,#47091,#47092,#47093,#47094,
#47095,#47096,#47097,#47098,#47099,#47100,#47101,#47102,#47103,#47104,#47105,
#47106,#47107,#47108,#47109,#47110,#47111,#47112,#47113,#47114,#47115,#47116,
#47117,#47118,#47119,#47120,#47121,#47122,#47123,#47124,#47125),
 .UNSPECIFIED.,.F.,.F.,(4,2,2,2,2,2,2,2,2,2,2,2,2,2,2,2,2,4),(0.297239095913451,
0.331909892910397,0.378184802292447,0.425437891635738,0.470595177353486,
0.517516832751099,0.563142306369242,0.608840424213731,0.655808186318039,
0.700696994400866,0.746904510560702,0.793857785223327,0.838950917376441,
0.885800877455259,0.931807710447616,0.977451263235396,1.0249004194449,1.04102688126702),
 .UNSPECIFIED.);
#551=B_SPLINE_CURVE_WITH_KNOTS('',3,(#47130,#47131,#47132,#47133,#47134,
#47135,#47136,#47137,#47138,#47139,#47140,#47141,#47142,#47143,#47144,#47145,
#47146,#47147,#47148,#47149,#47150,#47151,#47152,#47153,#47154,#47155,#47156,
#47157,#47158,#47159,#47160,#47161,#47162,#47163,#47164,#47165),
 .UNSPECIFIED.,.F.,.F.,(4,2,2,2,2,2,2,2,2,2,2,2,2,2,2,2,2,4),(9.92229190963911,
9.92979763035616,9.97661529584815,10.0223875882399,10.0674947390005,10.1145130077351,
10.1597537191833,10.2061418234609,10.252546736718,10.2972921295131,10.3441264845473,
10.3900441574768,10.4350167599153,10.4821947166382,10.5275825848168,10.5736460837947,
10.6202215550774,10.6639140416271),.UNSPECIFIED.);
#552=B_SPLINE_CURVE_WITH_KNOTS('',3,(#47166,#47167,#47168,#47169,#47170,
#47171,#47172,#47173,#47174,#47175,#47176,#47177,#47178,#47179,#47180,#47181,
#47182,#47183,#47184,#47185,#47186,#47187,#47188,#47189,#47190,#47191,#47192,
#47193,#47194,#47195,#47196,#47197,#47198,#47199,#47200,#47201),
 .UNSPECIFIED.,.F.,.F.,(4,2,2,2,2,2,2,2,2,2,2,2,2,2,2,2,2,4),(1.04102688126702,
1.06994936982564,1.11612372964813,1.1631224274379,1.20807774239958,1.25473316609544,
1.30100208017051,1.34647258781685,1.39373457189629,1.43885942222957,1.48486151898195,
1.53181724470879,1.57666541818597,1.62315856887522,1.66977391100141,1.71510631020256,
1.76221822633913,1.78477649063309),.UNSPECIFIED.);
#553=B_SPLINE_CURVE_WITH_KNOTS('',3,(#47206,#47207,#47208,#47209,#47210,
#47211,#47212,#47213,#47214,#47215,#47216,#47217,#47218,#47219,#47220,#47221,
#47222,#47223,#47224,#47225,#47226,#47227,#47228,#47229,#47230,#47231,#47232,
#47233,#47234,#47235,#47236,#47237,#47238,#47239,#47240,#47241),
 .UNSPECIFIED.,.F.,.F.,(4,2,2,2,2,2,2,2,2,2,2,2,2,2,2,2,2,4),(9.18066291513125,
9.19415090290438,9.24103359345902,9.28663151390442,9.33221017295977,9.37902708695585,
9.42408423987445,9.47131574850735,9.51748383149001,9.56220744499011,9.60904188441202,
9.65470687463485,9.70002122809167,9.74691845045314,9.7920482780309,9.83883277613507,
9.88510096784626,9.92229190963911),.UNSPECIFIED.);
#554=B_SPLINE_CURVE_WITH_KNOTS('',3,(#47242,#47243,#47244,#47245,#47246,
#47247,#47248,#47249,#47250,#47251,#47252,#47253,#47254,#47255,#47256,#47257,
#47258,#47259,#47260,#47261,#47262,#47263,#47264,#47265,#47266,#47267,#47268,
#47269,#47270,#47271,#47272,#47273,#47274,#47275,#47276,#47277),
 .UNSPECIFIED.,.F.,.F.,(4,2,2,2,2,2,2,2,2,2,2,2,2,2,2,2,2,4),(1.78477649063309,
1.80749817211998,1.85336437928791,1.90031249731947,1.94513254024406,1.99149805378257,
2.03852655563362,2.08375775348993,2.13075894105089,2.17626379582903,2.22203292704428,
2.26900641402836,2.31387226672767,2.36014760821912,2.40710960481156,2.4522612783082,
2.49917450341029,2.52844772796884),.UNSPECIFIED.);
#555=B_SPLINE_CURVE_WITH_KNOTS('',3,(#47282,#47283,#47284,#47285,#47286,
#47287,#47288,#47289,#47290,#47291,#47292,#47293,#47294,#47295,#47296,#47297,
#47298,#47299,#47300,#47301,#47302,#47303,#47304,#47305,#47306,#47307,#47308,
#47309,#47310,#47311,#47312,#47313,#47314,#47315,#47316,#47317),
 .UNSPECIFIED.,.F.,.F.,(4,2,2,2,2,2,2,2,2,2,2,2,2,2,2,2,2,4),(8.43774741884447,
8.45752571504742,8.50469343833677,8.5500742626266,8.59632293033626,8.64288344885183,
8.68775172489367,8.73467282146192,8.78075134679685,8.82574058111398,8.87308972399771,
8.91863816774379,8.9646115037511,9.01136150601258,9.05635901694108,9.10322659194124,
9.14933383291891,9.18066291513125),.UNSPECIFIED.);
#556=B_SPLINE_CURVE_WITH_KNOTS('',3,(#47318,#47319,#47320,#47321,#47322,
#47323,#47324,#47325,#47326,#47327,#47328,#47329,#47330,#47331,#47332,#47333,
#47334,#47335,#47336,#47337,#47338,#47339,#47340,#47341,#47342,#47343,#47344,
#47345,#47346,#47347,#47348,#47349,#47350,#47351,#47352,#47353),
 .UNSPECIFIED.,.F.,.F.,(4,2,2,2,2,2,2,2,2,2,2,2,2,2,2,2,2,4),(2.52844772796884,
2.54500824613052,2.59070535491167,2.638214681952,2.68319585525036,2.72942299914916,
2.77639940937737,2.82139145839567,2.86809231879591,2.91413323574597,2.95963794063351,
3.00693966003781,3.05194785331698,3.09798282203751,3.14489438166212,3.18973360823921,
3.23625334475753,3.27195608346076),.UNSPECIFIED.);
#557=B_SPLINE_CURVE_WITH_KNOTS('',3,(#47358,#47359,#47360,#47361,#47362,
#47363,#47364,#47365,#47366,#47367,#47368,#47369,#47370,#47371,#47372,#47373,
#47374,#47375,#47376,#47377,#47378,#47379,#47380,#47381,#47382,#47383,#47384,
#47385,#47386,#47387,#47388,#47389,#47390,#47391,#47392,#47393),
 .UNSPECIFIED.,.F.,.F.,(4,2,2,2,2,2,2,2,2,2,2,2,2,2,2,2,2,4),(7.69539854103273,
7.72155321848494,7.7684724835817,7.8136255677965,7.86065234102687,7.90693393580434,
7.9516908438395,7.99857209635814,8.04435399500581,8.0895977391991,8.13662142723008,
8.18186980363593,8.22847577989916,8.27487933356857,8.31965265394499,8.3665363700462,
8.41244823537304,8.43774741884447),.UNSPECIFIED.);
#558=B_SPLINE_CURVE_WITH_KNOTS('',3,(#47394,#47395,#47396,#47397,#47398,
#47399,#47400,#47401,#47402,#47403,#47404,#47405,#47406,#47407,#47408,#47409,
#47410,#47411,#47412,#47413,#47414,#47415,#47416,#47417,#47418,#47419,#47420,
#47421,#47422,#47423,#47424,#47425,#47426,#47427,#47428,#47429),
 .UNSPECIFIED.,.F.,.F.,(4,2,2,2,2,2,2,2,2,2,2,2,2,2,2,2,2,4),(3.27195608346076,
3.282592657188,3.3279388134706,3.37506873495414,3.42018650623354,3.46606423055494,
3.51294786154499,3.55771304574351,3.60408475803478,3.65080015723448,3.69602345065255,
3.74301955034469,3.78832280212397,3.83408062999374,3.88097059164275,3.92573930458549,
3.97199874621623,4.01433671221151),.UNSPECIFIED.);
#559=B_SPLINE_CURVE_WITH_KNOTS('',3,(#47434,#47435,#47436,#47437,#47438,
#47439,#47440,#47441,#47442,#47443,#47444,#47445,#47446,#47447,#47448,#47449,
#47450,#47451,#47452,#47453,#47454,#47455,#47456,#47457,#47458,#47459,#47460,
#47461,#47462,#47463,#47464,#47465,#47466,#47467,#47468,#47469),
 .UNSPECIFIED.,.F.,.F.,(4,2,2,2,2,2,2,2,2,2,2,2,2,2,2,2,2,4),(6.95232021216865,
6.98520940682934,7.03183776179107,7.07676034379647,7.12368218105456,7.16983534809316,
7.21477539351345,7.26220706699282,7.30783067803266,7.3536506056871,7.40048621914621,
7.44556384932218,7.49246290359126,7.5386603688324,7.5834734101616,7.63038481462985,
7.67607584920904,7.69539854103273),.UNSPECIFIED.);
#560=B_SPLINE_CURVE_WITH_KNOTS('',3,(#47470,#47471,#47472,#47473,#47474,
#47475,#47476,#47477,#47478,#47479,#47480,#47481,#47482,#47483,#47484,#47485,
#47486,#47487,#47488,#47489,#47490,#47491,#47492,#47493,#47494,#47495,#47496,
#47497,#47498,#47499,#47500,#47501,#47502,#47503,#47504,#47505,#47506,#47507),
 .UNSPECIFIED.,.F.,.F.,(4,2,2,2,2,2,2,2,2,2,2,2,2,2,2,2,2,2,4),(4.01433671221151,
4.01914805413287,4.06428615761616,4.11118860567824,4.15674023560365,4.20241784028498,
4.24934623552864,4.29418852097545,4.34037422725447,4.38728888642649,4.43235854054739,
4.47918474875809,4.52510312300865,4.57072126834585,4.61814520147569,4.66313508164065,
4.70928335610809,4.75623501458851,4.75775515205278),.UNSPECIFIED.);
#561=B_SPLINE_CURVE_WITH_KNOTS('',3,(#47512,#47513,#47514,#47515,#47516,
#47517,#47518,#47519,#47520,#47521,#47522,#47523,#47524,#47525,#47526,#47527,
#47528,#47529,#47530,#47531,#47532,#47533,#47534,#47535,#47536,#47537,#47538,
#47539,#47540,#47541,#47542,#47543,#47544,#47545,#47546,#47547),
 .UNSPECIFIED.,.F.,.F.,(4,2,2,2,2,2,2,2,2,2,2,2,2,2,2,2,2,4),(6.21040332353066,
6.24996363653887,6.29627383230895,6.34099487094829,6.38783578085351,6.43365110481032,
6.47875379116074,6.52581793545371,6.57110181115006,6.61745562645394,6.66390817507345,
6.70869049645745,6.75555365022892,6.80152025981645,6.84650073651534,6.89373059013836,
6.93916728504739,6.95232021216865),.UNSPECIFIED.);
#562=B_SPLINE_CURVE_WITH_KNOTS('',3,(#47548,#47549,#47550,#47551,#47552,
#47553,#47554,#47555,#47556,#47557,#47558,#47559,#47560,#47561,#47562,#47563,
#47564,#47565,#47566,#47567,#47568,#47569,#47570,#47571,#47572,#47573,#47574,
#47575,#47576,#47577,#47578,#47579,#47580,#47581,#47582,#47583),
 .UNSPECIFIED.,.F.,.F.,(4,2,2,2,2,2,2,2,2,2,2,2,2,2,2,2,2,4),(4.75775515205278,
4.80115954720664,4.84778657251392,4.89395239727177,4.93939241272434,4.98662379950037,
5.03167653106206,5.07764728797061,5.12455025523998,5.16935540816532,5.21581518399032,
5.26231483989851,5.30761133212679,5.3546868913279,5.39988274125814,5.44571192890845,
5.4926019451231,5.50046293121957),.UNSPECIFIED.);
#563=B_SPLINE_CURVE_WITH_KNOTS('',3,(#47588,#47589,#47590,#47591,#47592,
#47593,#47594,#47595,#47596,#47597,#47598,#47599,#47600,#47601,#47602,#47603,
#47604,#47605,#47606,#47607,#47608,#47609,#47610,#47611,#47612,#47613,#47614,
#47615,#47616,#47617,#47618,#47619,#47620,#47621,#47622,#47623,#47624,#47625),
 .UNSPECIFIED.,.F.,.F.,(4,2,2,2,2,2,2,2,2,2,2,2,2,2,2,2,2,2,4),(5.46823516997428,
5.46924523189168,5.51421339539498,5.56093347890932,5.60681683684292,5.65233399971011,
5.69965169327359,5.74457803521868,5.79062455915303,5.83749440380915,5.8823256252987,
5.92852964558371,5.97326608757821,6.0201185992117,6.06582034727076,6.11111957359516,
6.15805631170891,6.20322334029363,6.21040332353066),.UNSPECIFIED.);
#564=B_SPLINE_CURVE_WITH_KNOTS('',3,(#47626,#47627,#47628,#47629,#47630,
#47631,#47632,#47633,#47634,#47635,#47636,#47637,#47638,#47639,#47640,#47641,
#47642,#47643,#47644,#47645,#47646,#47647,#47648,#47649,#47650,#47651,#47652,
#47653,#47654,#47655,#47656,#47657,#47658,#47659,#47660,#47661),
 .UNSPECIFIED.,.F.,.F.,(4,2,2,2,2,2,2,2,2,2,2,2,2,2,2,2,2,4),(5.50046293121957,
5.53736683161235,5.58369353071173,5.6305968047525,5.67578632165126,5.72274499816332,
5.76815552869047,5.81388154564766,5.86079188348587,5.90559155055078,5.95219446597211,
5.9970962044243,6.04402631060266,6.09015041966504,6.13512165037609,6.18252051520117,
6.22811471720219,6.24337196603104),.UNSPECIFIED.);
#565=B_SPLINE_CURVE_WITH_KNOTS('',3,(#47666,#47667,#47668,#47669,#47670,
#47671,#47672,#47673,#47674,#47675,#47676,#47677,#47678,#47679,#47680,#47681,
#47682,#47683,#47684,#47685,#47686,#47687,#47688,#47689,#47690,#47691,#47692,
#47693,#47694,#47695,#47696,#47697,#47698,#47699,#47700,#47701),
 .UNSPECIFIED.,.F.,.F.,(4,2,2,2,2,2,2,2,2,2,2,2,2,2,2,2,2,4),(4.72706962089855,
4.73421323881064,4.77932354628057,4.82620128907514,4.87144673700927,4.91709114393615,
4.96388604536429,5.0085677160079,5.05471383888917,5.10184091457902,5.14687278115198,
5.19366407264861,5.2391662347845,5.28473750147929,5.33157602074619,5.37634188682691,
5.42242120372861,5.46823516997428),.UNSPECIFIED.);
#566=B_SPLINE_CURVE_WITH_KNOTS('',3,(#47702,#47703,#47704,#47705,#47706,
#47707,#47708,#47709,#47710,#47711,#47712,#47713,#47714,#47715,#47716,#47717,
#47718,#47719,#47720,#47721,#47722,#47723,#47724,#47725,#47726,#47727,#47728,
#47729,#47730,#47731,#47732,#47733,#47734,#47735,#47736,#47737),
 .UNSPECIFIED.,.F.,.F.,(4,2,2,2,2,2,2,2,2,2,2,2,2,2,2,2,2,4),(6.24337196603104,
6.27401821929249,6.32081950996656,6.36586527339041,6.4127571572649,6.4589180548967,
6.50373993867417,6.55064566532991,6.59629857778885,6.64183340160009,6.68871022418118,
6.73382376991178,6.78095970840426,6.82719337080345,6.87194020815821,6.91880678990272,
6.9645389314372,6.98590521985964),.UNSPECIFIED.);
#567=B_SPLINE_CURVE_WITH_KNOTS('',3,(#47742,#47743,#47744,#47745,#47746,
#47747,#47748,#47749,#47750,#47751,#47752,#47753,#47754,#47755,#47756,#47757,
#47758,#47759,#47760,#47761,#47762,#47763,#47764,#47765,#47766,#47767,#47768,
#47769,#47770,#47771,#47772,#47773,#47774,#47775,#47776,#47777),
 .UNSPECIFIED.,.F.,.F.,(4,2,2,2,2,2,2,2,2,2,2,2,2,2,2,2,2,4),(3.98607357350402,
3.99918191936072,4.04456087825365,4.09173064872777,4.13665634482318,4.18256457182781,
4.22936946042104,4.27409551151173,4.32048917025343,4.36678906526987,4.41201572517385,
4.45902034323992,4.50406884281734,4.54982631660765,4.5966093208145,4.64127491262894,
4.68752672363699,4.72706962089855),.UNSPECIFIED.);
#568=B_SPLINE_CURVE_WITH_KNOTS('',3,(#47778,#47779,#47780,#47781,#47782,
#47783,#47784,#47785,#47786,#47787,#47788,#47789,#47790,#47791,#47792,#47793,
#47794,#47795,#47796,#47797,#47798,#47799,#47800,#47801,#47802,#47803,#47804,
#47805,#47806,#47807,#47808,#47809,#47810,#47811,#47812,#47813),
 .UNSPECIFIED.,.F.,.F.,(4,2,2,2,2,2,2,2,2,2,2,2,2,2,2,2,2,4),(6.98590521985964,
7.00982424920481,7.05679371040423,7.10199149720955,7.1486926619025,7.19503766539008,
7.23977922568632,7.28663870486131,7.3324897765694,7.37758804450172,7.42469034180235,
7.47001006811599,7.51633373613469,7.56282588238178,7.60763958801924,7.65452614947266,
7.70053353816524,7.7280430341459),.UNSPECIFIED.);
#569=B_SPLINE_CURVE_WITH_KNOTS('',3,(#47818,#47819,#47820,#47821,#47822,
#47823,#47824,#47825,#47826,#47827,#47828,#47829,#47830,#47831,#47832,#47833,
#47834,#47835,#47836,#47837,#47838,#47839,#47840,#47841,#47842,#47843,#47844,
#47845,#47846,#47847,#47848,#47849,#47850,#47851,#47852,#47853),
 .UNSPECIFIED.,.F.,.F.,(4,2,2,2,2,2,2,2,2,2,2,2,2,2,2,2,2,4),(3.24392841407934,
3.26320118186788,3.30883357721227,3.35568585153,3.40044282038451,3.44658106056088,
3.49342094952175,3.53844090839015,3.58521656152064,3.63098154698795,3.67654687597848,
3.72391788461319,3.76880240701922,3.81489663770949,3.86175977891139,3.9066251798824,
3.95319412178152,3.98607357350402),.UNSPECIFIED.);
#570=B_SPLINE_CURVE_WITH_KNOTS('',3,(#47854,#47855,#47856,#47857,#47858,
#47859,#47860,#47861,#47862,#47863,#47864,#47865,#47866,#47867,#47868,#47869,
#47870,#47871,#47872,#47873,#47874,#47875,#47876,#47877,#47878,#47879,#47880,
#47881,#47882,#47883,#47884,#47885,#47886,#47887,#47888,#47889),
 .UNSPECIFIED.,.F.,.F.,(4,2,2,2,2,2,2,2,2,2,2,2,2,2,2,2,2,4),(7.7280430341459,
7.74552040966934,7.79279355251667,7.83827093210572,7.8842943505838,7.93096677709508,
7.97593141803747,8.02288189886512,8.06908057135937,8.1140384707018,8.16151829876598,
8.20718720882142,8.25300132576618,8.2998852910774,8.34500889959013,8.39194375347128,
8.43819004733793,8.47155481750159),.UNSPECIFIED.);
#571=B_SPLINE_CURVE_WITH_KNOTS('',3,(#47894,#47895,#47896,#47897,#47898,
#47899,#47900,#47901,#47902,#47903,#47904,#47905,#47906,#47907,#47908,#47909,
#47910,#47911,#47912,#47913,#47914,#47915,#47916,#47917,#47918,#47919,#47920,
#47921,#47922,#47923,#47924,#47925,#47926,#47927,#47928,#47929),
 .UNSPECIFIED.,.F.,.F.,(4,2,2,2,2,2,2,2,2,2,2,2,2,2,2,2,2,4),(2.50252141868207,
2.52776021043164,2.57361244595458,2.62043647340302,2.6651524611521,2.71149584066551,
2.75804622814296,2.80323613082756,2.85019899727244,2.89538716038286,2.941109939166,
2.98793181216642,3.03263210415199,3.07885401093438,3.12582513877793,3.17092021696239,
3.21777916276462,3.24392841407934),.UNSPECIFIED.);
#572=B_SPLINE_CURVE_WITH_KNOTS('',3,(#47930,#47931,#47932,#47933,#47934,
#47935,#47936,#47937,#47938,#47939,#47940,#47941,#47942,#47943,#47944,#47945,
#47946,#47947,#47948,#47949,#47950,#47951,#47952,#47953,#47954,#47955,#47956,
#47957,#47958,#47959,#47960,#47961,#47962,#47963,#47964,#47965),
 .UNSPECIFIED.,.F.,.F.,(4,2,2,2,2,2,2,2,2,2,2,2,2,2,2,2,2,4),(8.47155481750159,
8.48303098251424,8.52997744983096,8.57571769446406,8.62120106342097,8.66817233854124,
8.71337485643584,8.76038502225125,8.80672058392342,8.8515142195167,8.89843463378869,
8.94427102223284,8.98952825218029,9.0366093049851,9.0819121341257,9.12850816287234,
9.17497049631086,9.21453814874152),.UNSPECIFIED.);
#573=B_SPLINE_CURVE_WITH_KNOTS('',3,(#47970,#47971,#47972,#47973,#47974,
#47975,#47976,#47977,#47978,#47979,#47980,#47981,#47982,#47983,#47984,#47985,
#47986,#47987,#47988,#47989,#47990,#47991,#47992,#47993,#47994,#47995,#47996,
#47997,#47998,#47999,#48000,#48001,#48002,#48003,#48004,#48005),
 .UNSPECIFIED.,.F.,.F.,(4,2,2,2,2,2,2,2,2,2,2,2,2,2,2,2,2,4),(1.76055864693328,
1.79182126771535,1.83786803837673,1.88467512490527,1.92961375851794,1.97630255407359,
2.0222196260872,2.0677085751512,2.11499580318964,2.15992835930496,2.20594672076016,
2.2528077518393,2.29761785291437,2.34411769224053,2.39031055560415,2.43563240933956,
2.48273877805656,2.50252141868207),.UNSPECIFIED.);
#574=B_SPLINE_CURVE_WITH_KNOTS('',3,(#48006,#48007,#48008,#48009,#48010,
#48011,#48012,#48013,#48014,#48015,#48016,#48017,#48018,#48019,#48020,#48021,
#48022,#48023,#48024,#48025,#48026,#48027,#48028,#48029,#48030,#48031,#48032,
#48033,#48034,#48035,#48036,#48037,#48038,#48039,#48040,#48041,#48042,#48043),
 .UNSPECIFIED.,.F.,.F.,(4,2,2,2,2,2,2,2,2,2,2,2,2,2,2,2,2,2,4),(9.21453814874152,
9.21979055026988,9.26671782254207,9.31268919604266,9.35778979281078,9.40501998742909,
9.45046005687993,9.4967081920225,9.54333197258473,9.58825736766484,9.63522678342864,
9.68136954756796,9.72639248238748,9.77380894901864,9.81942121560885,9.86540543979499,
9.91222295415185,9.95728494289229,9.95826087397132),.UNSPECIFIED.);
#575=B_SPLINE_CURVE_WITH_KNOTS('',3,(#48048,#48049,#48050,#48051,#48052,
#48053,#48054,#48055,#48056,#48057,#48058,#48059,#48060,#48061,#48062,#48063,
#48064,#48065,#48066,#48067,#48068,#48069,#48070,#48071,#48072,#48073,#48074,
#48075,#48076,#48077,#48078,#48079,#48080,#48081,#48082,#48083),
 .UNSPECIFIED.,.F.,.F.,(4,2,2,2,2,2,2,2,2,2,2,2,2,2,2,2,2,4),(1.0198908055646,
1.05700253667009,1.10320928671584,1.14993696120769,1.19500709107715,1.24184222630525,
1.28709985760173,1.33270449750631,1.379478231302,1.42414417613706,1.4702513175641,
1.51742579982366,1.56242372917786,1.6091790650006,1.65470112473219,1.70023918105991,
1.74706140067451,1.76055864693328),.UNSPECIFIED.);
#576=B_SPLINE_CURVE_WITH_KNOTS('',3,(#48084,#48085,#48086,#48087,#48088,
#48089,#48090,#48091,#48092,#48093,#48094,#48095,#48096,#48097,#48098,#48099,
#48100,#48101,#48102,#48103,#48104,#48105,#48106,#48107,#48108,#48109,#48110,
#48111,#48112,#48113,#48114,#48115,#48116,#48117,#48118,#48119),
 .UNSPECIFIED.,.F.,.F.,(4,2,2,2,2,2,2,2,2,2,2,2,2,2,2,2,2,4),(9.95826087397132,
10.0042077855434,10.0503830644129,10.0952441977488,10.1421816171258,10.1878477047942,
10.2334488002604,10.2803373027871,10.3254627794739,10.3726944829175,10.4189361962616,
10.4637121618962,10.5106054781006,10.5563443378488,10.60168753486,10.6486621415555,
10.693865727852,10.7009872972758),.UNSPECIFIED.);
#577=B_SPLINE_CURVE_WITH_KNOTS('',3,(#48124,#48125,#48126,#48127,#48128,
#48129,#48130,#48131,#48132,#48133,#48134,#48135,#48136,#48137,#48138,#48139,
#48140,#48141,#48142,#48143,#48144,#48145,#48146,#48147,#48148,#48149,#48150,
#48151,#48152,#48153,#48154,#48155,#48156,#48157,#48158,#48159),
 .UNSPECIFIED.,.F.,.F.,(4,2,2,2,2,2,2,2,2,2,2,2,2,2,2,2,2,4),(0.279240333252414,
0.322844270949173,0.369357241132825,0.415363471402469,0.46069060038965,
0.507805353095372,0.55272028410885,0.598576537627569,0.645349536044773,
0.69003577120083,0.736378722628649,0.782709920293503,0.827890427170548,
0.874846064622692,0.919896118269451,0.965607538883625,1.01236420598534,
1.0198908055646),.UNSPECIFIED.);
#578=B_SPLINE_CURVE_WITH_KNOTS('',3,(#48160,#48161,#48162,#48163,#48164,
#48165,#48166,#48167,#48168,#48169,#48170,#48171,#48172,#48173,#48174,#48175,
#48176,#48177,#48178,#48179,#48180,#48181,#48182,#48183,#48184,#48185,#48186,
#48187,#48188,#48189,#48190,#48191,#48192,#48193,#48194,#48195),
 .UNSPECIFIED.,.F.,.F.,(4,2,2,2,2,2,2,2,2,2,2,2,2,2,2,2,2,4),(10.7009872972758,
10.7406554053031,10.7870025479307,10.8317614667191,10.8786424437052,10.9244941101883,
10.9696390710423,11.0167403153779,11.0620600256883,11.1084614451944,11.154950288831,
11.1997687866196,11.2466712469847,11.2926735167475,11.337694414731,11.3849606827389,
11.4304325644015,11.4435301988629),.UNSPECIFIED.);
#579=B_SPLINE_CURVE_WITH_KNOTS('',3,(#48198,#48199,#48200,#48201,#48202,
#48203,#48204,#48205,#48206,#48207,#48208,#48209,#48210,#48211,#48212,#48213,
#48214,#48215,#48216,#48217),.UNSPECIFIED.,.F.,.F.,(4,2,2,2,2,2,2,2,2,4),
(11.4435301988629,11.4765201718647,11.5231842534289,11.5681413990089,11.6151017516702,
11.6612899790245,11.7062685498772,11.753736029675,11.7850799770424,11.815365841815),
 .UNSPECIFIED.);
#580=B_SPLINE_CURVE_WITH_KNOTS('',3,(#48220,#48221,#48222,#48223,#48224,
#48225,#48226,#48227,#48228,#48229,#48230,#48231,#48232,#48233,#48234,#48235,
#48236,#48237),.UNSPECIFIED.,.F.,.F.,(4,2,2,2,2,2,2,2,4),(9.99999983579279E-7,
0.0240245188069277,0.0474912529693272,0.0929991717620865,0.140309272354935,
0.185169608656008,0.231206138227982,0.278031208662583,0.279240333252414),
 .UNSPECIFIED.);
#581=B_SPLINE_CURVE_WITH_KNOTS('',3,(#48240,#48241,#48242,#48243,#48244,
#48245,#48246,#48247,#48248,#48249,#48250,#48251,#48252,#48253,#48254,#48255,
#48256,#48257,#48258,#48259,#48260,#48261,#48262,#48263,#48264,#48265,#48266,
#48267,#48268,#48269,#48270,#48271),.UNSPECIFIED.,.F.,.F.,(4,2,2,2,2,2,
2,2,2,2,2,2,2,2,2,4),(-0.829142789718882,-0.77306457962365,-0.714223388829787,
-0.65718540765388,-0.597470281301096,-0.539279665144528,-0.481455062329678,
-0.4216816411846,-0.364162666057075,-0.304420722553672,-0.245430580868346,
-0.188433357111664,-0.128737077916135,-0.0703952695266761,-0.0354402198856821,
-9.99999999917733E-7),.UNSPECIFIED.);
#582=B_SPLINE_CURVE_WITH_KNOTS('',3,(#48274,#48275,#48276,#48277,#48278,
#48279,#48280,#48281,#48282,#48283,#48284,#48285,#48286,#48287,#48288,#48289,
#48290,#48291,#48292,#48293,#48294,#48295,#48296,#48297,#48298,#48299,#48300,
#48301,#48302,#48303),.UNSPECIFIED.,.F.,.F.,(4,2,2,2,2,2,2,2,2,2,2,2,2,
2,4),(-14.3815521744247,-14.3490819882549,-14.3173656294494,-14.2606308082457,
-14.2020989293593,-14.1427123139841,-14.0856330557203,-14.026327836904,
-13.9683949339112,-13.9106424935611,-13.8505851839565,-13.7937266961226,
-13.7353019168941,-13.6759104215302,-13.6754849562843),.UNSPECIFIED.);
#583=B_SPLINE_CURVE_WITH_KNOTS('',3,(#48322,#48323,#48324,#48325,#48326,
#48327,#48328,#48329,#48330,#48331,#48332,#48333,#48334,#48335,#48336,#48337,
#48338,#48339,#48340,#48341,#48342,#48343,#48344,#48345,#48346,#48347),
 .UNSPECIFIED.,.F.,.F.,(4,2,2,2,2,2,2,2,2,2,2,2,4),(0.480400932349348,0.485329977931986,
0.530683146887141,0.579550101290595,0.64089353991474,0.720505764207005,
0.804785042766715,0.896510611485352,0.997812688736786,1.10248963403809,
1.17665715785729,1.21374936533913,1.25141712065186),.UNSPECIFIED.);
#584=B_SPLINE_CURVE_WITH_KNOTS('',3,(#48351,#48352,#48353,#48354,#48355,
#48356,#48357,#48358,#48359,#48360,#48361,#48362,#48363,#48364,#48365,#48366),
 .UNSPECIFIED.,.F.,.F.,(4,2,2,2,2,2,2,4),(0.,0.0362708955824572,0.085273156200874,
0.169912753697905,0.248908834870632,0.337286385899651,0.42390178686825,
0.480400932349348),.UNSPECIFIED.);
#585=B_SPLINE_CURVE_WITH_KNOTS('',3,(#48367,#48368,#48369,#48370,#48371,
#48372,#48373,#48374,#48375,#48376,#48377,#48378),.UNSPECIFIED.,.F.,.F.,
(4,2,2,2,2,4),(-0.173020928061641,-0.143983119462096,-0.113362764878225,
-0.0824055056388063,-0.0457488593866804,-9.99999131029439E-7),
 .UNSPECIFIED.);
#586=B_SPLINE_CURVE_WITH_KNOTS('',3,(#48778,#48779,#48780,#48781,#48782,
#48783,#48784,#48785,#48786,#48787,#48788,#48789,#48790,#48791,#48792,#48793),
 .UNSPECIFIED.,.F.,.F.,(4,2,2,2,2,2,2,4),(-0.193591868481661,-0.164589722295103,
-0.136229103543845,-0.109019089206068,-0.086513074650219,-0.0622509824423357,
-0.0393944302207767,-1.00000006228451E-6),.UNSPECIFIED.);
#587=B_SPLINE_CURVE_WITH_KNOTS('',3,(#49184,#49185,#49186,#49187,#49188,
#49189,#49190,#49191,#49192,#49193,#49194,#49195,#49196,#49197,#49198,#49199,
#49200,#49201),.UNSPECIFIED.,.F.,.F.,(4,2,2,2,2,2,2,2,4),(-0.298889159334175,
-0.248475417408008,-0.215742180818938,-0.174449183868093,-0.150666431566684,
-0.103667997862826,-0.0537346078292575,-0.0261328721932875,-1.00000013070201E-6),
 .UNSPECIFIED.);
#655=CONICAL_SURFACE('',#10937,0.00115470053837925,0.78539816339745);
#656=CONICAL_SURFACE('',#10944,0.001125,0.785398163397445);
#657=CONICAL_SURFACE('',#10954,0.00115470053837925,0.78539816339745);
#658=CONICAL_SURFACE('',#10955,0.00115470053837925,0.78539816339745);
#659=CONICAL_SURFACE('',#10956,0.00115470053837925,0.78539816339745);
#660=CONICAL_SURFACE('',#10957,0.00115470053837925,0.78539816339745);
#661=CONICAL_SURFACE('',#10958,0.00115470053837925,0.78539816339745);
#681=(
BOUNDED_CURVE()
B_SPLINE_CURVE(2,(#48307,#48308,#48309),.UNSPECIFIED.,.F.,.F.)
B_SPLINE_CURVE_WITH_KNOTS((3,3),(-0.321867155116299,-0.124274873543865),
 .UNSPECIFIED.)
CURVE()
GEOMETRIC_REPRESENTATION_ITEM()
RATIONAL_B_SPLINE_CURVE((1.46410161513778,1.69059892324148,1.46410161513778))
REPRESENTATION_ITEM('')
);
#682=(
BOUNDED_CURVE()
B_SPLINE_CURVE(2,(#49214,#49215,#49216),.UNSPECIFIED.,.F.,.F.)
B_SPLINE_CURVE_WITH_KNOTS((3,3),(-0.3218671551163,-0.124274873543865),
 .UNSPECIFIED.)
CURVE()
GEOMETRIC_REPRESENTATION_ITEM()
RATIONAL_B_SPLINE_CURVE((1.46410161513778,1.69059892324148,1.46410161513778))
REPRESENTATION_ITEM('')
);
#683=(
BOUNDED_CURVE()
B_SPLINE_CURVE(2,(#49218,#49219,#49220),.UNSPECIFIED.,.F.,.F.)
B_SPLINE_CURVE_WITH_KNOTS((3,3),(-0.321867155116299,-0.124274873543866),
 .UNSPECIFIED.)
CURVE()
GEOMETRIC_REPRESENTATION_ITEM()
RATIONAL_B_SPLINE_CURVE((1.46410161513778,1.69059892324148,1.46410161513778))
REPRESENTATION_ITEM('')
);
#684=(
BOUNDED_CURVE()
B_SPLINE_CURVE(2,(#49222,#49223,#49224),.UNSPECIFIED.,.F.,.F.)
B_SPLINE_CURVE_WITH_KNOTS((3,3),(-0.3218671551163,-0.124274873543865),
 .UNSPECIFIED.)
CURVE()
GEOMETRIC_REPRESENTATION_ITEM()
RATIONAL_B_SPLINE_CURVE((1.46410161513778,1.69059892324148,1.46410161513778))
REPRESENTATION_ITEM('')
);
#685=(
BOUNDED_CURVE()
B_SPLINE_CURVE(2,(#49226,#49227,#49228),.UNSPECIFIED.,.F.,.F.)
B_SPLINE_CURVE_WITH_KNOTS((3,3),(-0.3218671551163,-0.124274873543865),
 .UNSPECIFIED.)
CURVE()
GEOMETRIC_REPRESENTATION_ITEM()
RATIONAL_B_SPLINE_CURVE((1.46410161513778,1.69059892324148,1.46410161513778))
REPRESENTATION_ITEM('')
);
#686=(
BOUNDED_CURVE()
B_SPLINE_CURVE(2,(#49230,#49231,#49232),.UNSPECIFIED.,.F.,.F.)
B_SPLINE_CURVE_WITH_KNOTS((3,3),(-0.321867155116299,-0.124274873543866),
 .UNSPECIFIED.)
CURVE()
GEOMETRIC_REPRESENTATION_ITEM()
RATIONAL_B_SPLINE_CURVE((1.46410161513778,1.69059892324148,1.46410161513778))
REPRESENTATION_ITEM('')
);
#764=FACE_BOUND('',#2197,.T.);
#765=FACE_BOUND('',#2203,.T.);
#766=FACE_BOUND('',#2205,.T.);
#796=SHAPE_REPRESENTATION_RELATIONSHIP('SRR','None',#50164,#816);
#816=ADVANCED_BREP_SHAPE_REPRESENTATION('',(#856),#50077);
#836=STYLED_ITEM('',(#50258),#856);
#856=MANIFOLD_SOLID_BREP('Body1',#9881);
#1085=PLANE('',#10946);
#1086=PLANE('',#10947);
#1087=PLANE('',#10953);
#1088=PLANE('',#10959);
#1089=PLANE('',#10960);
#1090=PLANE('',#10961);
#1091=PLANE('',#10962);
#1092=PLANE('',#10963);
#1093=PLANE('',#10964);
#1094=PLANE('',#10965);
#1566=FACE_OUTER_BOUND('',#2161,.T.);
#1567=FACE_OUTER_BOUND('',#2162,.T.);
#1568=FACE_OUTER_BOUND('',#2163,.T.);
#1569=FACE_OUTER_BOUND('',#2164,.T.);
#1570=FACE_OUTER_BOUND('',#2165,.T.);
#1571=FACE_OUTER_BOUND('',#2166,.T.);
#1572=FACE_OUTER_BOUND('',#2167,.T.);
#1573=FACE_OUTER_BOUND('',#2168,.T.);
#1574=FACE_OUTER_BOUND('',#2169,.T.);
#1575=FACE_OUTER_BOUND('',#2170,.T.);
#1576=FACE_OUTER_BOUND('',#2171,.T.);
#1577=FACE_OUTER_BOUND('',#2172,.T.);
#1578=FACE_OUTER_BOUND('',#2173,.T.);
#1579=FACE_OUTER_BOUND('',#2174,.T.);
#1580=FACE_OUTER_BOUND('',#2175,.T.);
#1581=FACE_OUTER_BOUND('',#2176,.T.);
#1582=FACE_OUTER_BOUND('',#2177,.T.);
#1583=FACE_OUTER_BOUND('',#2178,.T.);
#1584=FACE_OUTER_BOUND('',#2179,.T.);
#1585=FACE_OUTER_BOUND('',#2180,.T.);
#1586=FACE_OUTER_BOUND('',#2181,.T.);
#1587=FACE_OUTER_BOUND('',#2182,.T.);
#1588=FACE_OUTER_BOUND('',#2183,.T.);
#1589=FACE_OUTER_BOUND('',#2184,.T.);
#1590=FACE_OUTER_BOUND('',#2185,.T.);
#1591=FACE_OUTER_BOUND('',#2186,.T.);
#1592=FACE_OUTER_BOUND('',#2187,.T.);
#1593=FACE_OUTER_BOUND('',#2188,.T.);
#1594=FACE_OUTER_BOUND('',#2189,.T.);
#1595=FACE_OUTER_BOUND('',#2190,.T.);
#1596=FACE_OUTER_BOUND('',#2191,.T.);
#1597=FACE_OUTER_BOUND('',#2192,.T.);
#1598=FACE_OUTER_BOUND('',#2193,.T.);
#1599=FACE_OUTER_BOUND('',#2194,.T.);
#1600=FACE_OUTER_BOUND('',#2195,.T.);
#1601=FACE_OUTER_BOUND('',#2196,.T.);
#1602=FACE_OUTER_BOUND('',#2198,.T.);
#1603=FACE_OUTER_BOUND('',#2199,.T.);
#1604=FACE_OUTER_BOUND('',#2200,.T.);
#1605=FACE_OUTER_BOUND('',#2201,.T.);
#1606=FACE_OUTER_BOUND('',#2202,.T.);
#1607=FACE_OUTER_BOUND('',#2204,.T.);
#1608=FACE_OUTER_BOUND('',#2206,.T.);
#1609=FACE_OUTER_BOUND('',#2207,.T.);
#1610=FACE_OUTER_BOUND('',#2208,.T.);
#1611=FACE_OUTER_BOUND('',#2209,.T.);
#1612=FACE_OUTER_BOUND('',#2210,.T.);
#1613=FACE_OUTER_BOUND('',#2211,.T.);
#1614=FACE_OUTER_BOUND('',#2212,.T.);
#1615=FACE_OUTER_BOUND('',#2213,.T.);
#1616=FACE_OUTER_BOUND('',#2214,.T.);
#1617=FACE_OUTER_BOUND('',#2215,.T.);
#1618=FACE_OUTER_BOUND('',#2216,.T.);
#1619=FACE_OUTER_BOUND('',#2217,.T.);
#2161=EDGE_LOOP('',(#8770,#8771,#8772,#8773));
#2162=EDGE_LOOP('',(#8774,#8775,#8776,#8777));
#2163=EDGE_LOOP('',(#8778,#8779,#8780,#8781));
#2164=EDGE_LOOP('',(#8782,#8783,#8784,#8785));
#2165=EDGE_LOOP('',(#8786,#8787,#8788,#8789));
#2166=EDGE_LOOP('',(#8790,#8791,#8792,#8793));
#2167=EDGE_LOOP('',(#8794,#8795,#8796,#8797));
#2168=EDGE_LOOP('',(#8798,#8799,#8800,#8801));
#2169=EDGE_LOOP('',(#8802,#8803,#8804,#8805));
#2170=EDGE_LOOP('',(#8806,#8807,#8808,#8809));
#2171=EDGE_LOOP('',(#8810,#8811,#8812,#8813));
#2172=EDGE_LOOP('',(#8814,#8815,#8816,#8817));
#2173=EDGE_LOOP('',(#8818,#8819,#8820,#8821));
#2174=EDGE_LOOP('',(#8822,#8823,#8824,#8825));
#2175=EDGE_LOOP('',(#8826,#8827,#8828,#8829));
#2176=EDGE_LOOP('',(#8830,#8831,#8832,#8833));
#2177=EDGE_LOOP('',(#8834,#8835,#8836,#8837));
#2178=EDGE_LOOP('',(#8838,#8839,#8840,#8841));
#2179=EDGE_LOOP('',(#8842,#8843,#8844,#8845));
#2180=EDGE_LOOP('',(#8846,#8847,#8848,#8849));
#2181=EDGE_LOOP('',(#8850,#8851,#8852,#8853));
#2182=EDGE_LOOP('',(#8854,#8855,#8856,#8857));
#2183=EDGE_LOOP('',(#8858,#8859,#8860,#8861));
#2184=EDGE_LOOP('',(#8862,#8863,#8864,#8865));
#2185=EDGE_LOOP('',(#8866,#8867,#8868,#8869));
#2186=EDGE_LOOP('',(#8870,#8871,#8872,#8873));
#2187=EDGE_LOOP('',(#8874,#8875,#8876,#8877));
#2188=EDGE_LOOP('',(#8878,#8879,#8880,#8881));
#2189=EDGE_LOOP('',(#8882,#8883,#8884,#8885));
#2190=EDGE_LOOP('',(#8886,#8887,#8888,#8889));
#2191=EDGE_LOOP('',(#8890,#8891,#8892,#8893));
#2192=EDGE_LOOP('',(#8894,#8895,#8896,#8897));
#2193=EDGE_LOOP('',(#8898,#8899,#8900,#8901));
#2194=EDGE_LOOP('',(#8902,#8903));
#2195=EDGE_LOOP('',(#8904,#8905,#8906,#8907));
#2196=EDGE_LOOP('',(#8908));
#2197=EDGE_LOOP('',(#8909));
#2198=EDGE_LOOP('',(#8910,#8911,#8912,#8913,#8914,#8915,#8916,#8917));
#2199=EDGE_LOOP('',(#8918));
#2200=EDGE_LOOP('',(#8919,#8920,#8921,#8922,#8923,#8924,#8925,#8926,#8927,
#8928,#8929,#8930,#8931,#8932,#8933,#8934,#8935,#8936,#8937,#8938,#8939,
#8940,#8941,#8942,#8943,#8944,#8945,#8946,#8947,#8948,#8949,#8950,#8951,
#8952,#8953,#8954));
#2201=EDGE_LOOP('',(#8955,#8956,#8957,#8958,#8959,#8960,#8961,#8962,#8963,
#8964,#8965,#8966,#8967,#8968,#8969,#8970,#8971,#8972,#8973,#8974,#8975,
#8976,#8977,#8978,#8979,#8980,#8981,#8982,#8983,#8984,#8985,#8986,#8987,
#8988,#8989));
#2202=EDGE_LOOP('',(#8990));
#2203=EDGE_LOOP('',(#8991,#8992,#8993,#8994,#8995,#8996));
#2204=EDGE_LOOP('',(#8997));
#2205=EDGE_LOOP('',(#8998,#8999,#9000,#9001));
#2206=EDGE_LOOP('',(#9002,#9003));
#2207=EDGE_LOOP('',(#9004,#9005));
#2208=EDGE_LOOP('',(#9006,#9007));
#2209=EDGE_LOOP('',(#9008,#9009));
#2210=EDGE_LOOP('',(#9010,#9011));
#2211=EDGE_LOOP('',(#9012,#9013,#9014,#9015,#9016,#9017));
#2212=EDGE_LOOP('',(#9018,#9019,#9020,#9021));
#2213=EDGE_LOOP('',(#9022,#9023,#9024,#9025));
#2214=EDGE_LOOP('',(#9026,#9027,#9028,#9029));
#2215=EDGE_LOOP('',(#9030,#9031,#9032,#9033));
#2216=EDGE_LOOP('',(#9034,#9035,#9036,#9037));
#2217=EDGE_LOOP('',(#9038,#9039,#9040,#9041));
#2766=LINE('',#45889,#3344);
#2767=LINE('',#45932,#3345);
#2768=LINE('',#46012,#3346);
#2769=LINE('',#46088,#3347);
#2770=LINE('',#46164,#3348);
#2771=LINE('',#46240,#3349);
#2772=LINE('',#46316,#3350);
#2773=LINE('',#46392,#3351);
#2774=LINE('',#46468,#3352);
#2775=LINE('',#46548,#3353);
#2776=LINE('',#46624,#3354);
#2777=LINE('',#46700,#3355);
#2778=LINE('',#46776,#3356);
#2779=LINE('',#46852,#3357);
#2780=LINE('',#46928,#3358);
#2781=LINE('',#47006,#3359);
#2782=LINE('',#47051,#3360);
#2783=LINE('',#47129,#3361);
#2784=LINE('',#47205,#3362);
#2785=LINE('',#47281,#3363);
#2786=LINE('',#47357,#3364);
#2787=LINE('',#47433,#3365);
#2788=LINE('',#47511,#3366);
#2789=LINE('',#47587,#3367);
#2790=LINE('',#47665,#3368);
#2791=LINE('',#47741,#3369);
#2792=LINE('',#47817,#3370);
#2793=LINE('',#47893,#3371);
#2794=LINE('',#47969,#3372);
#2795=LINE('',#48047,#3373);
#2796=LINE('',#48123,#3374);
#2797=LINE('',#48315,#3375);
#2798=LINE('',#48349,#3376);
#2799=LINE('',#49236,#3377);
#2800=LINE('',#49238,#3378);
#2801=LINE('',#49240,#3379);
#2802=LINE('',#49242,#3380);
#2803=LINE('',#49244,#3381);
#2804=LINE('',#49245,#3382);
#2805=LINE('',#49247,#3383);
#2806=LINE('',#49248,#3384);
#2807=LINE('',#49250,#3385);
#2808=LINE('',#49252,#3386);
#2809=LINE('',#49254,#3387);
#2810=LINE('',#49256,#3388);
#3344=VECTOR('',#13148,0.0015);
#3345=VECTOR('',#13153,0.0015);
#3346=VECTOR('',#13156,0.0015);
#3347=VECTOR('',#13159,0.0015);
#3348=VECTOR('',#13162,0.0015);
#3349=VECTOR('',#13165,0.0015);
#3350=VECTOR('',#13168,0.0015);
#3351=VECTOR('',#13171,0.0015);
#3352=VECTOR('',#13174,0.0015);
#3353=VECTOR('',#13177,0.0015);
#3354=VECTOR('',#13180,0.0015);
#3355=VECTOR('',#13183,0.0015);
#3356=VECTOR('',#13186,0.0015);
#3357=VECTOR('',#13189,0.0015);
#3358=VECTOR('',#13192,0.0015);
#3359=VECTOR('',#13195,0.00117524047358083);
#3360=VECTOR('',#13200,0.00117524047358083);
#3361=VECTOR('',#13203,0.00117524047358083);
#3362=VECTOR('',#13206,0.00117524047358083);
#3363=VECTOR('',#13209,0.00117524047358083);
#3364=VECTOR('',#13212,0.00117524047358083);
#3365=VECTOR('',#13215,0.00117524047358083);
#3366=VECTOR('',#13218,0.00117524047358083);
#3367=VECTOR('',#13221,0.00117524047358083);
#3368=VECTOR('',#13224,0.00117524047358083);
#3369=VECTOR('',#13227,0.00117524047358083);
#3370=VECTOR('',#13230,0.00117524047358083);
#3371=VECTOR('',#13233,0.00117524047358083);
#3372=VECTOR('',#13236,0.00117524047358083);
#3373=VECTOR('',#13239,0.00117524047358083);
#3374=VECTOR('',#13242,0.00117524047358083);
#3375=VECTOR('',#13259,0.00285);
#3376=VECTOR('',#13268,0.001125);
#3377=VECTOR('',#13299,0.999999999999998);
#3378=VECTOR('',#13300,1.);
#3379=VECTOR('',#13301,0.999999999999998);
#3380=VECTOR('',#13302,0.999999999999998);
#3381=VECTOR('',#13303,1.);
#3382=VECTOR('',#13304,0.999999999999998);
#3383=VECTOR('',#13307,1.);
#3384=VECTOR('',#13308,1.);
#3385=VECTOR('',#13311,1.);
#3386=VECTOR('',#13314,1.);
#3387=VECTOR('',#13317,1.);
#3388=VECTOR('',#13320,1.);
#3733=CIRCLE('',#10901,0.00150000000001);
#3734=CIRCLE('',#10917,0.00117524047359083);
#3735=CIRCLE('',#10934,0.00117524047359083);
#3736=CIRCLE('',#10936,0.00150000000001);
#3737=CIRCLE('',#10938,0.00115470053838925);
#3738=CIRCLE('',#10940,0.00285000000001);
#3739=CIRCLE('',#10941,0.00285000000001);
#3740=CIRCLE('',#10943,0.00150000000001);
#3741=CIRCLE('',#10945,0.00112500000001);
#3742=CIRCLE('',#10948,0.00115470053838925);
#3743=CIRCLE('',#10949,0.00115470053838925);
#3744=CIRCLE('',#10950,0.00115470053838925);
#3745=CIRCLE('',#10951,0.00115470053838925);
#3746=CIRCLE('',#10952,0.00115470053838925);
#4644=VERTEX_POINT('',#45887);
#4645=VERTEX_POINT('',#45888);
#4646=VERTEX_POINT('',#45890);
#4647=VERTEX_POINT('',#45911);
#4648=VERTEX_POINT('',#45930);
#4649=VERTEX_POINT('',#45931);
#4650=VERTEX_POINT('',#46010);
#4651=VERTEX_POINT('',#46011);
#4652=VERTEX_POINT('',#46086);
#4653=VERTEX_POINT('',#46087);
#4654=VERTEX_POINT('',#46162);
#4655=VERTEX_POINT('',#46163);
#4656=VERTEX_POINT('',#46238);
#4657=VERTEX_POINT('',#46239);
#4658=VERTEX_POINT('',#46314);
#4659=VERTEX_POINT('',#46315);
#4660=VERTEX_POINT('',#46390);
#4661=VERTEX_POINT('',#46391);
#4662=VERTEX_POINT('',#46466);
#4663=VERTEX_POINT('',#46467);
#4664=VERTEX_POINT('',#46546);
#4665=VERTEX_POINT('',#46547);
#4666=VERTEX_POINT('',#46622);
#4667=VERTEX_POINT('',#46623);
#4668=VERTEX_POINT('',#46698);
#4669=VERTEX_POINT('',#46699);
#4670=VERTEX_POINT('',#46774);
#4671=VERTEX_POINT('',#46775);
#4672=VERTEX_POINT('',#46850);
#4673=VERTEX_POINT('',#46851);
#4674=VERTEX_POINT('',#46926);
#4675=VERTEX_POINT('',#46927);
#4676=VERTEX_POINT('',#47004);
#4677=VERTEX_POINT('',#47005);
#4678=VERTEX_POINT('',#47007);
#4679=VERTEX_POINT('',#47028);
#4680=VERTEX_POINT('',#47049);
#4681=VERTEX_POINT('',#47050);
#4682=VERTEX_POINT('',#47127);
#4683=VERTEX_POINT('',#47128);
#4684=VERTEX_POINT('',#47203);
#4685=VERTEX_POINT('',#47204);
#4686=VERTEX_POINT('',#47279);
#4687=VERTEX_POINT('',#47280);
#4688=VERTEX_POINT('',#47355);
#4689=VERTEX_POINT('',#47356);
#4690=VERTEX_POINT('',#47431);
#4691=VERTEX_POINT('',#47432);
#4692=VERTEX_POINT('',#47509);
#4693=VERTEX_POINT('',#47510);
#4694=VERTEX_POINT('',#47585);
#4695=VERTEX_POINT('',#47586);
#4696=VERTEX_POINT('',#47663);
#4697=VERTEX_POINT('',#47664);
#4698=VERTEX_POINT('',#47739);
#4699=VERTEX_POINT('',#47740);
#4700=VERTEX_POINT('',#47815);
#4701=VERTEX_POINT('',#47816);
#4702=VERTEX_POINT('',#47891);
#4703=VERTEX_POINT('',#47892);
#4704=VERTEX_POINT('',#47967);
#4705=VERTEX_POINT('',#47968);
#4706=VERTEX_POINT('',#48045);
#4707=VERTEX_POINT('',#48046);
#4708=VERTEX_POINT('',#48121);
#4709=VERTEX_POINT('',#48122);
#4710=VERTEX_POINT('',#48197);
#4711=VERTEX_POINT('',#48218);
#4712=VERTEX_POINT('',#48239);
#4713=VERTEX_POINT('',#48272);
#4714=VERTEX_POINT('',#48305);
#4715=VERTEX_POINT('',#48306);
#4716=VERTEX_POINT('',#48312);
#4717=VERTEX_POINT('',#48314);
#4718=VERTEX_POINT('',#48318);
#4719=VERTEX_POINT('',#48321);
#4720=VERTEX_POINT('',#48348);
#4721=VERTEX_POINT('',#49203);
#4722=VERTEX_POINT('',#49204);
#4723=VERTEX_POINT('',#49206);
#4724=VERTEX_POINT('',#49209);
#4725=VERTEX_POINT('',#49234);
#4726=VERTEX_POINT('',#49235);
#4727=VERTEX_POINT('',#49237);
#4728=VERTEX_POINT('',#49239);
#4729=VERTEX_POINT('',#49241);
#4730=VERTEX_POINT('',#49243);
#6038=EDGE_CURVE('',#4644,#4645,#2766,.T.);
#6039=EDGE_CURVE('',#4644,#4646,#517,.T.);
#6040=EDGE_CURVE('',#4646,#4647,#3733,.T.);
#6041=EDGE_CURVE('',#4645,#4647,#518,.F.);
#6042=EDGE_CURVE('',#4648,#4649,#2767,.T.);
#6043=EDGE_CURVE('',#4648,#4644,#519,.T.);
#6044=EDGE_CURVE('',#4649,#4645,#520,.F.);
#6045=EDGE_CURVE('',#4650,#4651,#2768,.T.);
#6046=EDGE_CURVE('',#4650,#4648,#521,.T.);
#6047=EDGE_CURVE('',#4651,#4649,#522,.F.);
#6048=EDGE_CURVE('',#4652,#4653,#2769,.T.);
#6049=EDGE_CURVE('',#4652,#4650,#523,.T.);
#6050=EDGE_CURVE('',#4653,#4651,#524,.F.);
#6051=EDGE_CURVE('',#4654,#4655,#2770,.T.);
#6052=EDGE_CURVE('',#4654,#4652,#525,.T.);
#6053=EDGE_CURVE('',#4655,#4653,#526,.F.);
#6054=EDGE_CURVE('',#4656,#4657,#2771,.T.);
#6055=EDGE_CURVE('',#4656,#4654,#527,.T.);
#6056=EDGE_CURVE('',#4657,#4655,#528,.F.);
#6057=EDGE_CURVE('',#4658,#4659,#2772,.T.);
#6058=EDGE_CURVE('',#4658,#4656,#529,.T.);
#6059=EDGE_CURVE('',#4659,#4657,#530,.F.);
#6060=EDGE_CURVE('',#4660,#4661,#2773,.T.);
#6061=EDGE_CURVE('',#4660,#4658,#531,.T.);
#6062=EDGE_CURVE('',#4661,#4659,#532,.F.);
#6063=EDGE_CURVE('',#4662,#4663,#2774,.T.);
#6064=EDGE_CURVE('',#4662,#4660,#533,.T.);
#6065=EDGE_CURVE('',#4663,#4661,#534,.F.);
#6066=EDGE_CURVE('',#4664,#4665,#2775,.T.);
#6067=EDGE_CURVE('',#4664,#4662,#535,.T.);
#6068=EDGE_CURVE('',#4665,#4663,#536,.F.);
#6069=EDGE_CURVE('',#4666,#4667,#2776,.T.);
#6070=EDGE_CURVE('',#4666,#4664,#537,.T.);
#6071=EDGE_CURVE('',#4667,#4665,#538,.F.);
#6072=EDGE_CURVE('',#4668,#4669,#2777,.T.);
#6073=EDGE_CURVE('',#4668,#4666,#539,.T.);
#6074=EDGE_CURVE('',#4669,#4667,#540,.F.);
#6075=EDGE_CURVE('',#4670,#4671,#2778,.T.);
#6076=EDGE_CURVE('',#4670,#4668,#541,.T.);
#6077=EDGE_CURVE('',#4671,#4669,#542,.F.);
#6078=EDGE_CURVE('',#4672,#4673,#2779,.T.);
#6079=EDGE_CURVE('',#4672,#4670,#543,.T.);
#6080=EDGE_CURVE('',#4673,#4671,#544,.F.);
#6081=EDGE_CURVE('',#4674,#4675,#2780,.T.);
#6082=EDGE_CURVE('',#4674,#4672,#545,.T.);
#6083=EDGE_CURVE('',#4675,#4673,#546,.F.);
#6084=EDGE_CURVE('',#4676,#4677,#2781,.T.);
#6085=EDGE_CURVE('',#4678,#4676,#547,.F.);
#6086=EDGE_CURVE('',#4679,#4678,#3734,.T.);
#6087=EDGE_CURVE('',#4679,#4677,#548,.T.);
#6088=EDGE_CURVE('',#4680,#4681,#2782,.T.);
#6089=EDGE_CURVE('',#4676,#4680,#549,.F.);
#6090=EDGE_CURVE('',#4677,#4681,#550,.T.);
#6091=EDGE_CURVE('',#4682,#4683,#2783,.T.);
#6092=EDGE_CURVE('',#4680,#4682,#551,.F.);
#6093=EDGE_CURVE('',#4681,#4683,#552,.T.);
#6094=EDGE_CURVE('',#4684,#4685,#2784,.T.);
#6095=EDGE_CURVE('',#4682,#4684,#553,.F.);
#6096=EDGE_CURVE('',#4683,#4685,#554,.T.);
#6097=EDGE_CURVE('',#4686,#4687,#2785,.T.);
#6098=EDGE_CURVE('',#4684,#4686,#555,.F.);
#6099=EDGE_CURVE('',#4685,#4687,#556,.T.);
#6100=EDGE_CURVE('',#4688,#4689,#2786,.T.);
#6101=EDGE_CURVE('',#4686,#4688,#557,.F.);
#6102=EDGE_CURVE('',#4687,#4689,#558,.T.);
#6103=EDGE_CURVE('',#4690,#4691,#2787,.T.);
#6104=EDGE_CURVE('',#4688,#4690,#559,.F.);
#6105=EDGE_CURVE('',#4689,#4691,#560,.T.);
#6106=EDGE_CURVE('',#4692,#4693,#2788,.T.);
#6107=EDGE_CURVE('',#4690,#4692,#561,.F.);
#6108=EDGE_CURVE('',#4691,#4693,#562,.T.);
#6109=EDGE_CURVE('',#4694,#4695,#2789,.T.);
#6110=EDGE_CURVE('',#4692,#4694,#563,.F.);
#6111=EDGE_CURVE('',#4693,#4695,#564,.T.);
#6112=EDGE_CURVE('',#4696,#4697,#2790,.T.);
#6113=EDGE_CURVE('',#4694,#4696,#565,.F.);
#6114=EDGE_CURVE('',#4695,#4697,#566,.T.);
#6115=EDGE_CURVE('',#4698,#4699,#2791,.T.);
#6116=EDGE_CURVE('',#4696,#4698,#567,.F.);
#6117=EDGE_CURVE('',#4697,#4699,#568,.T.);
#6118=EDGE_CURVE('',#4700,#4701,#2792,.T.);
#6119=EDGE_CURVE('',#4698,#4700,#569,.F.);
#6120=EDGE_CURVE('',#4699,#4701,#570,.T.);
#6121=EDGE_CURVE('',#4702,#4703,#2793,.T.);
#6122=EDGE_CURVE('',#4700,#4702,#571,.F.);
#6123=EDGE_CURVE('',#4701,#4703,#572,.T.);
#6124=EDGE_CURVE('',#4704,#4705,#2794,.T.);
#6125=EDGE_CURVE('',#4702,#4704,#573,.F.);
#6126=EDGE_CURVE('',#4703,#4705,#574,.T.);
#6127=EDGE_CURVE('',#4706,#4707,#2795,.T.);
#6128=EDGE_CURVE('',#4704,#4706,#575,.F.);
#6129=EDGE_CURVE('',#4705,#4707,#576,.T.);
#6130=EDGE_CURVE('',#4708,#4709,#2796,.T.);
#6131=EDGE_CURVE('',#4706,#4708,#577,.F.);
#6132=EDGE_CURVE('',#4707,#4709,#578,.T.);
#6133=EDGE_CURVE('',#4709,#4710,#579,.T.);
#6134=EDGE_CURVE('',#4710,#4711,#3735,.T.);
#6135=EDGE_CURVE('',#4708,#4711,#580,.F.);
#6136=EDGE_CURVE('',#4712,#4675,#581,.F.);
#6137=EDGE_CURVE('',#4712,#4713,#3736,.T.);
#6138=EDGE_CURVE('',#4713,#4674,#582,.T.);
#6139=EDGE_CURVE('',#4714,#4715,#681,.T.);
#6140=EDGE_CURVE('',#4714,#4715,#3737,.T.);
#6141=EDGE_CURVE('',#4716,#4716,#3738,.T.);
#6142=EDGE_CURVE('',#4716,#4717,#2797,.T.);
#6143=EDGE_CURVE('',#4717,#4717,#3739,.T.);
#6144=EDGE_CURVE('',#4718,#4718,#3740,.T.);
#6145=EDGE_CURVE('',#4712,#4719,#583,.F.);
#6146=EDGE_CURVE('',#4719,#4720,#2798,.T.);
#6147=EDGE_CURVE('',#4720,#4720,#3741,.T.);
#6148=EDGE_CURVE('',#4719,#4679,#584,.F.);
#6149=EDGE_CURVE('',#4678,#4713,#585,.T.);
#6150=EDGE_CURVE('',#4647,#4710,#586,.F.);
#6151=EDGE_CURVE('',#4711,#4646,#587,.F.);
#6152=EDGE_CURVE('',#4721,#4722,#3742,.T.);
#6153=EDGE_CURVE('',#4723,#4721,#3743,.T.);
#6154=EDGE_CURVE('',#4715,#4723,#3744,.T.);
#6155=EDGE_CURVE('',#4724,#4714,#3745,.T.);
#6156=EDGE_CURVE('',#4722,#4724,#3746,.T.);
#6157=EDGE_CURVE('',#4715,#4723,#682,.T.);
#6158=EDGE_CURVE('',#4723,#4721,#683,.T.);
#6159=EDGE_CURVE('',#4721,#4722,#684,.T.);
#6160=EDGE_CURVE('',#4722,#4724,#685,.T.);
#6161=EDGE_CURVE('',#4724,#4714,#686,.T.);
#6162=EDGE_CURVE('',#4725,#4726,#2799,.T.);
#6163=EDGE_CURVE('',#4726,#4727,#2800,.T.);
#6164=EDGE_CURVE('',#4727,#4728,#2801,.T.);
#6165=EDGE_CURVE('',#4728,#4729,#2802,.T.);
#6166=EDGE_CURVE('',#4729,#4730,#2803,.T.);
#6167=EDGE_CURVE('',#4730,#4725,#2804,.T.);
#6168=EDGE_CURVE('',#4726,#4714,#2805,.T.);
#6169=EDGE_CURVE('',#4727,#4715,#2806,.T.);
#6170=EDGE_CURVE('',#4728,#4723,#2807,.T.);
#6171=EDGE_CURVE('',#4729,#4721,#2808,.T.);
#6172=EDGE_CURVE('',#4730,#4722,#2809,.T.);
#6173=EDGE_CURVE('',#4725,#4724,#2810,.T.);
#8770=ORIENTED_EDGE('',*,*,#6038,.F.);
#8771=ORIENTED_EDGE('',*,*,#6039,.T.);
#8772=ORIENTED_EDGE('',*,*,#6040,.T.);
#8773=ORIENTED_EDGE('',*,*,#6041,.F.);
#8774=ORIENTED_EDGE('',*,*,#6042,.F.);
#8775=ORIENTED_EDGE('',*,*,#6043,.T.);
#8776=ORIENTED_EDGE('',*,*,#6038,.T.);
#8777=ORIENTED_EDGE('',*,*,#6044,.F.);
#8778=ORIENTED_EDGE('',*,*,#6045,.F.);
#8779=ORIENTED_EDGE('',*,*,#6046,.T.);
#8780=ORIENTED_EDGE('',*,*,#6042,.T.);
#8781=ORIENTED_EDGE('',*,*,#6047,.F.);
#8782=ORIENTED_EDGE('',*,*,#6048,.F.);
#8783=ORIENTED_EDGE('',*,*,#6049,.T.);
#8784=ORIENTED_EDGE('',*,*,#6045,.T.);
#8785=ORIENTED_EDGE('',*,*,#6050,.F.);
#8786=ORIENTED_EDGE('',*,*,#6051,.F.);
#8787=ORIENTED_EDGE('',*,*,#6052,.T.);
#8788=ORIENTED_EDGE('',*,*,#6048,.T.);
#8789=ORIENTED_EDGE('',*,*,#6053,.F.);
#8790=ORIENTED_EDGE('',*,*,#6054,.F.);
#8791=ORIENTED_EDGE('',*,*,#6055,.T.);
#8792=ORIENTED_EDGE('',*,*,#6051,.T.);
#8793=ORIENTED_EDGE('',*,*,#6056,.F.);
#8794=ORIENTED_EDGE('',*,*,#6057,.F.);
#8795=ORIENTED_EDGE('',*,*,#6058,.T.);
#8796=ORIENTED_EDGE('',*,*,#6054,.T.);
#8797=ORIENTED_EDGE('',*,*,#6059,.F.);
#8798=ORIENTED_EDGE('',*,*,#6060,.F.);
#8799=ORIENTED_EDGE('',*,*,#6061,.T.);
#8800=ORIENTED_EDGE('',*,*,#6057,.T.);
#8801=ORIENTED_EDGE('',*,*,#6062,.F.);
#8802=ORIENTED_EDGE('',*,*,#6063,.F.);
#8803=ORIENTED_EDGE('',*,*,#6064,.T.);
#8804=ORIENTED_EDGE('',*,*,#6060,.T.);
#8805=ORIENTED_EDGE('',*,*,#6065,.F.);
#8806=ORIENTED_EDGE('',*,*,#6066,.F.);
#8807=ORIENTED_EDGE('',*,*,#6067,.T.);
#8808=ORIENTED_EDGE('',*,*,#6063,.T.);
#8809=ORIENTED_EDGE('',*,*,#6068,.F.);
#8810=ORIENTED_EDGE('',*,*,#6069,.F.);
#8811=ORIENTED_EDGE('',*,*,#6070,.T.);
#8812=ORIENTED_EDGE('',*,*,#6066,.T.);
#8813=ORIENTED_EDGE('',*,*,#6071,.F.);
#8814=ORIENTED_EDGE('',*,*,#6072,.F.);
#8815=ORIENTED_EDGE('',*,*,#6073,.T.);
#8816=ORIENTED_EDGE('',*,*,#6069,.T.);
#8817=ORIENTED_EDGE('',*,*,#6074,.F.);
#8818=ORIENTED_EDGE('',*,*,#6075,.F.);
#8819=ORIENTED_EDGE('',*,*,#6076,.T.);
#8820=ORIENTED_EDGE('',*,*,#6072,.T.);
#8821=ORIENTED_EDGE('',*,*,#6077,.F.);
#8822=ORIENTED_EDGE('',*,*,#6078,.F.);
#8823=ORIENTED_EDGE('',*,*,#6079,.T.);
#8824=ORIENTED_EDGE('',*,*,#6075,.T.);
#8825=ORIENTED_EDGE('',*,*,#6080,.F.);
#8826=ORIENTED_EDGE('',*,*,#6081,.F.);
#8827=ORIENTED_EDGE('',*,*,#6082,.T.);
#8828=ORIENTED_EDGE('',*,*,#6078,.T.);
#8829=ORIENTED_EDGE('',*,*,#6083,.F.);
#8830=ORIENTED_EDGE('',*,*,#6084,.F.);
#8831=ORIENTED_EDGE('',*,*,#6085,.F.);
#8832=ORIENTED_EDGE('',*,*,#6086,.F.);
#8833=ORIENTED_EDGE('',*,*,#6087,.T.);
#8834=ORIENTED_EDGE('',*,*,#6088,.F.);
#8835=ORIENTED_EDGE('',*,*,#6089,.F.);
#8836=ORIENTED_EDGE('',*,*,#6084,.T.);
#8837=ORIENTED_EDGE('',*,*,#6090,.T.);
#8838=ORIENTED_EDGE('',*,*,#6091,.F.);
#8839=ORIENTED_EDGE('',*,*,#6092,.F.);
#8840=ORIENTED_EDGE('',*,*,#6088,.T.);
#8841=ORIENTED_EDGE('',*,*,#6093,.T.);
#8842=ORIENTED_EDGE('',*,*,#6094,.F.);
#8843=ORIENTED_EDGE('',*,*,#6095,.F.);
#8844=ORIENTED_EDGE('',*,*,#6091,.T.);
#8845=ORIENTED_EDGE('',*,*,#6096,.T.);
#8846=ORIENTED_EDGE('',*,*,#6097,.F.);
#8847=ORIENTED_EDGE('',*,*,#6098,.F.);
#8848=ORIENTED_EDGE('',*,*,#6094,.T.);
#8849=ORIENTED_EDGE('',*,*,#6099,.T.);
#8850=ORIENTED_EDGE('',*,*,#6100,.F.);
#8851=ORIENTED_EDGE('',*,*,#6101,.F.);
#8852=ORIENTED_EDGE('',*,*,#6097,.T.);
#8853=ORIENTED_EDGE('',*,*,#6102,.T.);
#8854=ORIENTED_EDGE('',*,*,#6103,.F.);
#8855=ORIENTED_EDGE('',*,*,#6104,.F.);
#8856=ORIENTED_EDGE('',*,*,#6100,.T.);
#8857=ORIENTED_EDGE('',*,*,#6105,.T.);
#8858=ORIENTED_EDGE('',*,*,#6106,.F.);
#8859=ORIENTED_EDGE('',*,*,#6107,.F.);
#8860=ORIENTED_EDGE('',*,*,#6103,.T.);
#8861=ORIENTED_EDGE('',*,*,#6108,.T.);
#8862=ORIENTED_EDGE('',*,*,#6109,.F.);
#8863=ORIENTED_EDGE('',*,*,#6110,.F.);
#8864=ORIENTED_EDGE('',*,*,#6106,.T.);
#8865=ORIENTED_EDGE('',*,*,#6111,.T.);
#8866=ORIENTED_EDGE('',*,*,#6112,.F.);
#8867=ORIENTED_EDGE('',*,*,#6113,.F.);
#8868=ORIENTED_EDGE('',*,*,#6109,.T.);
#8869=ORIENTED_EDGE('',*,*,#6114,.T.);
#8870=ORIENTED_EDGE('',*,*,#6115,.F.);
#8871=ORIENTED_EDGE('',*,*,#6116,.F.);
#8872=ORIENTED_EDGE('',*,*,#6112,.T.);
#8873=ORIENTED_EDGE('',*,*,#6117,.T.);
#8874=ORIENTED_EDGE('',*,*,#6118,.F.);
#8875=ORIENTED_EDGE('',*,*,#6119,.F.);
#8876=ORIENTED_EDGE('',*,*,#6115,.T.);
#8877=ORIENTED_EDGE('',*,*,#6120,.T.);
#8878=ORIENTED_EDGE('',*,*,#6121,.F.);
#8879=ORIENTED_EDGE('',*,*,#6122,.F.);
#8880=ORIENTED_EDGE('',*,*,#6118,.T.);
#8881=ORIENTED_EDGE('',*,*,#6123,.T.);
#8882=ORIENTED_EDGE('',*,*,#6124,.F.);
#8883=ORIENTED_EDGE('',*,*,#6125,.F.);
#8884=ORIENTED_EDGE('',*,*,#6121,.T.);
#8885=ORIENTED_EDGE('',*,*,#6126,.T.);
#8886=ORIENTED_EDGE('',*,*,#6127,.F.);
#8887=ORIENTED_EDGE('',*,*,#6128,.F.);
#8888=ORIENTED_EDGE('',*,*,#6124,.T.);
#8889=ORIENTED_EDGE('',*,*,#6129,.T.);
#8890=ORIENTED_EDGE('',*,*,#6130,.F.);
#8891=ORIENTED_EDGE('',*,*,#6131,.F.);
#8892=ORIENTED_EDGE('',*,*,#6127,.T.);
#8893=ORIENTED_EDGE('',*,*,#6132,.T.);
#8894=ORIENTED_EDGE('',*,*,#6130,.T.);
#8895=ORIENTED_EDGE('',*,*,#6133,.T.);
#8896=ORIENTED_EDGE('',*,*,#6134,.T.);
#8897=ORIENTED_EDGE('',*,*,#6135,.F.);
#8898=ORIENTED_EDGE('',*,*,#6081,.T.);
#8899=ORIENTED_EDGE('',*,*,#6136,.F.);
#8900=ORIENTED_EDGE('',*,*,#6137,.T.);
#8901=ORIENTED_EDGE('',*,*,#6138,.T.);
#8902=ORIENTED_EDGE('',*,*,#6139,.F.);
#8903=ORIENTED_EDGE('',*,*,#6140,.T.);
#8904=ORIENTED_EDGE('',*,*,#6141,.F.);
#8905=ORIENTED_EDGE('',*,*,#6142,.T.);
#8906=ORIENTED_EDGE('',*,*,#6143,.T.);
#8907=ORIENTED_EDGE('',*,*,#6142,.F.);
#8908=ORIENTED_EDGE('',*,*,#6141,.T.);
#8909=ORIENTED_EDGE('',*,*,#6144,.F.);
#8910=ORIENTED_EDGE('',*,*,#6145,.T.);
#8911=ORIENTED_EDGE('',*,*,#6146,.T.);
#8912=ORIENTED_EDGE('',*,*,#6147,.F.);
#8913=ORIENTED_EDGE('',*,*,#6146,.F.);
#8914=ORIENTED_EDGE('',*,*,#6148,.T.);
#8915=ORIENTED_EDGE('',*,*,#6086,.T.);
#8916=ORIENTED_EDGE('',*,*,#6149,.T.);
#8917=ORIENTED_EDGE('',*,*,#6137,.F.);
#8918=ORIENTED_EDGE('',*,*,#6147,.T.);
#8919=ORIENTED_EDGE('',*,*,#6136,.T.);
#8920=ORIENTED_EDGE('',*,*,#6083,.T.);
#8921=ORIENTED_EDGE('',*,*,#6080,.T.);
#8922=ORIENTED_EDGE('',*,*,#6077,.T.);
#8923=ORIENTED_EDGE('',*,*,#6074,.T.);
#8924=ORIENTED_EDGE('',*,*,#6071,.T.);
#8925=ORIENTED_EDGE('',*,*,#6068,.T.);
#8926=ORIENTED_EDGE('',*,*,#6065,.T.);
#8927=ORIENTED_EDGE('',*,*,#6062,.T.);
#8928=ORIENTED_EDGE('',*,*,#6059,.T.);
#8929=ORIENTED_EDGE('',*,*,#6056,.T.);
#8930=ORIENTED_EDGE('',*,*,#6053,.T.);
#8931=ORIENTED_EDGE('',*,*,#6050,.T.);
#8932=ORIENTED_EDGE('',*,*,#6047,.T.);
#8933=ORIENTED_EDGE('',*,*,#6044,.T.);
#8934=ORIENTED_EDGE('',*,*,#6041,.T.);
#8935=ORIENTED_EDGE('',*,*,#6150,.T.);
#8936=ORIENTED_EDGE('',*,*,#6133,.F.);
#8937=ORIENTED_EDGE('',*,*,#6132,.F.);
#8938=ORIENTED_EDGE('',*,*,#6129,.F.);
#8939=ORIENTED_EDGE('',*,*,#6126,.F.);
#8940=ORIENTED_EDGE('',*,*,#6123,.F.);
#8941=ORIENTED_EDGE('',*,*,#6120,.F.);
#8942=ORIENTED_EDGE('',*,*,#6117,.F.);
#8943=ORIENTED_EDGE('',*,*,#6114,.F.);
#8944=ORIENTED_EDGE('',*,*,#6111,.F.);
#8945=ORIENTED_EDGE('',*,*,#6108,.F.);
#8946=ORIENTED_EDGE('',*,*,#6105,.F.);
#8947=ORIENTED_EDGE('',*,*,#6102,.F.);
#8948=ORIENTED_EDGE('',*,*,#6099,.F.);
#8949=ORIENTED_EDGE('',*,*,#6096,.F.);
#8950=ORIENTED_EDGE('',*,*,#6093,.F.);
#8951=ORIENTED_EDGE('',*,*,#6090,.F.);
#8952=ORIENTED_EDGE('',*,*,#6087,.F.);
#8953=ORIENTED_EDGE('',*,*,#6148,.F.);
#8954=ORIENTED_EDGE('',*,*,#6145,.F.);
#8955=ORIENTED_EDGE('',*,*,#6085,.T.);
#8956=ORIENTED_EDGE('',*,*,#6089,.T.);
#8957=ORIENTED_EDGE('',*,*,#6092,.T.);
#8958=ORIENTED_EDGE('',*,*,#6095,.T.);
#8959=ORIENTED_EDGE('',*,*,#6098,.T.);
#8960=ORIENTED_EDGE('',*,*,#6101,.T.);
#8961=ORIENTED_EDGE('',*,*,#6104,.T.);
#8962=ORIENTED_EDGE('',*,*,#6107,.T.);
#8963=ORIENTED_EDGE('',*,*,#6110,.T.);
#8964=ORIENTED_EDGE('',*,*,#6113,.T.);
#8965=ORIENTED_EDGE('',*,*,#6116,.T.);
#8966=ORIENTED_EDGE('',*,*,#6119,.T.);
#8967=ORIENTED_EDGE('',*,*,#6122,.T.);
#8968=ORIENTED_EDGE('',*,*,#6125,.T.);
#8969=ORIENTED_EDGE('',*,*,#6128,.T.);
#8970=ORIENTED_EDGE('',*,*,#6131,.T.);
#8971=ORIENTED_EDGE('',*,*,#6135,.T.);
#8972=ORIENTED_EDGE('',*,*,#6151,.T.);
#8973=ORIENTED_EDGE('',*,*,#6039,.F.);
#8974=ORIENTED_EDGE('',*,*,#6043,.F.);
#8975=ORIENTED_EDGE('',*,*,#6046,.F.);
#8976=ORIENTED_EDGE('',*,*,#6049,.F.);
#8977=ORIENTED_EDGE('',*,*,#6052,.F.);
#8978=ORIENTED_EDGE('',*,*,#6055,.F.);
#8979=ORIENTED_EDGE('',*,*,#6058,.F.);
#8980=ORIENTED_EDGE('',*,*,#6061,.F.);
#8981=ORIENTED_EDGE('',*,*,#6064,.F.);
#8982=ORIENTED_EDGE('',*,*,#6067,.F.);
#8983=ORIENTED_EDGE('',*,*,#6070,.F.);
#8984=ORIENTED_EDGE('',*,*,#6073,.F.);
#8985=ORIENTED_EDGE('',*,*,#6076,.F.);
#8986=ORIENTED_EDGE('',*,*,#6079,.F.);
#8987=ORIENTED_EDGE('',*,*,#6082,.F.);
#8988=ORIENTED_EDGE('',*,*,#6138,.F.);
#8989=ORIENTED_EDGE('',*,*,#6149,.F.);
#8990=ORIENTED_EDGE('',*,*,#6144,.T.);
#8991=ORIENTED_EDGE('',*,*,#6152,.F.);
#8992=ORIENTED_EDGE('',*,*,#6153,.F.);
#8993=ORIENTED_EDGE('',*,*,#6154,.F.);
#8994=ORIENTED_EDGE('',*,*,#6140,.F.);
#8995=ORIENTED_EDGE('',*,*,#6155,.F.);
#8996=ORIENTED_EDGE('',*,*,#6156,.F.);
#8997=ORIENTED_EDGE('',*,*,#6143,.F.);
#8998=ORIENTED_EDGE('',*,*,#6040,.F.);
#8999=ORIENTED_EDGE('',*,*,#6151,.F.);
#9000=ORIENTED_EDGE('',*,*,#6134,.F.);
#9001=ORIENTED_EDGE('',*,*,#6150,.F.);
#9002=ORIENTED_EDGE('',*,*,#6154,.T.);
#9003=ORIENTED_EDGE('',*,*,#6157,.F.);
#9004=ORIENTED_EDGE('',*,*,#6153,.T.);
#9005=ORIENTED_EDGE('',*,*,#6158,.F.);
#9006=ORIENTED_EDGE('',*,*,#6152,.T.);
#9007=ORIENTED_EDGE('',*,*,#6159,.F.);
#9008=ORIENTED_EDGE('',*,*,#6156,.T.);
#9009=ORIENTED_EDGE('',*,*,#6160,.F.);
#9010=ORIENTED_EDGE('',*,*,#6155,.T.);
#9011=ORIENTED_EDGE('',*,*,#6161,.F.);
#9012=ORIENTED_EDGE('',*,*,#6162,.T.);
#9013=ORIENTED_EDGE('',*,*,#6163,.T.);
#9014=ORIENTED_EDGE('',*,*,#6164,.T.);
#9015=ORIENTED_EDGE('',*,*,#6165,.T.);
#9016=ORIENTED_EDGE('',*,*,#6166,.T.);
#9017=ORIENTED_EDGE('',*,*,#6167,.T.);
#9018=ORIENTED_EDGE('',*,*,#6168,.T.);
#9019=ORIENTED_EDGE('',*,*,#6139,.T.);
#9020=ORIENTED_EDGE('',*,*,#6169,.F.);
#9021=ORIENTED_EDGE('',*,*,#6163,.F.);
#9022=ORIENTED_EDGE('',*,*,#6169,.T.);
#9023=ORIENTED_EDGE('',*,*,#6157,.T.);
#9024=ORIENTED_EDGE('',*,*,#6170,.F.);
#9025=ORIENTED_EDGE('',*,*,#6164,.F.);
#9026=ORIENTED_EDGE('',*,*,#6170,.T.);
#9027=ORIENTED_EDGE('',*,*,#6158,.T.);
#9028=ORIENTED_EDGE('',*,*,#6171,.F.);
#9029=ORIENTED_EDGE('',*,*,#6165,.F.);
#9030=ORIENTED_EDGE('',*,*,#6171,.T.);
#9031=ORIENTED_EDGE('',*,*,#6159,.T.);
#9032=ORIENTED_EDGE('',*,*,#6172,.F.);
#9033=ORIENTED_EDGE('',*,*,#6166,.F.);
#9034=ORIENTED_EDGE('',*,*,#6172,.T.);
#9035=ORIENTED_EDGE('',*,*,#6160,.T.);
#9036=ORIENTED_EDGE('',*,*,#6173,.F.);
#9037=ORIENTED_EDGE('',*,*,#6167,.F.);
#9038=ORIENTED_EDGE('',*,*,#6173,.T.);
#9039=ORIENTED_EDGE('',*,*,#6161,.T.);
#9040=ORIENTED_EDGE('',*,*,#6168,.F.);
#9041=ORIENTED_EDGE('',*,*,#6162,.F.);
#9281=CYLINDRICAL_SURFACE('',#10900,0.0015);
#9282=CYLINDRICAL_SURFACE('',#10902,0.0015);
#9283=CYLINDRICAL_SURFACE('',#10903,0.0015);
#9284=CYLINDRICAL_SURFACE('',#10904,0.0015);
#9285=CYLINDRICAL_SURFACE('',#10905,0.0015);
#9286=CYLINDRICAL_SURFACE('',#10906,0.0015);
#9287=CYLINDRICAL_SURFACE('',#10907,0.0015);
#9288=CYLINDRICAL_SURFACE('',#10908,0.0015);
#9289=CYLINDRICAL_SURFACE('',#10909,0.0015);
#9290=CYLINDRICAL_SURFACE('',#10910,0.0015);
#9291=CYLINDRICAL_SURFACE('',#10911,0.0015);
#9292=CYLINDRICAL_SURFACE('',#10912,0.0015);
#9293=CYLINDRICAL_SURFACE('',#10913,0.0015);
#9294=CYLINDRICAL_SURFACE('',#10914,0.0015);
#9295=CYLINDRICAL_SURFACE('',#10915,0.0015);
#9296=CYLINDRICAL_SURFACE('',#10916,0.00117524047358083);
#9297=CYLINDRICAL_SURFACE('',#10918,0.00117524047358083);
#9298=CYLINDRICAL_SURFACE('',#10919,0.00117524047358083);
#9299=CYLINDRICAL_SURFACE('',#10920,0.00117524047358083);
#9300=CYLINDRICAL_SURFACE('',#10921,0.00117524047358083);
#9301=CYLINDRICAL_SURFACE('',#10922,0.00117524047358083);
#9302=CYLINDRICAL_SURFACE('',#10923,0.00117524047358083);
#9303=CYLINDRICAL_SURFACE('',#10924,0.00117524047358083);
#9304=CYLINDRICAL_SURFACE('',#10925,0.00117524047358083);
#9305=CYLINDRICAL_SURFACE('',#10926,0.00117524047358083);
#9306=CYLINDRICAL_SURFACE('',#10927,0.00117524047358083);
#9307=CYLINDRICAL_SURFACE('',#10928,0.00117524047358083);
#9308=CYLINDRICAL_SURFACE('',#10929,0.00117524047358083);
#9309=CYLINDRICAL_SURFACE('',#10930,0.00117524047358083);
#9310=CYLINDRICAL_SURFACE('',#10931,0.00117524047358083);
#9311=CYLINDRICAL_SURFACE('',#10932,0.00117524047358083);
#9312=CYLINDRICAL_SURFACE('',#10933,0.00117524047358083);
#9313=CYLINDRICAL_SURFACE('',#10935,0.0015);
#9314=CYLINDRICAL_SURFACE('',#10939,0.00285);
#9788=ADVANCED_FACE('',(#1566),#9281,.T.);
#9789=ADVANCED_FACE('',(#1567),#9282,.T.);
#9790=ADVANCED_FACE('',(#1568),#9283,.T.);
#9791=ADVANCED_FACE('',(#1569),#9284,.T.);
#9792=ADVANCED_FACE('',(#1570),#9285,.T.);
#9793=ADVANCED_FACE('',(#1571),#9286,.T.);
#9794=ADVANCED_FACE('',(#1572),#9287,.T.);
#9795=ADVANCED_FACE('',(#1573),#9288,.T.);
#9796=ADVANCED_FACE('',(#1574),#9289,.T.);
#9797=ADVANCED_FACE('',(#1575),#9290,.T.);
#9798=ADVANCED_FACE('',(#1576),#9291,.T.);
#9799=ADVANCED_FACE('',(#1577),#9292,.T.);
#9800=ADVANCED_FACE('',(#1578),#9293,.T.);
#9801=ADVANCED_FACE('',(#1579),#9294,.T.);
#9802=ADVANCED_FACE('',(#1580),#9295,.T.);
#9803=ADVANCED_FACE('',(#1581),#9296,.T.);
#9804=ADVANCED_FACE('',(#1582),#9297,.T.);
#9805=ADVANCED_FACE('',(#1583),#9298,.T.);
#9806=ADVANCED_FACE('',(#1584),#9299,.T.);
#9807=ADVANCED_FACE('',(#1585),#9300,.T.);
#9808=ADVANCED_FACE('',(#1586),#9301,.T.);
#9809=ADVANCED_FACE('',(#1587),#9302,.T.);
#9810=ADVANCED_FACE('',(#1588),#9303,.T.);
#9811=ADVANCED_FACE('',(#1589),#9304,.T.);
#9812=ADVANCED_FACE('',(#1590),#9305,.T.);
#9813=ADVANCED_FACE('',(#1591),#9306,.T.);
#9814=ADVANCED_FACE('',(#1592),#9307,.T.);
#9815=ADVANCED_FACE('',(#1593),#9308,.T.);
#9816=ADVANCED_FACE('',(#1594),#9309,.T.);
#9817=ADVANCED_FACE('',(#1595),#9310,.T.);
#9818=ADVANCED_FACE('',(#1596),#9311,.T.);
#9819=ADVANCED_FACE('',(#1597),#9312,.T.);
#9820=ADVANCED_FACE('',(#1598),#9313,.T.);
#9821=ADVANCED_FACE('',(#1599),#655,.F.);
#9822=ADVANCED_FACE('',(#1600),#9314,.T.);
#9823=ADVANCED_FACE('',(#1601,#764),#93,.T.);
#9824=ADVANCED_FACE('',(#1602),#656,.T.);
#9825=ADVANCED_FACE('',(#1603),#1085,.T.);
#9826=ADVANCED_FACE('',(#1604),#91,.T.);
#9827=ADVANCED_FACE('',(#1605),#92,.T.);
#9828=ADVANCED_FACE('',(#1606,#765),#1086,.F.);
#9829=ADVANCED_FACE('',(#1607,#766),#1087,.F.);
#9830=ADVANCED_FACE('',(#1608),#657,.F.);
#9831=ADVANCED_FACE('',(#1609),#658,.F.);
#9832=ADVANCED_FACE('',(#1610),#659,.F.);
#9833=ADVANCED_FACE('',(#1611),#660,.F.);
#9834=ADVANCED_FACE('',(#1612),#661,.F.);
#9835=ADVANCED_FACE('',(#1613),#1088,.T.);
#9836=ADVANCED_FACE('',(#1614),#1089,.F.);
#9837=ADVANCED_FACE('',(#1615),#1090,.F.);
#9838=ADVANCED_FACE('',(#1616),#1091,.F.);
#9839=ADVANCED_FACE('',(#1617),#1092,.F.);
#9840=ADVANCED_FACE('',(#1618),#1093,.F.);
#9841=ADVANCED_FACE('',(#1619),#1094,.F.);
#9881=CLOSED_SHELL('',(#9788,#9789,#9790,#9791,#9792,#9793,#9794,#9795,
#9796,#9797,#9798,#9799,#9800,#9801,#9802,#9803,#9804,#9805,#9806,#9807,
#9808,#9809,#9810,#9811,#9812,#9813,#9814,#9815,#9816,#9817,#9818,#9819,
#9820,#9821,#9822,#9823,#9824,#9825,#9826,#9827,#9828,#9829,#9830,#9831,
#9832,#9833,#9834,#9835,#9836,#9837,#9838,#9839,#9840,#9841));
#10899=AXIS2_PLACEMENT_3D('',#45885,#13144,#13145);
#10900=AXIS2_PLACEMENT_3D('',#45886,#13146,#13147);
#10901=AXIS2_PLACEMENT_3D('',#45912,#13149,#13150);
#10902=AXIS2_PLACEMENT_3D('',#45929,#13151,#13152);
#10903=AXIS2_PLACEMENT_3D('',#46009,#13154,#13155);
#10904=AXIS2_PLACEMENT_3D('',#46085,#13157,#13158);
#10905=AXIS2_PLACEMENT_3D('',#46161,#13160,#13161);
#10906=AXIS2_PLACEMENT_3D('',#46237,#13163,#13164);
#10907=AXIS2_PLACEMENT_3D('',#46313,#13166,#13167);
#10908=AXIS2_PLACEMENT_3D('',#46389,#13169,#13170);
#10909=AXIS2_PLACEMENT_3D('',#46465,#13172,#13173);
#10910=AXIS2_PLACEMENT_3D('',#46545,#13175,#13176);
#10911=AXIS2_PLACEMENT_3D('',#46621,#13178,#13179);
#10912=AXIS2_PLACEMENT_3D('',#46697,#13181,#13182);
#10913=AXIS2_PLACEMENT_3D('',#46773,#13184,#13185);
#10914=AXIS2_PLACEMENT_3D('',#46849,#13187,#13188);
#10915=AXIS2_PLACEMENT_3D('',#46925,#13190,#13191);
#10916=AXIS2_PLACEMENT_3D('',#47003,#13193,#13194);
#10917=AXIS2_PLACEMENT_3D('',#47029,#13196,#13197);
#10918=AXIS2_PLACEMENT_3D('',#47048,#13198,#13199);
#10919=AXIS2_PLACEMENT_3D('',#47126,#13201,#13202);
#10920=AXIS2_PLACEMENT_3D('',#47202,#13204,#13205);
#10921=AXIS2_PLACEMENT_3D('',#47278,#13207,#13208);
#10922=AXIS2_PLACEMENT_3D('',#47354,#13210,#13211);
#10923=AXIS2_PLACEMENT_3D('',#47430,#13213,#13214);
#10924=AXIS2_PLACEMENT_3D('',#47508,#13216,#13217);
#10925=AXIS2_PLACEMENT_3D('',#47584,#13219,#13220);
#10926=AXIS2_PLACEMENT_3D('',#47662,#13222,#13223);
#10927=AXIS2_PLACEMENT_3D('',#47738,#13225,#13226);
#10928=AXIS2_PLACEMENT_3D('',#47814,#13228,#13229);
#10929=AXIS2_PLACEMENT_3D('',#47890,#13231,#13232);
#10930=AXIS2_PLACEMENT_3D('',#47966,#13234,#13235);
#10931=AXIS2_PLACEMENT_3D('',#48044,#13237,#13238);
#10932=AXIS2_PLACEMENT_3D('',#48120,#13240,#13241);
#10933=AXIS2_PLACEMENT_3D('',#48196,#13243,#13244);
#10934=AXIS2_PLACEMENT_3D('',#48219,#13245,#13246);
#10935=AXIS2_PLACEMENT_3D('',#48238,#13247,#13248);
#10936=AXIS2_PLACEMENT_3D('',#48273,#13249,#13250);
#10937=AXIS2_PLACEMENT_3D('',#48304,#13251,#13252);
#10938=AXIS2_PLACEMENT_3D('',#48310,#13253,#13254);
#10939=AXIS2_PLACEMENT_3D('',#48311,#13255,#13256);
#10940=AXIS2_PLACEMENT_3D('',#48313,#13257,#13258);
#10941=AXIS2_PLACEMENT_3D('',#48316,#13260,#13261);
#10942=AXIS2_PLACEMENT_3D('',#48317,#13262,#13263);
#10943=AXIS2_PLACEMENT_3D('',#48319,#13264,#13265);
#10944=AXIS2_PLACEMENT_3D('',#48320,#13266,#13267);
#10945=AXIS2_PLACEMENT_3D('',#48350,#13269,#13270);
#10946=AXIS2_PLACEMENT_3D('',#48379,#13271,#13272);
#10947=AXIS2_PLACEMENT_3D('',#49202,#13273,#13274);
#10948=AXIS2_PLACEMENT_3D('',#49205,#13275,#13276);
#10949=AXIS2_PLACEMENT_3D('',#49207,#13277,#13278);
#10950=AXIS2_PLACEMENT_3D('',#49208,#13279,#13280);
#10951=AXIS2_PLACEMENT_3D('',#49210,#13281,#13282);
#10952=AXIS2_PLACEMENT_3D('',#49211,#13283,#13284);
#10953=AXIS2_PLACEMENT_3D('',#49212,#13285,#13286);
#10954=AXIS2_PLACEMENT_3D('',#49213,#13287,#13288);
#10955=AXIS2_PLACEMENT_3D('',#49217,#13289,#13290);
#10956=AXIS2_PLACEMENT_3D('',#49221,#13291,#13292);
#10957=AXIS2_PLACEMENT_3D('',#49225,#13293,#13294);
#10958=AXIS2_PLACEMENT_3D('',#49229,#13295,#13296);
#10959=AXIS2_PLACEMENT_3D('',#49233,#13297,#13298);
#10960=AXIS2_PLACEMENT_3D('',#49246,#13305,#13306);
#10961=AXIS2_PLACEMENT_3D('',#49249,#13309,#13310);
#10962=AXIS2_PLACEMENT_3D('',#49251,#13312,#13313);
#10963=AXIS2_PLACEMENT_3D('',#49253,#13315,#13316);
#10964=AXIS2_PLACEMENT_3D('',#49255,#13318,#13319);
#10965=AXIS2_PLACEMENT_3D('',#49257,#13321,#13322);
#13144=DIRECTION('axis',(0.,0.,1.));
#13145=DIRECTION('refdir',(1.,0.,0.));
#13146=DIRECTION('center_axis',(-5.55111512312578E-17,1.,-3.44969278837093E-14));
#13147=DIRECTION('ref_axis',(2.08166817117221E-16,3.44969278837093E-14,
1.));
#13148=DIRECTION('',(5.55111512312578E-17,-1.,3.44969278837093E-14));
#13149=DIRECTION('center_axis',(-5.55111512326456E-17,1.,-6.70116359450593E-12));
#13150=DIRECTION('ref_axis',(2.08166817116851E-16,6.70116359450593E-12,
1.));
#13151=DIRECTION('center_axis',(-5.55111512312578E-17,1.,-3.44969278837093E-14));
#13152=DIRECTION('ref_axis',(2.08166817117221E-16,3.44969278837093E-14,
1.));
#13153=DIRECTION('',(5.55111512312578E-17,-1.,3.44969278837093E-14));
#13154=DIRECTION('center_axis',(-5.55111512312578E-17,1.,-3.44969278837093E-14));
#13155=DIRECTION('ref_axis',(2.08166817117221E-16,3.44969278837093E-14,
1.));
#13156=DIRECTION('',(5.55111512312578E-17,-1.,3.44969278837093E-14));
#13157=DIRECTION('center_axis',(-5.55111512312578E-17,1.,-3.44969278837093E-14));
#13158=DIRECTION('ref_axis',(2.08166817117221E-16,3.44969278837093E-14,
1.));
#13159=DIRECTION('',(5.55111512312578E-17,-1.,3.44969278837093E-14));
#13160=DIRECTION('center_axis',(-5.55111512312578E-17,1.,-3.44969278837093E-14));
#13161=DIRECTION('ref_axis',(2.08166817117221E-16,3.44969278837093E-14,
1.));
#13162=DIRECTION('',(5.55111512312578E-17,-1.,3.44969278837093E-14));
#13163=DIRECTION('center_axis',(-5.55111512312578E-17,1.,-3.44969278837093E-14));
#13164=DIRECTION('ref_axis',(2.08166817117221E-16,3.44969278837093E-14,
1.));
#13165=DIRECTION('',(5.55111512312578E-17,-1.,3.44969278837093E-14));
#13166=DIRECTION('center_axis',(-5.55111512312578E-17,1.,-3.44969278837093E-14));
#13167=DIRECTION('ref_axis',(2.08166817117221E-16,3.44969278837093E-14,
1.));
#13168=DIRECTION('',(5.55111512312578E-17,-1.,3.44969278837093E-14));
#13169=DIRECTION('center_axis',(-5.55111512312578E-17,1.,-3.44969278837093E-14));
#13170=DIRECTION('ref_axis',(2.08166817117221E-16,3.44969278837093E-14,
1.));
#13171=DIRECTION('',(5.55111512312578E-17,-1.,3.44969278837093E-14));
#13172=DIRECTION('center_axis',(-5.55111512312578E-17,1.,-3.44969278837093E-14));
#13173=DIRECTION('ref_axis',(2.08166817117221E-16,3.44969278837093E-14,
1.));
#13174=DIRECTION('',(5.55111512312578E-17,-1.,3.44969278837093E-14));
#13175=DIRECTION('center_axis',(-5.55111512312578E-17,1.,-3.44969278837093E-14));
#13176=DIRECTION('ref_axis',(2.08166817117221E-16,3.44969278837093E-14,
1.));
#13177=DIRECTION('',(5.55111512312578E-17,-1.,3.44969278837093E-14));
#13178=DIRECTION('center_axis',(-5.55111512312578E-17,1.,-3.44969278837093E-14));
#13179=DIRECTION('ref_axis',(2.08166817117221E-16,3.44969278837093E-14,
1.));
#13180=DIRECTION('',(5.55111512312578E-17,-1.,3.44969278837093E-14));
#13181=DIRECTION('center_axis',(-5.55111512312578E-17,1.,-3.44969278837093E-14));
#13182=DIRECTION('ref_axis',(2.08166817117221E-16,3.44969278837093E-14,
1.));
#13183=DIRECTION('',(5.55111512312578E-17,-1.,3.44969278837093E-14));
#13184=DIRECTION('center_axis',(-5.55111512312578E-17,1.,-3.44969278837093E-14));
#13185=DIRECTION('ref_axis',(2.08166817117221E-16,3.44969278837093E-14,
1.));
#13186=DIRECTION('',(5.55111512312578E-17,-1.,3.44969278837093E-14));
#13187=DIRECTION('center_axis',(-5.55111512312578E-17,1.,-3.44969278837093E-14));
#13188=DIRECTION('ref_axis',(2.08166817117221E-16,3.44969278837093E-14,
1.));
#13189=DIRECTION('',(5.55111512312578E-17,-1.,3.44969278837093E-14));
#13190=DIRECTION('center_axis',(-5.55111512312578E-17,1.,-3.44969278837093E-14));
#13191=DIRECTION('ref_axis',(2.08166817117221E-16,3.44969278837093E-14,
1.));
#13192=DIRECTION('',(5.55111512312578E-17,-1.,3.44969278837093E-14));
#13193=DIRECTION('center_axis',(5.55111512312577E-17,-1.,3.39243069331623E-14));
#13194=DIRECTION('ref_axis',(-2.08166817117221E-16,-3.39243069331623E-14,
-1.));
#13195=DIRECTION('',(-5.55111512312577E-17,1.,-3.39243069331623E-14));
#13196=DIRECTION('center_axis',(8.50884136963852E-12,1.,-8.54339380881831E-12));
#13197=DIRECTION('ref_axis',(-8.51176958293838E-12,-8.54339380874589E-12,
-1.));
#13198=DIRECTION('center_axis',(5.55111512312577E-17,-1.,3.39243069331623E-14));
#13199=DIRECTION('ref_axis',(-2.08166817117221E-16,-3.39243069331623E-14,
-1.));
#13200=DIRECTION('',(-5.55111512312577E-17,1.,-3.39243069331623E-14));
#13201=DIRECTION('center_axis',(5.55111512312577E-17,-1.,3.39243069331623E-14));
#13202=DIRECTION('ref_axis',(-2.08166817117221E-16,-3.39243069331623E-14,
-1.));
#13203=DIRECTION('',(-5.55111512312577E-17,1.,-3.39243069331623E-14));
#13204=DIRECTION('center_axis',(5.55111512312577E-17,-1.,3.39243069331623E-14));
#13205=DIRECTION('ref_axis',(-2.08166817117221E-16,-3.39243069331623E-14,
-1.));
#13206=DIRECTION('',(-5.55111512312577E-17,1.,-3.39243069331623E-14));
#13207=DIRECTION('center_axis',(5.55111512312577E-17,-1.,3.39243069331623E-14));
#13208=DIRECTION('ref_axis',(-2.08166817117221E-16,-3.39243069331623E-14,
-1.));
#13209=DIRECTION('',(-5.55111512312577E-17,1.,-3.39243069331623E-14));
#13210=DIRECTION('center_axis',(5.55111512312577E-17,-1.,3.39243069331623E-14));
#13211=DIRECTION('ref_axis',(-2.08166817117221E-16,-3.39243069331623E-14,
-1.));
#13212=DIRECTION('',(-5.55111512312577E-17,1.,-3.39243069331623E-14));
#13213=DIRECTION('center_axis',(5.55111512312577E-17,-1.,3.39243069331623E-14));
#13214=DIRECTION('ref_axis',(-2.08166817117221E-16,-3.39243069331623E-14,
-1.));
#13215=DIRECTION('',(-5.55111512312577E-17,1.,-3.39243069331623E-14));
#13216=DIRECTION('center_axis',(5.55111512312577E-17,-1.,3.39243069331623E-14));
#13217=DIRECTION('ref_axis',(-2.08166817117221E-16,-3.39243069331623E-14,
-1.));
#13218=DIRECTION('',(-5.55111512312577E-17,1.,-3.39243069331623E-14));
#13219=DIRECTION('center_axis',(5.55111512312577E-17,-1.,3.39243069331623E-14));
#13220=DIRECTION('ref_axis',(-2.08166817117221E-16,-3.39243069331623E-14,
-1.));
#13221=DIRECTION('',(-5.55111512312577E-17,1.,-3.39243069331623E-14));
#13222=DIRECTION('center_axis',(5.55111512312577E-17,-1.,3.39243069331623E-14));
#13223=DIRECTION('ref_axis',(-2.08166817117221E-16,-3.39243069331623E-14,
-1.));
#13224=DIRECTION('',(-5.55111512312577E-17,1.,-3.39243069331623E-14));
#13225=DIRECTION('center_axis',(5.55111512312577E-17,-1.,3.39243069331623E-14));
#13226=DIRECTION('ref_axis',(-2.08166817117221E-16,-3.39243069331623E-14,
-1.));
#13227=DIRECTION('',(-5.55111512312577E-17,1.,-3.39243069331623E-14));
#13228=DIRECTION('center_axis',(5.55111512312577E-17,-1.,3.39243069331623E-14));
#13229=DIRECTION('ref_axis',(-2.08166817117221E-16,-3.39243069331623E-14,
-1.));
#13230=DIRECTION('',(-5.55111512312577E-17,1.,-3.39243069331623E-14));
#13231=DIRECTION('center_axis',(5.55111512312577E-17,-1.,3.39243069331623E-14));
#13232=DIRECTION('ref_axis',(-2.08166817117221E-16,-3.39243069331623E-14,
-1.));
#13233=DIRECTION('',(-5.55111512312577E-17,1.,-3.39243069331623E-14));
#13234=DIRECTION('center_axis',(5.55111512312577E-17,-1.,3.39243069331623E-14));
#13235=DIRECTION('ref_axis',(-2.08166817117221E-16,-3.39243069331623E-14,
-1.));
#13236=DIRECTION('',(-5.55111512312577E-17,1.,-3.39243069331623E-14));
#13237=DIRECTION('center_axis',(5.55111512312577E-17,-1.,3.39243069331623E-14));
#13238=DIRECTION('ref_axis',(-2.08166817117221E-16,-3.39243069331623E-14,
-1.));
#13239=DIRECTION('',(-5.55111512312577E-17,1.,-3.39243069331623E-14));
#13240=DIRECTION('center_axis',(5.55111512312577E-17,-1.,3.39243069331623E-14));
#13241=DIRECTION('ref_axis',(-2.08166817117221E-16,-3.39243069331623E-14,
-1.));
#13242=DIRECTION('',(-5.55111512312577E-17,1.,-3.39243069331623E-14));
#13243=DIRECTION('center_axis',(5.55111512312577E-17,-1.,3.39243069331623E-14));
#13244=DIRECTION('ref_axis',(-2.08166817117221E-16,-3.39243069331623E-14,
-1.));
#13245=DIRECTION('center_axis',(-5.55111512330291E-17,1.,-8.54339380874589E-12));
#13246=DIRECTION('ref_axis',(-2.08166817116748E-16,-8.54339380874589E-12,
-1.));
#13247=DIRECTION('center_axis',(-5.55111512312578E-17,1.,-3.44969278837093E-14));
#13248=DIRECTION('ref_axis',(2.08166817117221E-16,3.44969278837093E-14,
1.));
#13249=DIRECTION('center_axis',(5.55111512326456E-17,-1.,6.70116359450593E-12));
#13250=DIRECTION('ref_axis',(2.08166817116851E-16,6.70116359450593E-12,
1.));
#13251=DIRECTION('center_axis',(5.55111512312578E-17,-1.,3.43614026121486E-14));
#13252=DIRECTION('ref_axis',(1.,5.55111512312506E-17,-2.08166817117223E-16));
#13253=DIRECTION('center_axis',(5.55111512312578E-17,-1.,3.43614026121486E-14));
#13254=DIRECTION('ref_axis',(1.,5.55111512312506E-17,-2.08166817117223E-16));
#13255=DIRECTION('center_axis',(5.55111512312578E-17,-1.,3.43614026121486E-14));
#13256=DIRECTION('ref_axis',(1.,5.55111512312506E-17,-2.08166817117223E-16));
#13257=DIRECTION('center_axis',(5.55111512312578E-17,-1.,3.43614026121486E-14));
#13258=DIRECTION('ref_axis',(1.,5.55111512312506E-17,-2.08166817117223E-16));
#13259=DIRECTION('',(-5.55111512312578E-17,1.,-3.43614026121486E-14));
#13260=DIRECTION('center_axis',(5.55111512312578E-17,-1.,3.43614026121486E-14));
#13261=DIRECTION('ref_axis',(1.,5.55111512312506E-17,-2.08166817117223E-16));
#13262=DIRECTION('center_axis',(1.,0.,6.56279692788602E-15));
#13263=DIRECTION('ref_axis',(6.56279692788602E-15,-3.50015836153921E-14,
-1.));
#13264=DIRECTION('center_axis',(5.55111512312578E-17,-1.,3.43614026121486E-14));
#13265=DIRECTION('ref_axis',(1.,5.55111512312506E-17,-2.08166817117223E-16));
#13266=DIRECTION('center_axis',(5.55111512312578E-17,-1.,3.44969278837093E-14));
#13267=DIRECTION('ref_axis',(-2.08166817117221E-16,-3.44969278837093E-14,
-1.));
#13268=DIRECTION('',(-9.98528738451518E-17,0.707106781186525,-0.70710678118657));
#13269=DIRECTION('center_axis',(-5.55111512331082E-17,1.,-8.92338581669359E-12));
#13270=DIRECTION('ref_axis',(2.08166817116727E-16,8.92338581669359E-12,
1.));
#13271=DIRECTION('center_axis',(-5.55111512312578E-17,1.,-3.44969278837093E-14));
#13272=DIRECTION('ref_axis',(-2.08166817117221E-16,-3.44969278837093E-14,
-1.));
#13273=DIRECTION('center_axis',(-5.55111512312578E-17,1.,-3.43614026121486E-14));
#13274=DIRECTION('ref_axis',(-2.08166817117221E-16,-3.43614026121486E-14,
-1.));
#13275=DIRECTION('center_axis',(5.55111512312578E-17,-1.,3.43614026121486E-14));
#13276=DIRECTION('ref_axis',(1.,5.55111512312506E-17,-2.08166817117223E-16));
#13277=DIRECTION('center_axis',(5.55111512312578E-17,-1.,3.43614026121486E-14));
#13278=DIRECTION('ref_axis',(1.,5.55111512312506E-17,-2.08166817117223E-16));
#13279=DIRECTION('center_axis',(5.55111512312578E-17,-1.,3.43614026121486E-14));
#13280=DIRECTION('ref_axis',(1.,5.55111512312506E-17,-2.08166817117223E-16));
#13281=DIRECTION('center_axis',(5.55111512312578E-17,-1.,3.43614026121486E-14));
#13282=DIRECTION('ref_axis',(1.,5.55111512312506E-17,-2.08166817117223E-16));
#13283=DIRECTION('center_axis',(5.55111512312578E-17,-1.,3.43614026121486E-14));
#13284=DIRECTION('ref_axis',(1.,5.55111512312506E-17,-2.08166817117223E-16));
#13285=DIRECTION('center_axis',(5.55111512312578E-17,-1.,3.43614026121486E-14));
#13286=DIRECTION('ref_axis',(1.,5.55111512312506E-17,-2.08166817117223E-16));
#13287=DIRECTION('center_axis',(5.55111512312578E-17,-1.,3.43614026121486E-14));
#13288=DIRECTION('ref_axis',(1.,5.55111512312506E-17,-2.08166817117223E-16));
#13289=DIRECTION('center_axis',(5.55111512312578E-17,-1.,3.43614026121486E-14));
#13290=DIRECTION('ref_axis',(1.,5.55111512312506E-17,-2.08166817117223E-16));
#13291=DIRECTION('center_axis',(5.55111512312578E-17,-1.,3.43614026121486E-14));
#13292=DIRECTION('ref_axis',(-1.,-5.55111512312617E-17,-1.13457712818104E-16));
#13293=DIRECTION('center_axis',(5.55111512312578E-17,-1.,3.43614026121486E-14));
#13294=DIRECTION('ref_axis',(1.,5.55111512312506E-17,-2.08166817117223E-16));
#13295=DIRECTION('center_axis',(5.55111512312578E-17,-1.,3.43614026121486E-14));
#13296=DIRECTION('ref_axis',(1.,5.55111512312506E-17,-2.08166817117223E-16));
#13297=DIRECTION('center_axis',(5.55111512312578E-17,-1.,3.43614026121486E-14));
#13298=DIRECTION('ref_axis',(1.,5.55111512312506E-17,-2.08166817117223E-16));
#13299=DIRECTION('',(0.866025403784438,1.71326272389147E-14,0.500000000000001));
#13300=DIRECTION('',(2.08166817117221E-16,3.43614026121486E-14,1.));
#13301=DIRECTION('',(-0.866025403784438,1.72287753732339E-14,0.500000000000001));
#13302=DIRECTION('',(-0.866025403784438,-1.71326272389147E-14,-0.500000000000001));
#13303=DIRECTION('',(9.97962250772482E-15,-3.43614026121486E-14,-1.));
#13304=DIRECTION('',(0.866025403784438,-1.72287753732339E-14,-0.500000000000001));
#13305=DIRECTION('center_axis',(1.,-5.5511151231265E-17,-2.08166817117219E-16));
#13306=DIRECTION('ref_axis',(2.08166817117221E-16,3.43614026121486E-14,
1.));
#13307=DIRECTION('',(5.55111512312578E-17,-1.,3.43614026121486E-14));
#13308=DIRECTION('',(5.55111512312578E-17,-1.,3.43614026121486E-14));
#13309=DIRECTION('center_axis',(0.5,2.97300919961701E-14,0.866025403784439));
#13310=DIRECTION('ref_axis',(-2.77555756156401E-17,1.,-3.43133285449891E-14));
#13311=DIRECTION('',(5.55111512312578E-17,-1.,3.43614026121486E-14));
#13312=DIRECTION('center_axis',(-0.5,2.97856031474013E-14,0.866025403784439));
#13313=DIRECTION('ref_axis',(2.77555756156334E-17,-1.,3.44094766793082E-14));
#13314=DIRECTION('',(5.55111512312578E-17,-1.,3.43614026121486E-14));
#13315=DIRECTION('center_axis',(-1.,5.55111512312585E-17,2.0377492275074E-17));
#13316=DIRECTION('ref_axis',(2.03774922750759E-17,3.43614026121486E-14,
1.));
#13317=DIRECTION('',(5.55111512312578E-17,-1.,3.43614026121486E-14));
#13318=DIRECTION('center_axis',(-0.5,-2.97300919961701E-14,-0.866025403784439));
#13319=DIRECTION('ref_axis',(-0.866025403784439,1.72287753732339E-14,0.5));
#13320=DIRECTION('',(5.55111512312578E-17,-1.,3.43614026121486E-14));
#13321=DIRECTION('center_axis',(0.5,-2.97856031474012E-14,-0.866025403784438));
#13322=DIRECTION('ref_axis',(-2.77555756156474E-17,1.,-3.44094766793081E-14));
#45885=CARTESIAN_POINT('',(0.,0.,0.));
#45886=CARTESIAN_POINT('Origin',(-0.0125,-0.0332787743898722,-0.0121758532865583));
#45887=CARTESIAN_POINT('',(-0.0125000000000001,-0.0410287743898722,-0.013675853286558));
#45888=CARTESIAN_POINT('',(-0.0125,-0.0410912743898722,-0.013675853286558));
#45889=CARTESIAN_POINT('',(-0.0125,-0.0332787743898722,-0.0136758532865583));
#45890=CARTESIAN_POINT('',(-0.0125,-0.0412787743898722,-0.0106758532865581));
#45891=CARTESIAN_POINT('Ctrl Pts',(-0.0125000000000001,-0.0410287743898722,
-0.013675853286558));
#45892=CARTESIAN_POINT('Ctrl Pts',(-0.0123310037568044,-0.0410369052254139,
-0.013675853286558));
#45893=CARTESIAN_POINT('Ctrl Pts',(-0.0121630120248185,-0.0410457809002103,
-0.0136472992089388));
#45894=CARTESIAN_POINT('Ctrl Pts',(-0.011817556294753,-0.0410657705028026,
-0.0135260203918559));
#45895=CARTESIAN_POINT('Ctrl Pts',(-0.0116465966412278,-0.0410768017393218,
-0.013425006683115));
#45896=CARTESIAN_POINT('Ctrl Pts',(-0.0113584236030566,-0.041097826154242,
-0.0131672580894708));
#45897=CARTESIAN_POINT('Ctrl Pts',(-0.0112422133833523,-0.0411071596872922,
-0.0130149179329953));
#45898=CARTESIAN_POINT('Ctrl Pts',(-0.0110687981756656,-0.0411264893050654,
-0.0126669848130804));
#45899=CARTESIAN_POINT('Ctrl Pts',(-0.0110163755255651,-0.041137257974845,
-0.0124731487570469));
#45900=CARTESIAN_POINT('Ctrl Pts',(-0.0109904456301969,-0.0411590554039909,
-0.0120807950324208));
#45901=CARTESIAN_POINT('Ctrl Pts',(-0.0110154549296438,-0.0411698689270392,
-0.0118861516175517));
#45902=CARTESIAN_POINT('Ctrl Pts',(-0.0111374431285804,-0.0411902090678481,
-0.0115200290829898));
#45903=CARTESIAN_POINT('Ctrl Pts',(-0.0112321814406848,-0.0411990041550593,
-0.0113516555803048));
#45904=CARTESIAN_POINT('Ctrl Pts',(-0.0114852510225052,-0.0412194684440373,
-0.0110532705506603));
#45905=CARTESIAN_POINT('Ctrl Pts',(-0.0116435964173627,-0.0412305591150924,
-0.0109282686617132));
#45906=CARTESIAN_POINT('Ctrl Pts',(-0.0119282935685727,-0.0412482657298701,
-0.0107839404603842));
#45907=CARTESIAN_POINT('Ctrl Pts',(-0.0120409179303487,-0.0412548259507756,
-0.0107428436245518));
#45908=CARTESIAN_POINT('Ctrl Pts',(-0.0122696303330434,-0.0412673211268715,
-0.0106891587868862));
#45909=CARTESIAN_POINT('Ctrl Pts',(-0.0123846449056647,-0.0412732243653083,
-0.010675853286558));
#45910=CARTESIAN_POINT('Ctrl Pts',(-0.0125000000000008,-0.0412787743898722,
-0.010675853286558));
#45911=CARTESIAN_POINT('',(-0.0114490560961827,-0.0412787743898703,-0.0111055650491926));
#45912=CARTESIAN_POINT('Origin',(-0.0125,-0.0412787743898622,-0.0121758532865581));
#45913=CARTESIAN_POINT('Ctrl Pts',(-0.0114490560961864,-0.0412787743898736,
-0.0111055650491953));
#45914=CARTESIAN_POINT('Ctrl Pts',(-0.011369903560121,-0.0412728072190045,
-0.0111832869864692));
#45915=CARTESIAN_POINT('Ctrl Pts',(-0.0112996137814574,-0.0412670291836058,
-0.0112695507929254));
#45916=CARTESIAN_POINT('Ctrl Pts',(-0.0111804215237056,-0.041256161491045,
-0.0114543406788185));
#45917=CARTESIAN_POINT('Ctrl Pts',(-0.0111315202178879,-0.0412509305323926,
-0.0115520427211916));
#45918=CARTESIAN_POINT('Ctrl Pts',(-0.0110262339331569,-0.0412351603642107,
-0.0118359057484655));
#45919=CARTESIAN_POINT('Ctrl Pts',(-0.0109946931267627,-0.0412244372150451,
-0.0120289224334467));
#45920=CARTESIAN_POINT('Ctrl Pts',(-0.0110069213898787,-0.0412026370083603,
-0.012421326153772));
#45921=CARTESIAN_POINT('Ctrl Pts',(-0.0110525758723153,-0.0411917716832378,
-0.0126169020059778));
#45922=CARTESIAN_POINT('Ctrl Pts',(-0.0112138449798316,-0.0411721120389683,
-0.0129707756028294));
#45923=CARTESIAN_POINT('Ctrl Pts',(-0.0113247528666018,-0.0411630611644425,
-0.0131271171485231));
#45924=CARTESIAN_POINT('Ctrl Pts',(-0.0116033993474256,-0.0411422340676681,
-0.0133942627702646));
#45925=CARTESIAN_POINT('Ctrl Pts',(-0.0117700971634697,-0.0411312526809726,
-0.0135008636044037));
#45926=CARTESIAN_POINT('Ctrl Pts',(-0.012127119866988,-0.0411101878892364,
-0.0136408146449594));
#45927=CARTESIAN_POINT('Ctrl Pts',(-0.0123128074865679,-0.0411002806938739,
-0.013675853286558));
#45928=CARTESIAN_POINT('Ctrl Pts',(-0.0125,-0.0410912743898722,-0.013675853286558));
#45929=CARTESIAN_POINT('Origin',(-0.0125,-0.0332787743898722,-0.0121758532865583));
#45930=CARTESIAN_POINT('',(-0.0125000000060198,-0.0405287743892929,-0.0136758532865581));
#45931=CARTESIAN_POINT('',(-0.0125,-0.0405912743898722,-0.013675853286558));
#45932=CARTESIAN_POINT('',(-0.0125,-0.0332787743898722,-0.0136758532865583));
#45933=CARTESIAN_POINT('Ctrl Pts',(-0.0125000000120396,-0.0405287743892929,
-0.013675853286558));
#45934=CARTESIAN_POINT('Ctrl Pts',(-0.0124987572094776,-0.0405288341836588,
-0.013675853286568));
#45935=CARTESIAN_POINT('Ctrl Pts',(-0.0124975143416151,-0.0405288940240707,
-0.0136758517420196));
#45936=CARTESIAN_POINT('Ctrl Pts',(-0.0122974686446526,-0.0405385325399391,
-0.013675354481734));
#45937=CARTESIAN_POINT('Ctrl Pts',(-0.0121007703785393,-0.0405491076079653,
-0.0136353434234573));
#45938=CARTESIAN_POINT('Ctrl Pts',(-0.0117374538093306,-0.0405708394897221,
-0.0134822784373148));
#45939=CARTESIAN_POINT('Ctrl Pts',(-0.0115738416018138,-0.0405817781404356,
-0.0133718716677857));
#45940=CARTESIAN_POINT('Ctrl Pts',(-0.011301901014316,-0.0406024633052192,
-0.0130982206497631));
#45941=CARTESIAN_POINT('Ctrl Pts',(-0.0111947045203311,-0.0406113771296748,
-0.0129390039701075));
#45942=CARTESIAN_POINT('Ctrl Pts',(-0.011042116736427,-0.0406312662509237,
-0.0125809997876281));
#45943=CARTESIAN_POINT('Ctrl Pts',(-0.0110013057341337,-0.0406421920366129,
-0.0123843356452229));
#45944=CARTESIAN_POINT('Ctrl Pts',(-0.0109987917193966,-0.0406639779942384,
-0.0119921884079635));
#45945=CARTESIAN_POINT('Ctrl Pts',(-0.011034922411109,-0.0406746296998768,
-0.011800457706473));
#45946=CARTESIAN_POINT('Ctrl Pts',(-0.0111781023805049,-0.0406946024933454,
-0.0114409474240369));
#45947=CARTESIAN_POINT('Ctrl Pts',(-0.0112838956978466,-0.0407035761797072,
-0.0112766344138636));
#45948=CARTESIAN_POINT('Ctrl Pts',(-0.0115555377678104,-0.040724503960149,
-0.0109937321846102));
#45949=CARTESIAN_POINT('Ctrl Pts',(-0.0117201175586749,-0.0407356025304129,
-0.0108792442147851));
#45950=CARTESIAN_POINT('Ctrl Pts',(-0.0120774319930893,-0.0407571067909325,
-0.0107239775907649));
#45951=CARTESIAN_POINT('Ctrl Pts',(-0.0122656438239637,-0.0407673282668937,
-0.0106819969098197));
#45952=CARTESIAN_POINT('Ctrl Pts',(-0.0126553925473199,-0.0407863927730581,
-0.0106707392789394));
#45953=CARTESIAN_POINT('Ctrl Pts',(-0.0128533159096088,-0.0407965705151329,
-0.0107045526893804));
#45954=CARTESIAN_POINT('Ctrl Pts',(-0.013221934375852,-0.0408182477555405,
-0.0108464674319101));
#45955=CARTESIAN_POINT('Ctrl Pts',(-0.013389366022574,-0.0408292385129775,
-0.0109521345807257));
#45956=CARTESIAN_POINT('Ctrl Pts',(-0.0136696297580511,-0.0408500994714692,
-0.0112176980570621));
#45957=CARTESIAN_POINT('Ctrl Pts',(-0.0137814349586155,-0.0408591910787262,
-0.0113733536859315));
#45958=CARTESIAN_POINT('Ctrl Pts',(-0.0139447812266889,-0.0408787950173215,
-0.0117262245806454));
#45959=CARTESIAN_POINT('Ctrl Pts',(-0.0139915942490026,-0.0408896448117446,
-0.0119215208802603));
#45960=CARTESIAN_POINT('Ctrl Pts',(-0.0140061572662983,-0.0409114464355421,
-0.0123139501086151));
#45961=CARTESIAN_POINT('Ctrl Pts',(-0.0139757246497111,-0.0409221858438013,
-0.0125072594572816));
#45962=CARTESIAN_POINT('Ctrl Pts',(-0.0138434593065443,-0.0409423501554539,
-0.0128702170670279));
#45963=CARTESIAN_POINT('Ctrl Pts',(-0.0137434259685003,-0.0409511935153639,
-0.013036618757154));
#45964=CARTESIAN_POINT('Ctrl Pts',(-0.0134813821431137,-0.0409718843948055,
-0.0133276171976694));
#45965=CARTESIAN_POINT('Ctrl Pts',(-0.0133199546623563,-0.0409829838826118,
-0.0134475981602884));
#45966=CARTESIAN_POINT('Ctrl Pts',(-0.0129665065567941,-0.0410046194391406,
-0.0136142881186541));
#45967=CARTESIAN_POINT('Ctrl Pts',(-0.0127790874858517,-0.0410149640512427,
-0.0136620748011502));
#45968=CARTESIAN_POINT('Ctrl Pts',(-0.0125584819942821,-0.0410259369456405,
-0.0136749990796436));
#45969=CARTESIAN_POINT('Ctrl Pts',(-0.0125292271033337,-0.0410273682002074,
-0.013675853286558));
#45970=CARTESIAN_POINT('Ctrl Pts',(-0.0125000000000001,-0.0410287743898722,
-0.013675853286558));
#45971=CARTESIAN_POINT('Ctrl Pts',(-0.0125,-0.0410912743898722,-0.013675853286558));
#45972=CARTESIAN_POINT('Ctrl Pts',(-0.0125113747299722,-0.0410907271229213,
-0.013675853286558));
#45973=CARTESIAN_POINT('Ctrl Pts',(-0.0125227546763987,-0.0410901760109885,
-0.0136757239023752));
#45974=CARTESIAN_POINT('Ctrl Pts',(-0.0127251001422328,-0.0410803127085477,
-0.0136711176420125));
#45975=CARTESIAN_POINT('Ctrl Pts',(-0.0129134534013763,-0.0410701177212372,
-0.0136303355134427));
#45976=CARTESIAN_POINT('Ctrl Pts',(-0.0132715207217928,-0.0410486429794191,
-0.0134774355994801));
#45977=CARTESIAN_POINT('Ctrl Pts',(-0.0134367284628191,-0.0410375459405851,
-0.0133640904027179));
#45978=CARTESIAN_POINT('Ctrl Pts',(-0.0137103402832416,-0.0410165702878582,
-0.0130828764790717));
#45979=CARTESIAN_POINT('Ctrl Pts',(-0.0138173294561724,-0.0410075597821429,
-0.0129189903474292));
#45980=CARTESIAN_POINT('Ctrl Pts',(-0.0139627406925233,-0.0409876267591427,
-0.0125601959334253));
#45981=CARTESIAN_POINT('Ctrl Pts',(-0.0140000274969595,-0.0409769941033067,
-0.0123688081283793));
#45982=CARTESIAN_POINT('Ctrl Pts',(-0.013999971375087,-0.040955102830591,
-0.0119747652194958));
#45983=CARTESIAN_POINT('Ctrl Pts',(-0.0139595925151208,-0.0409440550648995,
-0.0117759054370492));
#45984=CARTESIAN_POINT('Ctrl Pts',(-0.0138070343033204,-0.0409240423457135,
-0.0114156764917013));
#45985=CARTESIAN_POINT('Ctrl Pts',(-0.0137001812896997,-0.0409151386209105,
-0.011256190631885));
#45986=CARTESIAN_POINT('Ctrl Pts',(-0.0134288624351978,-0.0408944667371465,
-0.0109819408574324));
#45987=CARTESIAN_POINT('Ctrl Pts',(-0.0132655396963218,-0.0408835323615525,
-0.0108711866178111));
#45988=CARTESIAN_POINT('Ctrl Pts',(-0.0129026172736487,-0.0408617964416594,
-0.010717293576936));
#45989=CARTESIAN_POINT('Ctrl Pts',(-0.0127060091691163,-0.0408512130176722,
-0.0106768255396282));
#45990=CARTESIAN_POINT('Ctrl Pts',(-0.0123168175128777,-0.0408324360956953,
-0.0106749560709455));
#45991=CARTESIAN_POINT('Ctrl Pts',(-0.0121279086191053,-0.0408224153260697,
-0.0107102984066759));
#45992=CARTESIAN_POINT('Ctrl Pts',(-0.0117665402452652,-0.0408010779468522,
-0.0108525356747639));
#45993=CARTESIAN_POINT('Ctrl Pts',(-0.0115985989294966,-0.0407899934803529,
-0.0109606935771387));
#45994=CARTESIAN_POINT('Ctrl Pts',(-0.0113161557621315,-0.0407688064846784,
-0.0112342195052963));
#45995=CARTESIAN_POINT('Ctrl Pts',(-0.0112037429817825,-0.0407595888241137,
-0.0113961934702125));
#45996=CARTESIAN_POINT('Ctrl Pts',(-0.0110483591824526,-0.0407398361172091,
-0.0117517421944951));
#45997=CARTESIAN_POINT('Ctrl Pts',(-0.0110059452638139,-0.0407292931602785,
-0.0119415154192466));
#45998=CARTESIAN_POINT('Ctrl Pts',(-0.0109950050778346,-0.040707471801418,
-0.012334299878735));
#45999=CARTESIAN_POINT('Ctrl Pts',(-0.0110295836685338,-0.0406963977400064,
-0.0125336329841446));
#46000=CARTESIAN_POINT('Ctrl Pts',(-0.0111715482076857,-0.0406761503208377,
-0.0128980865291808));
#46001=CARTESIAN_POINT('Ctrl Pts',(-0.0112740700591782,-0.0406673359253655,
-0.0130610109528272));
#46002=CARTESIAN_POINT('Ctrl Pts',(-0.0115375390549893,-0.0406468334447887,
-0.013342758566626));
#46003=CARTESIAN_POINT('Ctrl Pts',(-0.0116971602707559,-0.0406359575123747,
-0.0134578200778564));
#46004=CARTESIAN_POINT('Ctrl Pts',(-0.0120549643964648,-0.0406141809859732,
-0.0136220401034243));
#46005=CARTESIAN_POINT('Ctrl Pts',(-0.0122503452868441,-0.0406034974610594,
-0.0136682373713582));
#46006=CARTESIAN_POINT('Ctrl Pts',(-0.0124660532323911,-0.0405929156522489,
-0.0136755653672513));
#46007=CARTESIAN_POINT('Ctrl Pts',(-0.012483031769083,-0.0405920907742628,
-0.013675853286558));
#46008=CARTESIAN_POINT('Ctrl Pts',(-0.0125,-0.0405912743898722,-0.013675853286558));
#46009=CARTESIAN_POINT('Origin',(-0.0125,-0.0332787743898722,-0.0121758532865583));
#46010=CARTESIAN_POINT('',(-0.0124999999999999,-0.0400287743898722,-0.0136758532865581));
#46011=CARTESIAN_POINT('',(-0.0124999999999999,-0.0400912743898722,-0.0136758532865581));
#46012=CARTESIAN_POINT('',(-0.0125,-0.0332787743898722,-0.0136758532865583));
#46013=CARTESIAN_POINT('Ctrl Pts',(-0.0124999999999999,-0.0400287743898722,
-0.0136758532865581));
#46014=CARTESIAN_POINT('Ctrl Pts',(-0.0124694471611225,-0.0400302443640181,
-0.0136758532865581));
#46015=CARTESIAN_POINT('Ctrl Pts',(-0.0124388664803809,-0.0400317416070417,
-0.0136749198304824));
#46016=CARTESIAN_POINT('Ctrl Pts',(-0.0122098031798663,-0.040043152132264,
-0.0136608901971213));
#46017=CARTESIAN_POINT('Ctrl Pts',(-0.0120157224682894,-0.0400539206585675,
-0.0136093809034139));
#46018=CARTESIAN_POINT('Ctrl Pts',(-0.0116629600624993,-0.0400757180652648,
-0.0134356766721402));
#46019=CARTESIAN_POINT('Ctrl Pts',(-0.0115068921859352,-0.0400865317053801,
-0.0133167031196287));
#46020=CARTESIAN_POINT('Ctrl Pts',(-0.0112508017365673,-0.040106872136986,
-0.0130280092514512));
#46021=CARTESIAN_POINT('Ctrl Pts',(-0.0111523479187016,-0.0401156672027425,
-0.0128617826548918));
#46022=CARTESIAN_POINT('Ctrl Pts',(-0.0110204556653628,-0.0401361311101657,
-0.0124934323212756));
#46023=CARTESIAN_POINT('Ctrl Pts',(-0.010991363760272,-0.0401472217588229,
-0.0122938006454451));
#46024=CARTESIAN_POINT('Ctrl Pts',(-0.0110126554031447,-0.0401689616212987,
-0.0119024831208814));
#46025=CARTESIAN_POINT('Ctrl Pts',(-0.0110598708065288,-0.0401794126837581,
-0.0117143639966109));
#46026=CARTESIAN_POINT('Ctrl Pts',(-0.0112247217947709,-0.040198990321795,
-0.0113619665119461));
#46027=CARTESIAN_POINT('Ctrl Pts',(-0.0113424057089055,-0.0402084693809643,
-0.0112018214805116));
#46028=CARTESIAN_POINT('Ctrl Pts',(-0.0116332683993669,-0.0402298525779533,
-0.0109358153468117));
#46029=CARTESIAN_POINT('Ctrl Pts',(-0.0118036878778282,-0.0402409162520149,
-0.0108326982758898));
#46030=CARTESIAN_POINT('Ctrl Pts',(-0.0121679453562284,-0.0402621064966329,
-0.010700761929268));
#46031=CARTESIAN_POINT('Ctrl Pts',(-0.0123573587950066,-0.0402717657912653,
-0.0106706055510168));
#46032=CARTESIAN_POINT('Ctrl Pts',(-0.0127460490307744,-0.0402908073618348,
-0.010682870854761));
#46033=CARTESIAN_POINT('Ctrl Pts',(-0.0129415380509213,-0.0403014829530466,
-0.010728595223169));
#46034=CARTESIAN_POINT('Ctrl Pts',(-0.0132997771202757,-0.0403232568342346,
-0.0108919666765583));
#46035=CARTESIAN_POINT('Ctrl Pts',(-0.0134597089744393,-0.0403341379321879,
-0.0110066761057188));
#46036=CARTESIAN_POINT('Ctrl Pts',(-0.0137238299600728,-0.0403546546024114,
-0.0112878052673025));
#46037=CARTESIAN_POINT('Ctrl Pts',(-0.0138267112847511,-0.0403634737192496,
-0.0114504412153531));
#46038=CARTESIAN_POINT('Ctrl Pts',(-0.0139695604469646,-0.0403837018117274,
-0.0118145468799539));
#46039=CARTESIAN_POINT('Ctrl Pts',(-0.0140046223532685,-0.0403947740259202,
-0.0120138467354232));
#46040=CARTESIAN_POINT('Ctrl Pts',(-0.013994596363098,-0.0404166018478708,
-0.0124067475305343));
#46041=CARTESIAN_POINT('Ctrl Pts',(-0.0139526076603594,-0.0404271525714348,
-0.0125966605546868));
#46042=CARTESIAN_POINT('Ctrl Pts',(-0.0137980560284191,-0.0404469204853329,
-0.0129524830048515));
#46043=CARTESIAN_POINT('Ctrl Pts',(-0.0136861008222104,-0.0404561181892372,
-0.0131146169506719));
#46044=CARTESIAN_POINT('Ctrl Pts',(-0.013404396191646,-0.0404772877229826,
-0.0133887934326412));
#46045=CARTESIAN_POINT('Ctrl Pts',(-0.0132366782755996,-0.0404883736009471,
-0.013497389087432));
#46046=CARTESIAN_POINT('Ctrl Pts',(-0.0128767235416822,-0.0405096552507722,
-0.0136400685935656));
#46047=CARTESIAN_POINT('Ctrl Pts',(-0.0126891657892081,-0.0405196731465533,
-0.0136758532850397));
#46048=CARTESIAN_POINT('Ctrl Pts',(-0.0125000000120396,-0.0405287743892929,
-0.013675853286558));
#46049=CARTESIAN_POINT('Ctrl Pts',(-0.0125,-0.0405912743898722,-0.013675853286558));
#46050=CARTESIAN_POINT('Ctrl Pts',(-0.0126727962989084,-0.0405829607240647,
-0.013675853286558));
#46051=CARTESIAN_POINT('Ctrl Pts',(-0.0128444453311079,-0.0405738729629493,
-0.0136459987312399));
#46052=CARTESIAN_POINT('Ctrl Pts',(-0.0131929587111633,-0.040553625536909,
-0.0135207342751592));
#46053=CARTESIAN_POINT('Ctrl Pts',(-0.0133635929868223,-0.0405425641398687,
-0.0134180712166641));
#46054=CARTESIAN_POINT('Ctrl Pts',(-0.0136552065447141,-0.0405211637088506,
-0.0131527451984548));
#46055=CARTESIAN_POINT('Ctrl Pts',(-0.0137733655749261,-0.0405116583157249,
-0.0129927639519044));
#46056=CARTESIAN_POINT('Ctrl Pts',(-0.0139390592873679,-0.0404920964463481,
-0.012640650303122));
#46057=CARTESIAN_POINT('Ctrl Pts',(-0.0139866987686684,-0.0404816538751068,
-0.0124526840207797));
#46058=CARTESIAN_POINT('Ctrl Pts',(-0.0140089072219678,-0.0404599219717202,
-0.012061509759821));
#46059=CARTESIAN_POINT('Ctrl Pts',(-0.0139803025204997,-0.0404488302397,
-0.0118618585834583));
#46060=CARTESIAN_POINT('Ctrl Pts',(-0.013849307610282,-0.0404283473669271,
-0.0114931668735456));
#46061=CARTESIAN_POINT('Ctrl Pts',(-0.0137512141637692,-0.0404195509932525,
-0.011326644505451));
#46062=CARTESIAN_POINT('Ctrl Pts',(-0.0134957770731844,-0.0403992250386819,
-0.0110373401599413));
#46063=CARTESIAN_POINT('Ctrl Pts',(-0.0133400270608699,-0.0403884172488764,
-0.0109180266615527));
#46064=CARTESIAN_POINT('Ctrl Pts',(-0.01298772143095,-0.0403666187882543,
-0.01074349332997));
#46065=CARTESIAN_POINT('Ctrl Pts',(-0.0127937625255864,-0.0403558431576918,
-0.0106915173083895));
#46066=CARTESIAN_POINT('Ctrl Pts',(-0.012405793577543,-0.0403364909631712,
-0.010666820235419));
#46067=CARTESIAN_POINT('Ctrl Pts',(-0.0122157058669701,-0.0403271798962426,
-0.0106908431745191));
#46068=CARTESIAN_POINT('Ctrl Pts',(-0.0118481678724113,-0.0403061687289893,
-0.0108106507153509));
#46069=CARTESIAN_POINT('Ctrl Pts',(-0.0116750154297604,-0.0402951404696745,
-0.0109077592225594));
#46070=CARTESIAN_POINT('Ctrl Pts',(-0.0113743103213689,-0.0402735349761782,
-0.0111647204625964));
#46071=CARTESIAN_POINT('Ctrl Pts',(-0.0112503297515439,-0.0402636715557126,
-0.0113227043014299));
#46072=CARTESIAN_POINT('Ctrl Pts',(-0.0110744481394087,-0.0402443027342696,
-0.0116713430874041));
#46073=CARTESIAN_POINT('Ctrl Pts',(-0.0110217276392305,-0.0402339667415927,
-0.0118573909555889));
#46074=CARTESIAN_POINT('Ctrl Pts',(-0.0109885016422904,-0.0402123400312024,
-0.0122466717426135));
#46075=CARTESIAN_POINT('Ctrl Pts',(-0.0110112352664487,-0.04020124024701,
-0.0124464678580768));
#46076=CARTESIAN_POINT('Ctrl Pts',(-0.0111313730440562,-0.0401805319503916,
-0.012819217197209));
#46077=CARTESIAN_POINT('Ctrl Pts',(-0.0112251248681721,-0.0401716818652295,
-0.0129893326753298));
#46078=CARTESIAN_POINT('Ctrl Pts',(-0.0114727097220533,-0.0401515313486256,
-0.0132859217269655));
#46079=CARTESIAN_POINT('Ctrl Pts',(-0.0116246004946155,-0.0401407980247833,
-0.0134092388500089));
#46080=CARTESIAN_POINT('Ctrl Pts',(-0.0119712889551903,-0.0401189968436632,
-0.013593599342218));
#46081=CARTESIAN_POINT('Ctrl Pts',(-0.0121637008225687,-0.0401081411524129,
-0.0136511370969502));
#46082=CARTESIAN_POINT('Ctrl Pts',(-0.0124077851078071,-0.0400957700688394,
-0.0136737297222342));
#46083=CARTESIAN_POINT('Ctrl Pts',(-0.0124539166169377,-0.0400934915776735,
-0.0136758532865581));
#46084=CARTESIAN_POINT('Ctrl Pts',(-0.0124999999999998,-0.0400912743898722,
-0.0136758532865581));
#46085=CARTESIAN_POINT('Origin',(-0.0125,-0.0332787743898722,-0.0121758532865583));
#46086=CARTESIAN_POINT('',(-0.0124999999999999,-0.0395287743898722,-0.0136758532865581));
#46087=CARTESIAN_POINT('',(-0.0125,-0.0395912743898722,-0.0136758532865581));
#46088=CARTESIAN_POINT('',(-0.0125,-0.0332787743898722,-0.0136758532865583));
#46089=CARTESIAN_POINT('Ctrl Pts',(-0.0124999999999998,-0.0395287743898722,
-0.0136758532865581));
#46090=CARTESIAN_POINT('Ctrl Pts',(-0.0124397722908538,-0.0395316720968796,
-0.0136758532865581));
#46091=CARTESIAN_POINT('Ctrl Pts',(-0.0123794869155727,-0.0395346733294052,
-0.0136722262485745));
#46092=CARTESIAN_POINT('Ctrl Pts',(-0.0121219968180532,-0.0395479289769376,
-0.0136410088687577));
#46093=CARTESIAN_POINT('Ctrl Pts',(-0.0119312721431936,-0.0395588546503147,
-0.0135780294542973));
#46094=CARTESIAN_POINT('Ctrl Pts',(-0.0115903954706135,-0.039580640649201,
-0.0133841492104154));
#46095=CARTESIAN_POINT('Ctrl Pts',(-0.0114424103773941,-0.0395912925013576,
-0.0132570002329958));
#46096=CARTESIAN_POINT('Ctrl Pts',(-0.0112026418538901,-0.0396112656029744,
-0.0129532598395549));
#46097=CARTESIAN_POINT('Ctrl Pts',(-0.0111132317672345,-0.03962023901688,
-0.0127794900004168));
#46098=CARTESIAN_POINT('Ctrl Pts',(-0.0110040333182525,-0.0396411664246257,
-0.0124027966609954));
#46099=CARTESIAN_POINT('Ctrl Pts',(-0.0109871636068316,-0.0396522650049775,
-0.0122030222146618));
#46100=CARTESIAN_POINT('Ctrl Pts',(-0.0110313371454244,-0.0396737694912329,
-0.0118159414620639));
#46101=CARTESIAN_POINT('Ctrl Pts',(-0.0110890781104405,-0.0396839911712235,
-0.0116319512222338));
#46102=CARTESIAN_POINT('Ctrl Pts',(-0.0112741873004969,-0.0397030562170287,
-0.011288780397739));
#46103=CARTESIAN_POINT('Ctrl Pts',(-0.0114024250252582,-0.0397132333722956,
-0.0111342742979425));
#46104=CARTESIAN_POINT('Ctrl Pts',(-0.0117096250808491,-0.03973491050597,
-0.0108859835900327));
#46105=CARTESIAN_POINT('Ctrl Pts',(-0.0118848478870789,-0.039745901334608,
-0.0107938085621011));
#46106=CARTESIAN_POINT('Ctrl Pts',(-0.0122549601010164,-0.0397667625550083,
-0.0106838577867322));
#46107=CARTESIAN_POINT('Ctrl Pts',(-0.0124456633148463,-0.0397758544896276,
-0.0106648507771582));
#46108=CARTESIAN_POINT('Ctrl Pts',(-0.0128329329067826,-0.0397954579958913,
-0.0106998063931913));
#46109=CARTESIAN_POINT('Ctrl Pts',(-0.0130254735586308,-0.0398063076685071,
-0.0107569044158373));
#46110=CARTESIAN_POINT('Ctrl Pts',(-0.0133726179144054,-0.0398281093002484,
-0.0109404914967616));
#46111=CARTESIAN_POINT('Ctrl Pts',(-0.0135248186503528,-0.0398388488330703,
-0.0110634952707375));
#46112=CARTESIAN_POINT('Ctrl Pts',(-0.0137730290862697,-0.0398590134280308,
-0.0113595076033407));
#46113=CARTESIAN_POINT('Ctrl Pts',(-0.0138671274858221,-0.0398678566542454,
-0.0115293340452784));
#46114=CARTESIAN_POINT('Ctrl Pts',(-0.0139881351226471,-0.0398885471754151,
-0.0119017634263324));
#46115=CARTESIAN_POINT('Ctrl Pts',(-0.0140113373792064,-0.0398996466565376,
-0.012101554086537));
#46116=CARTESIAN_POINT('Ctrl Pts',(-0.0139789887328644,-0.0399212823937301,
-0.0124909973560022));
#46117=CARTESIAN_POINT('Ctrl Pts',(-0.0139266718072984,-0.0399316271824345,
-0.0126772035526814));
#46118=CARTESIAN_POINT('Ctrl Pts',(-0.0137516058177497,-0.0399510116243861,
-0.0130261235078094));
#46119=CARTESIAN_POINT('Ctrl Pts',(-0.013628096636719,-0.0399608436849657,
-0.0131842686005688));
#46120=CARTESIAN_POINT('Ctrl Pts',(-0.0133281201988757,-0.0399824329953701,
-0.013441909343706));
#46121=CARTESIAN_POINT('Ctrl Pts',(-0.0131551638916299,-0.0399934642923688,
-0.0135394669240204));
#46122=CARTESIAN_POINT('Ctrl Pts',(-0.0128169677388121,-0.0400128231181185,
-0.013650611731408));
#46123=CARTESIAN_POINT('Ctrl Pts',(-0.0126588938146744,-0.0400211296076493,
-0.0136758532865581));
#46124=CARTESIAN_POINT('Ctrl Pts',(-0.0124999999999999,-0.0400287743898722,
-0.0136758532865581));
#46125=CARTESIAN_POINT('Ctrl Pts',(-0.0124999999999998,-0.0400912743898722,
-0.0136758532865581));
#46126=CARTESIAN_POINT('Ctrl Pts',(-0.012643270042393,-0.0400843813067437,
-0.0136758532865581));
#46127=CARTESIAN_POINT('Ctrl Pts',(-0.0127860199934178,-0.0400769432292705,
-0.013655332665471));
#46128=CARTESIAN_POINT('Ctrl Pts',(-0.0131119931383006,-0.0400585920843435,
-0.0135592934969406));
#46129=CARTESIAN_POINT('Ctrl Pts',(-0.0132873867431685,-0.0400476048159138,
-0.0134675424684249));
#46130=CARTESIAN_POINT('Ctrl Pts',(-0.0135967024168737,-0.0400258116011465,
-0.0132187371992349));
#46131=CARTESIAN_POINT('Ctrl Pts',(-0.0137263197857993,-0.0400155425052295,
-0.0130626793629855));
#46132=CARTESIAN_POINT('Ctrl Pts',(-0.0139118317301532,-0.0399963603319162,
-0.0127174002433472));
#46133=CARTESIAN_POINT('Ctrl Pts',(-0.0139692730889719,-0.0399861315727515,
-0.0125332825783836));
#46134=CARTESIAN_POINT('Ctrl Pts',(-0.0140127915577626,-0.0399646192699105,
-0.0121460611272465));
#46135=CARTESIAN_POINT('Ctrl Pts',(-0.0139955701085837,-0.0399535203560068,
-0.011946280676979));
#46136=CARTESIAN_POINT('Ctrl Pts',(-0.0138857124295479,-0.0399326059177996,
-0.0115698207892499));
#46137=CARTESIAN_POINT('Ctrl Pts',(-0.0137960414682695,-0.0399236418495419,
-0.0113962721629051));
#46138=CARTESIAN_POINT('Ctrl Pts',(-0.0135558045660159,-0.0399036580386168,
-0.0110929574901586));
#46139=CARTESIAN_POINT('Ctrl Pts',(-0.0134075838011624,-0.0398930011048476,
-0.0109660337699312));
#46140=CARTESIAN_POINT('Ctrl Pts',(-0.0130663529960187,-0.0398712137032887,
-0.0107727164054306));
#46141=CARTESIAN_POINT('Ctrl Pts',(-0.0128755232127017,-0.0398602919526901,
-0.0107100602641833));
#46142=CARTESIAN_POINT('Ctrl Pts',(-0.0124891318972407,-0.0398404188604484,
-0.0106638783334612));
#46143=CARTESIAN_POINT('Ctrl Pts',(-0.0122976941481818,-0.039831497093174,
-0.0106774319536756));
#46144=CARTESIAN_POINT('Ctrl Pts',(-0.0119248928036891,-0.0398108018848791,
-0.0107767485825008));
#46145=CARTESIAN_POINT('Ctrl Pts',(-0.0117475906205829,-0.0397998600318385,
-0.0108635589025283));
#46146=CARTESIAN_POINT('Ctrl Pts',(-0.0114337693742506,-0.0397781312888341,
-0.0111022393075453));
#46147=CARTESIAN_POINT('Ctrl Pts',(-0.011301035805563,-0.0397675625902032,
-0.0112528111734217));
#46148=CARTESIAN_POINT('Ctrl Pts',(-0.0111061596572095,-0.0397488264073279,
-0.0115897783668008));
#46149=CARTESIAN_POINT('Ctrl Pts',(-0.0110430381314342,-0.0397387448591258,
-0.0117713848399931));
#46150=CARTESIAN_POINT('Ctrl Pts',(-0.0109871330632712,-0.0397173852783954,
-0.0121558572931412));
#46151=CARTESIAN_POINT('Ctrl Pts',(-0.0109976930687457,-0.039706298373389,
-0.0123554215832577));
#46152=CARTESIAN_POINT('Ctrl Pts',(-0.0110949915117192,-0.0396851421175358,
-0.0127362341886165));
#46153=CARTESIAN_POINT('Ctrl Pts',(-0.0111797045151038,-0.0396759592379689,
-0.0129140176159246));
#46154=CARTESIAN_POINT('Ctrl Pts',(-0.0114110754907633,-0.0396561797995405,
-0.0132253311141067));
#46155=CARTESIAN_POINT('Ctrl Pts',(-0.0115548035822409,-0.0396456232140526,
-0.0133564238347563));
#46156=CARTESIAN_POINT('Ctrl Pts',(-0.0118904751661538,-0.0396237905618976,
-0.0135609990743401));
#46157=CARTESIAN_POINT('Ctrl Pts',(-0.0120807658386286,-0.0396127197921006,
-0.0136299536740986));
#46158=CARTESIAN_POINT('Ctrl Pts',(-0.0123523154948988,-0.0395985312031165,
-0.0136704050760884));
#46159=CARTESIAN_POINT('Ctrl Pts',(-0.0124261829920253,-0.0395948259123243,
-0.0136758532865581));
#46160=CARTESIAN_POINT('Ctrl Pts',(-0.0124999999999999,-0.0395912743898722,
-0.0136758532865581));
#46161=CARTESIAN_POINT('Origin',(-0.0125,-0.0332787743898722,-0.0121758532865583));
#46162=CARTESIAN_POINT('',(-0.0125,-0.0390287743898722,-0.0136758532865581));
#46163=CARTESIAN_POINT('',(-0.0125,-0.0390912743898722,-0.0136758532865581));
#46164=CARTESIAN_POINT('',(-0.0125,-0.0332787743898722,-0.0136758532865583));
#46165=CARTESIAN_POINT('Ctrl Pts',(-0.0125,-0.0390287743898722,-0.0136758532865581));
#46166=CARTESIAN_POINT('Ctrl Pts',(-0.0124102850117373,-0.0390330908042575,
-0.0136758532865581));
#46167=CARTESIAN_POINT('Ctrl Pts',(-0.012320558270234,-0.0390376313209618,
-0.0136678059602836));
#46168=CARTESIAN_POINT('Ctrl Pts',(-0.01203533333192,-0.0390527935499012,
-0.0136159898032078));
#46169=CARTESIAN_POINT('Ctrl Pts',(-0.0118478964733522,-0.0390638841748649,
-0.0135413774667673));
#46170=CARTESIAN_POINT('Ctrl Pts',(-0.0115196390269793,-0.0390856242050675,
-0.0133272949545545));
#46171=CARTESIAN_POINT('Ctrl Pts',(-0.0113803234820742,-0.0390960754472454,
-0.0131923518382069));
#46172=CARTESIAN_POINT('Ctrl Pts',(-0.0111575496436965,-0.0391156534197134,
-0.0128734004360286));
#46173=CARTESIAN_POINT('Ctrl Pts',(-0.011077693887836,-0.0391251319252631,
-0.0126914176495188));
#46174=CARTESIAN_POINT('Ctrl Pts',(-0.0109927367071867,-0.0391465147559555,
-0.0123065266970562));
#46175=CARTESIAN_POINT('Ctrl Pts',(-0.0109886338190343,-0.0391575784775955,
-0.0121073797075351));
#46176=CARTESIAN_POINT('Ctrl Pts',(-0.0110564826923846,-0.0391787690060196,
-0.011725950195901));
#46177=CARTESIAN_POINT('Ctrl Pts',(-0.0111250641709478,-0.0391884289306804,
-0.0115468311043905));
#46178=CARTESIAN_POINT('Ctrl Pts',(-0.0113300146585407,-0.0392074699993104,
-0.0112163372912574));
#46179=CARTESIAN_POINT('Ctrl Pts',(-0.0114673500864563,-0.0392181454215954,
-0.0110698940278283));
#46180=CARTESIAN_POINT('Ctrl Pts',(-0.0117879424564227,-0.0392399192452917,
-0.0108413186480632));
#46181=CARTESIAN_POINT('Ctrl Pts',(-0.0119672464793475,-0.0392508004521428,
-0.0107601588791299));
#46182=CARTESIAN_POINT('Ctrl Pts',(-0.0123427675174401,-0.0392713174229338,
-0.0106719694479415));
#46183=CARTESIAN_POINT('Ctrl Pts',(-0.0125350535616568,-0.0392801366451525,
-0.0106641799268804));
#46184=CARTESIAN_POINT('Ctrl Pts',(-0.0129218058778295,-0.0393003643275987,
-0.0107225018333852));
#46185=CARTESIAN_POINT('Ctrl Pts',(-0.0131119400693353,-0.0393114365019678,
-0.010791778030731));
#46186=CARTESIAN_POINT('Ctrl Pts',(-0.0134472009486803,-0.0393332644596337,
-0.0109968956298863));
#46187=CARTESIAN_POINT('Ctrl Pts',(-0.0135906831652189,-0.0393438153472172,
-0.0111282090938635));
#46188=CARTESIAN_POINT('Ctrl Pts',(-0.0138215724648837,-0.0393635835830235,
-0.0114399535849478));
#46189=CARTESIAN_POINT('Ctrl Pts',(-0.0139060147553127,-0.0393727808693334,
-0.0116179699168607));
#46190=CARTESIAN_POINT('Ctrl Pts',(-0.0140026259839428,-0.0393939500327153,
-0.0119990148577352));
#46191=CARTESIAN_POINT('Ctrl Pts',(-0.0140128240180074,-0.0394050359398672,
-0.0121985611864688));
#46192=CARTESIAN_POINT('Ctrl Pts',(-0.013956248745159,-0.0394263862253205,
-0.0125828663246282));
#46193=CARTESIAN_POINT('Ctrl Pts',(-0.0138928231002549,-0.0394364421224273,
-0.0127643320341397));
#46194=CARTESIAN_POINT('Ctrl Pts',(-0.0136973858617855,-0.0394551953887276,
-0.0131009423942271));
#46195=CARTESIAN_POINT('Ctrl Pts',(-0.0135643935655737,-0.0394657702792724,
-0.0132512890397871));
#46196=CARTESIAN_POINT('Ctrl Pts',(-0.0132501881407943,-0.0394875020742744,
-0.0134894139001271));
#46197=CARTESIAN_POINT('Ctrl Pts',(-0.0130727702861836,-0.0394984408148763,
-0.0135759118234382));
#46198=CARTESIAN_POINT('Ctrl Pts',(-0.0127582698832516,-0.0395158841726235,
-0.0136591420254606));
#46199=CARTESIAN_POINT('Ctrl Pts',(-0.0126292903182273,-0.0395225539065362,
-0.0136758532865581));
#46200=CARTESIAN_POINT('Ctrl Pts',(-0.0124999999999998,-0.0395287743898722,
-0.0136758532865581));
#46201=CARTESIAN_POINT('Ctrl Pts',(-0.0124999999999999,-0.0395912743898722,
-0.0136758532865581));
#46202=CARTESIAN_POINT('Ctrl Pts',(-0.012616080968727,-0.0395856894416603,
-0.0136758532865581));
#46203=CARTESIAN_POINT('Ctrl Pts',(-0.0127320006990499,-0.0395797380488127,
-0.0136623820065603));
#46204=CARTESIAN_POINT('Ctrl Pts',(-0.0130352221126667,-0.0395631559363599,
-0.0135906208525869));
#46205=CARTESIAN_POINT('Ctrl Pts',(-0.0132144148882381,-0.0395522709514737,
-0.0135091323883231));
#46206=CARTESIAN_POINT('Ctrl Pts',(-0.0135346236164816,-0.0395304991674054,
-0.0132799659482055));
#46207=CARTESIAN_POINT('Ctrl Pts',(-0.0136716958454091,-0.0395198296493871,
-0.0131332793643585));
#46208=CARTESIAN_POINT('Ctrl Pts',(-0.0138760644607809,-0.0395008060819552,
-0.0128024077621056));
#46209=CARTESIAN_POINT('Ctrl Pts',(-0.0139443304909923,-0.0394911240563624,
-0.0126231472833809));
#46210=CARTESIAN_POINT('Ctrl Pts',(-0.0140114946017313,-0.0394699236436718,
-0.0122415398549506));
#46211=CARTESIAN_POINT('Ctrl Pts',(-0.0140070212567482,-0.0394588582824967,
-0.0120423633537985));
#46212=CARTESIAN_POINT('Ctrl Pts',(-0.013921351111115,-0.0394374882375592,
-0.0116577025449237));
#46213=CARTESIAN_POINT('Ctrl Pts',(-0.0138412148809848,-0.0394280288982809,
-0.0114759632715372));
#46214=CARTESIAN_POINT('Ctrl Pts',(-0.0136179473921991,-0.0394084392709806,
-0.0111574473229837));
#46215=CARTESIAN_POINT('Ctrl Pts',(-0.0134783771898,-0.0393979817752759,
-0.0110227201593938));
#46216=CARTESIAN_POINT('Ctrl Pts',(-0.0131496894052637,-0.0393762359278434,
-0.0108091735944673));
#46217=CARTESIAN_POINT('Ctrl Pts',(-0.0129620852800822,-0.0393651461472728,
-0.0107348813704491));
#46218=CARTESIAN_POINT('Ctrl Pts',(-0.0125770224262023,-0.0393446967179505,
-0.0106656503418758));
#46219=CARTESIAN_POINT('Ctrl Pts',(-0.0123838966512107,-0.0393359023193282,
-0.0106681509271087));
#46220=CARTESIAN_POINT('Ctrl Pts',(-0.0120059896027197,-0.039315550867305,
-0.0107462489914163));
#46221=CARTESIAN_POINT('Ctrl Pts',(-0.0118250255834797,-0.0393047328042361,
-0.0108222603862315));
#46222=CARTESIAN_POINT('Ctrl Pts',(-0.0114985868770511,-0.0392829362870622,
-0.0110415265794009));
#46223=CARTESIAN_POINT('Ctrl Pts',(-0.0113572005343832,-0.0392721732215874,
-0.011184108607497));
#46224=CARTESIAN_POINT('Ctrl Pts',(-0.0111431977622291,-0.0392528616647807,
-0.0115086609782096));
#46225=CARTESIAN_POINT('Ctrl Pts',(-0.0110697032319431,-0.0392435098340271,
-0.0116856152917699));
#46226=CARTESIAN_POINT('Ctrl Pts',(-0.0109912787660915,-0.0392224748475099,
-0.0120642450490785));
#46227=CARTESIAN_POINT('Ctrl Pts',(-0.0109896599278592,-0.0392114412748625,
-0.0122628493567319));
#46228=CARTESIAN_POINT('Ctrl Pts',(-0.0110635220924074,-0.0391898643579785,
-0.0126512338606453));
#46229=CARTESIAN_POINT('Ctrl Pts',(-0.0111390114930965,-0.039180055942407,
-0.0128370186377876));
#46230=CARTESIAN_POINT('Ctrl Pts',(-0.011354149385122,-0.0391606595848464,
-0.0131626577503477));
#46231=CARTESIAN_POINT('Ctrl Pts',(-0.011489508880533,-0.039150308105931,
-0.01330086146796));
#46232=CARTESIAN_POINT('Ctrl Pts',(-0.0118110442018891,-0.0391286655421054,
-0.0135230782526652));
#46233=CARTESIAN_POINT('Ctrl Pts',(-0.0119958440066602,-0.0391175663324443,
-0.0136025671493725));
#46234=CARTESIAN_POINT('Ctrl Pts',(-0.01229269653651,-0.03910154681736,
-0.0136651060283512));
#46235=CARTESIAN_POINT('Ctrl Pts',(-0.0123963195413974,-0.0390962627182625,
-0.0136758532865581));
#46236=CARTESIAN_POINT('Ctrl Pts',(-0.0125,-0.0390912743898722,-0.0136758532865581));
#46237=CARTESIAN_POINT('Origin',(-0.0125,-0.0332787743898722,-0.0121758532865583));
#46238=CARTESIAN_POINT('',(-0.0125,-0.0385287743898722,-0.0136758532865581));
#46239=CARTESIAN_POINT('',(-0.0125000000000001,-0.0385912743898721,-0.0136758532865581));
#46240=CARTESIAN_POINT('',(-0.0125,-0.0332787743898722,-0.0136758532865583));
#46241=CARTESIAN_POINT('Ctrl Pts',(-0.0125000000000001,-0.0385287743898722,
-0.0136758532865581));
#46242=CARTESIAN_POINT('Ctrl Pts',(-0.0123794141842183,-0.038534576077639,
-0.0136758532865581));
#46243=CARTESIAN_POINT('Ctrl Pts',(-0.0122590243636787,-0.0385407721431061,
-0.0136613162156284));
#46244=CARTESIAN_POINT('Ctrl Pts',(-0.0119486306014825,-0.0385578286507219,
-0.0135848997079368));
#46245=CARTESIAN_POINT('Ctrl Pts',(-0.0117671804892131,-0.0385689272417041,
-0.0134996312460684));
#46246=CARTESIAN_POINT('Ctrl Pts',(-0.0114540318222995,-0.0385904319664484,
-0.01326785055669));
#46247=CARTESIAN_POINT('Ctrl Pts',(-0.0113235541708813,-0.0386006538620198,
-0.0131258562376278));
#46248=CARTESIAN_POINT('Ctrl Pts',(-0.0111188968888253,-0.0386197194780385,
-0.012793970871615));
#46249=CARTESIAN_POINT('Ctrl Pts',(-0.0110492001005163,-0.0386298960133832,
-0.0126056640633596));
#46250=CARTESIAN_POINT('Ctrl Pts',(-0.0109877544422508,-0.0386515730342179,
-0.0122154776883335));
#46251=CARTESIAN_POINT('Ctrl Pts',(-0.0109955302872684,-0.0386625639380715,
-0.0120176414189686));
#46252=CARTESIAN_POINT('Ctrl Pts',(-0.0110853483635358,-0.0386834254352273,
-0.0116421344701649));
#46253=CARTESIAN_POINT('Ctrl Pts',(-0.0111642308846139,-0.0386925177159721,
-0.0114674735719249));
#46254=CARTESIAN_POINT('Ctrl Pts',(-0.0113881225163157,-0.038712120765372,
-0.0111495554750252));
#46255=CARTESIAN_POINT('Ctrl Pts',(-0.0115338344365946,-0.0387229703092475,
-0.0110113523446981));
#46256=CARTESIAN_POINT('Ctrl Pts',(-0.0118663882652761,-0.0387447719493325,
-0.0108024934291675));
#46257=CARTESIAN_POINT('Ctrl Pts',(-0.0120490105383213,-0.038755511613758,
-0.0107321765653561));
#46258=CARTESIAN_POINT('Ctrl Pts',(-0.0124294659781935,-0.0387756765080802,
-0.0106652085216324));
#46259=CARTESIAN_POINT('Ctrl Pts',(-0.0126235875562038,-0.0387845195932171,
-0.0106686206804526));
#46260=CARTESIAN_POINT('Ctrl Pts',(-0.0130066280278391,-0.0388052097357883,
-0.0107500202547862));
#46261=CARTESIAN_POINT('Ctrl Pts',(-0.0131912578178942,-0.038816309209822,
-0.0108298131430346));
#46262=CARTESIAN_POINT('Ctrl Pts',(-0.0135123635693991,-0.0388379451378713,
-0.0110525350766006));
#46263=CARTESIAN_POINT('Ctrl Pts',(-0.0136474716068829,-0.0388482901131671,
-0.0111909402018134));
#46264=CARTESIAN_POINT('Ctrl Pts',(-0.0138621260050081,-0.0388676748870375,
-0.0115169997375278));
#46265=CARTESIAN_POINT('Ctrl Pts',(-0.0139373370580137,-0.0388775062857149,
-0.0117030274117301));
#46266=CARTESIAN_POINT('Ctrl Pts',(-0.0140104925159708,-0.0388990952514589,
-0.0120916287951207));
#46267=CARTESIAN_POINT('Ctrl Pts',(-0.0140085120609981,-0.0389101266123352,
-0.0122901932908941));
#46268=CARTESIAN_POINT('Ctrl Pts',(-0.0139294190175121,-0.038931151586005,
-0.0126686428169504));
#46269=CARTESIAN_POINT('Ctrl Pts',(-0.0138556111572235,-0.0389404860779281,
-0.0128454614561909));
#46270=CARTESIAN_POINT('Ctrl Pts',(-0.0136410319840247,-0.0389598147421072,
-0.0131696313364146));
#46271=CARTESIAN_POINT('Ctrl Pts',(-0.0134993905740551,-0.0389705831167817,
-0.0133119627061757));
#46272=CARTESIAN_POINT('Ctrl Pts',(-0.0131725875188633,-0.0389923804997031,
-0.013530628995685));
#46273=CARTESIAN_POINT('Ctrl Pts',(-0.0129915223515988,-0.0390031942634895,
-0.0136063104228091));
#46274=CARTESIAN_POINT('Ctrl Pts',(-0.0127017552483669,-0.0390187847025531,
-0.0136656748839404));
#46275=CARTESIAN_POINT('Ctrl Pts',(-0.0126008988146715,-0.0390239198933879,
-0.0136758532865581));
#46276=CARTESIAN_POINT('Ctrl Pts',(-0.0125,-0.0390287743898722,-0.0136758532865581));
#46277=CARTESIAN_POINT('Ctrl Pts',(-0.0125,-0.0390912743898722,-0.0136758532865581));
#46278=CARTESIAN_POINT('Ctrl Pts',(-0.0125877964667036,-0.0390870502803984,
-0.0136758532865581));
#46279=CARTESIAN_POINT('Ctrl Pts',(-0.0126756132986267,-0.0390826111114244,
-0.0136681464181381));
#46280=CARTESIAN_POINT('Ctrl Pts',(-0.0129533820634803,-0.0390678757946181,
-0.0136187846265947));
#46281=CARTESIAN_POINT('Ctrl Pts',(-0.0131359171196588,-0.0390571315460259,
-0.0135481516687388));
#46282=CARTESIAN_POINT('Ctrl Pts',(-0.0134681410692972,-0.0390353296470555,
-0.0133387120660686));
#46283=CARTESIAN_POINT('Ctrl Pts',(-0.0136136171138924,-0.0390244846183957,
-0.0132002629348385));
#46284=CARTESIAN_POINT('Ctrl Pts',(-0.0138369629638526,-0.0390048975436701,
-0.0128819746045067));
#46285=CARTESIAN_POINT('Ctrl Pts',(-0.0139155473163728,-0.0389957930392524,
-0.0127071889753984));
#46286=CARTESIAN_POINT('Ctrl Pts',(-0.0140047407173374,-0.038974921874698,
-0.0123315080134204));
#46287=CARTESIAN_POINT('Ctrl Pts',(-0.0140121793945736,-0.0389639283573359,
-0.0121336247009018));
#46288=CARTESIAN_POINT('Ctrl Pts',(-0.0139497766392526,-0.0389421607788429,
-0.0117418082880286));
#46289=CARTESIAN_POINT('Ctrl Pts',(-0.0138788071942519,-0.0389319518037048,
-0.0115520760702422));
#46290=CARTESIAN_POINT('Ctrl Pts',(-0.0136714681141962,-0.0389127435133528,
-0.0112196994386224));
#46291=CARTESIAN_POINT('Ctrl Pts',(-0.0135401761026448,-0.0389024995235825,
-0.0110783202415268));
#46292=CARTESIAN_POINT('Ctrl Pts',(-0.013225621670663,-0.0388809705086359,
-0.0108480999613873));
#46293=CARTESIAN_POINT('Ctrl Pts',(-0.0130436057320444,-0.0388698709869924,
-0.0107637780356961));
#46294=CARTESIAN_POINT('Ctrl Pts',(-0.0126623790169372,-0.0388489847068865,
-0.0106721759916537));
#46295=CARTESIAN_POINT('Ctrl Pts',(-0.012467377748664,-0.038840040025568,
-0.0106637870047411));
#46296=CARTESIAN_POINT('Ctrl Pts',(-0.0120848733994664,-0.0388200330567339,
-0.0107215209158405));
#46297=CARTESIAN_POINT('Ctrl Pts',(-0.0119010131213935,-0.0388093652043643,
-0.0107871082580299));
#46298=CARTESIAN_POINT('Ctrl Pts',(-0.0115636563115328,-0.0387875749787294,
-0.0109872372459273));
#46299=CARTESIAN_POINT('Ctrl Pts',(-0.0114144740244839,-0.0387766618409924,
-0.0111217189037022));
#46300=CARTESIAN_POINT('Ctrl Pts',(-0.011182456665273,-0.0387568225883833,
-0.0114340661432391));
#46301=CARTESIAN_POINT('Ctrl Pts',(-0.0110991208743787,-0.0387478832409401,
-0.0116068939673372));
#46302=CARTESIAN_POINT('Ctrl Pts',(-0.0110000573294581,-0.0387271668939019,
-0.0119797882140237));
#46303=CARTESIAN_POINT('Ctrl Pts',(-0.0109872994414402,-0.0387162183877965,
-0.0121768613239213));
#46304=CARTESIAN_POINT('Ctrl Pts',(-0.0110385688249589,-0.0386944898572231,
-0.0125679748742433));
#46305=CARTESIAN_POINT('Ctrl Pts',(-0.0111033523870144,-0.0386839675002031,
-0.01275796594061));
#46306=CARTESIAN_POINT('Ctrl Pts',(-0.0112990288784539,-0.0386652033326514,
-0.0130945543474498));
#46307=CARTESIAN_POINT('Ctrl Pts',(-0.0114253717544253,-0.038655096449513,
-0.0132395698600731));
#46308=CARTESIAN_POINT('Ctrl Pts',(-0.0117313428234367,-0.0386337227421488,
-0.0134790658880104));
#46309=CARTESIAN_POINT('Ctrl Pts',(-0.0119098782540256,-0.0386226337802118,
-0.0135690360810097));
#46310=CARTESIAN_POINT('Ctrl Pts',(-0.0122310551597517,-0.0386047175243793,
-0.0136577265720446));
#46311=CARTESIAN_POINT('Ctrl Pts',(-0.0123653456229713,-0.0385977529516076,
-0.0136758532865581));
#46312=CARTESIAN_POINT('Ctrl Pts',(-0.0125000000000002,-0.0385912743898721,
-0.0136758532865581));
#46313=CARTESIAN_POINT('Origin',(-0.0125,-0.0332787743898722,-0.0121758532865583));
#46314=CARTESIAN_POINT('',(-0.0125000000000001,-0.0380287743898722,-0.0136758532865581));
#46315=CARTESIAN_POINT('',(-0.0125000000000001,-0.0380912743898722,-0.0136758532865581));
#46316=CARTESIAN_POINT('',(-0.0125,-0.0332787743898722,-0.0136758532865583));
#46317=CARTESIAN_POINT('Ctrl Pts',(-0.0125000000000002,-0.0380287743898722,
-0.0136758532865581));
#46318=CARTESIAN_POINT('Ctrl Pts',(-0.0123468034371259,-0.03803614506294,
-0.0136758532865582));
#46319=CARTESIAN_POINT('Ctrl Pts',(-0.0121942736987196,-0.0380441354069111,
-0.0136523901601837));
#46320=CARTESIAN_POINT('Ctrl Pts',(-0.0118596124296688,-0.0380631766785471,
-0.0135465547026092));
#46321=CARTESIAN_POINT('Ctrl Pts',(-0.0116850882356659,-0.0380742404504398,
-0.0134505436856338));
#46322=CARTESIAN_POINT('Ctrl Pts',(-0.0113886699720512,-0.0380954312788031,
-0.0132010853574274));
#46323=CARTESIAN_POINT('Ctrl Pts',(-0.0112678305352291,-0.0381050918695822,
-0.0130521386517754));
#46324=CARTESIAN_POINT('Ctrl Pts',(-0.0110840709912425,-0.0381241324077053,
-0.0127094089655602));
#46325=CARTESIAN_POINT('Ctrl Pts',(-0.0110259047331901,-0.0381348076514243,
-0.0125172545786196));
#46326=CARTESIAN_POINT('Ctrl Pts',(-0.0109882274892282,-0.0381565814142957,
-0.0121253268469331));
#46327=CARTESIAN_POINT('Ctrl Pts',(-0.0110075827607697,-0.0381674627362096,
-0.0119294630524846));
#46328=CARTESIAN_POINT('Ctrl Pts',(-0.0111189496812055,-0.0381879800246486,
-0.0115601518605821));
#46329=CARTESIAN_POINT('Ctrl Pts',(-0.0112083371616353,-0.0381967993584789,
-0.011389728754414));
#46330=CARTESIAN_POINT('Ctrl Pts',(-0.0114522049126026,-0.0382170266075629,
-0.0110839391223943));
#46331=CARTESIAN_POINT('Ctrl Pts',(-0.0116072608860987,-0.0382280987398141,
-0.0109539071854659));
#46332=CARTESIAN_POINT('Ctrl Pts',(-0.0119525203723629,-0.038249926840854,
-0.0107661025200344));
#46333=CARTESIAN_POINT('Ctrl Pts',(-0.0121379802140337,-0.0382604779017553,
-0.0107074901961218));
#46334=CARTESIAN_POINT('Ctrl Pts',(-0.0125233994980509,-0.0382802464777539,
-0.010663387242309));
#46335=CARTESIAN_POINT('Ctrl Pts',(-0.0127197852926541,-0.0382894433229697,
-0.0106792555844373));
#46336=CARTESIAN_POINT('Ctrl Pts',(-0.0130980898374368,-0.0383106120949194,
-0.0107860886823309));
#46337=CARTESIAN_POINT('Ctrl Pts',(-0.0132760070182737,-0.0383216980328853,
-0.010877020852352));
#46338=CARTESIAN_POINT('Ctrl Pts',(-0.0135805519682038,-0.0383430486008001,
-0.0111181539708168));
#46339=CARTESIAN_POINT('Ctrl Pts',(-0.0137060013753424,-0.0383531052730338,
-0.011263809183469));
#46340=CARTESIAN_POINT('Ctrl Pts',(-0.013899813786559,-0.0383718580207817,
-0.01160135864293));
#46341=CARTESIAN_POINT('Ctrl Pts',(-0.013963531508504,-0.0383824327237375,
-0.011791703296134));
#46342=CARTESIAN_POINT('Ctrl Pts',(-0.014012671420935,-0.0384041644269998,
-0.0121828739548556));
#46343=CARTESIAN_POINT('Ctrl Pts',(-0.0139988818636063,-0.0384151032625681,
-0.0123797729950841));
#46344=CARTESIAN_POINT('Ctrl Pts',(-0.0138978995332542,-0.0384357890048659,
-0.0127521163564446));
#46345=CARTESIAN_POINT('Ctrl Pts',(-0.0138136297020046,-0.0384447032789115,
-0.0129245666781789));
#46346=CARTESIAN_POINT('Ctrl Pts',(-0.0135799148579252,-0.0384645914793258,
-0.0132357359086626));
#46347=CARTESIAN_POINT('Ctrl Pts',(-0.0134300176507454,-0.0384755170339867,
-0.0133694262977071));
#46348=CARTESIAN_POINT('Ctrl Pts',(-0.0130916835139492,-0.0384973030764192,
-0.0135677119104125));
#46349=CARTESIAN_POINT('Ctrl Pts',(-0.012907579061836,-0.0385079550833858,
-0.0136323058962518));
#46350=CARTESIAN_POINT('Ctrl Pts',(-0.0126444967607305,-0.038521677422535,
-0.013670638193534));
#46351=CARTESIAN_POINT('Ctrl Pts',(-0.0125722202694161,-0.0385252996905398,
-0.0136758532865581));
#46352=CARTESIAN_POINT('Ctrl Pts',(-0.0125000000000001,-0.0385287743898722,
-0.0136758532865581));
#46353=CARTESIAN_POINT('Ctrl Pts',(-0.0125000000000002,-0.0385912743898721,
-0.0136758532865581));
#46354=CARTESIAN_POINT('Ctrl Pts',(-0.0125594873863622,-0.0385884123016614,
-0.0136758532865581));
#46355=CARTESIAN_POINT('Ctrl Pts',(-0.0126190362728254,-0.0385854489647548,
-0.0136723148548114));
#46356=CARTESIAN_POINT('Ctrl Pts',(-0.0128698073234571,-0.03857254964562,
-0.013642287566719));
#46357=CARTESIAN_POINT('Ctrl Pts',(-0.0130550497567754,-0.0385619806919748,
-0.0135826545417134));
#46358=CARTESIAN_POINT('Ctrl Pts',(-0.013399470622655,-0.0385401379867543,
-0.0133928715926655));
#46359=CARTESIAN_POINT('Ctrl Pts',(-0.0135538922728016,-0.0385290704095098,
-0.0132619049557047));
#46360=CARTESIAN_POINT('Ctrl Pts',(-0.0137960248429441,-0.0385088883780659,
-0.0129547377373805));
#46361=CARTESIAN_POINT('Ctrl Pts',(-0.0138844117973256,-0.0385000560761349,
-0.0127839236392865));
#46362=CARTESIAN_POINT('Ctrl Pts',(-0.0139937657294113,-0.0384795057647236,
-0.0124140180338837));
#46363=CARTESIAN_POINT('Ctrl Pts',(-0.0140120447189885,-0.0384686126132817,
-0.0122179413079291));
#46364=CARTESIAN_POINT('Ctrl Pts',(-0.0139721430713558,-0.0384468455456825,
-0.0118261340911449));
#46365=CARTESIAN_POINT('Ctrl Pts',(-0.0139128954156917,-0.0384361890881392,
-0.0116343178553643));
#46366=CARTESIAN_POINT('Ctrl Pts',(-0.0137271825090755,-0.0384172039469478,
-0.0112925853139198));
#46367=CARTESIAN_POINT('Ctrl Pts',(-0.0136054562112809,-0.0384074724867839,
-0.0111442784519007));
#46368=CARTESIAN_POINT('Ctrl Pts',(-0.0133074675371577,-0.0383862504485875,
-0.010896416600494));
#46369=CARTESIAN_POINT('Ctrl Pts',(-0.0131322781585097,-0.0383751816197932,
-0.0108013756686641));
#46370=CARTESIAN_POINT('Ctrl Pts',(-0.0127559744500297,-0.0383538397431168,
-0.0106848452504786));
#46371=CARTESIAN_POINT('Ctrl Pts',(-0.0125586701070593,-0.0383444215515382,
-0.0106641750728909));
#46372=CARTESIAN_POINT('Ctrl Pts',(-0.0121714806461621,-0.03832480637397,
-0.0106996896469178));
#46373=CARTESIAN_POINT('Ctrl Pts',(-0.0119851516068347,-0.0383143352349756,
-0.0107539192876731));
#46374=CARTESIAN_POINT('Ctrl Pts',(-0.0116364222186638,-0.0382925768265017,
-0.0109332049743318));
#46375=CARTESIAN_POINT('Ctrl Pts',(-0.0114787086991418,-0.0382814890247829,
-0.0110591980073559));
#46376=CARTESIAN_POINT('Ctrl Pts',(-0.0112274347351725,-0.0382610706184389,
-0.0113590413635251));
#46377=CARTESIAN_POINT('Ctrl Pts',(-0.011133746819209,-0.038252276689046,
-0.0115278119014317));
#46378=CARTESIAN_POINT('Ctrl Pts',(-0.0110138243780798,-0.0382319017134448,
-0.0118945614622528));
#46379=CARTESIAN_POINT('Ctrl Pts',(-0.0109899111987811,-0.038221074298395,
-0.01208945493315));
#46380=CARTESIAN_POINT('Ctrl Pts',(-0.0110181266666995,-0.0381992799340672,
-0.0124817534910504));
#46381=CARTESIAN_POINT('Ctrl Pts',(-0.0110716710870686,-0.0381885286786585,
-0.0126752760884084));
#46382=CARTESIAN_POINT('Ctrl Pts',(-0.0112471031745442,-0.0381692548532336,
-0.0130222049460577));
#46383=CARTESIAN_POINT('Ctrl Pts',(-0.0113642073769202,-0.0381598638672979,
-0.0131738826292774));
#46384=CARTESIAN_POINT('Ctrl Pts',(-0.0116539785569142,-0.0381388068708262,
-0.0134300360959381));
#46385=CARTESIAN_POINT('Ctrl Pts',(-0.0118256383976094,-0.0381277685483548,
-0.013530092139203));
#46386=CARTESIAN_POINT('Ctrl Pts',(-0.0121690566623018,-0.0381079616211234,
-0.0136483236368381));
#46387=CARTESIAN_POINT('Ctrl Pts',(-0.0123340617498559,-0.0380992580976547,
-0.0136758532865582));
#46388=CARTESIAN_POINT('Ctrl Pts',(-0.0125000000000002,-0.0380912743898722,
-0.0136758532865581));
#46389=CARTESIAN_POINT('Origin',(-0.0125,-0.0332787743898722,-0.0121758532865583));
#46390=CARTESIAN_POINT('',(-0.0125,-0.0375287743898722,-0.0136758532865582));
#46391=CARTESIAN_POINT('',(-0.0124999999604478,-0.0375912743936781,-0.0136758532865582));
#46392=CARTESIAN_POINT('',(-0.0125,-0.0332787743898722,-0.0136758532865583));
#46393=CARTESIAN_POINT('Ctrl Pts',(-0.0125,-0.0375287743898722,-0.0136758532865582));
#46394=CARTESIAN_POINT('Ctrl Pts',(-0.0123159669085782,-0.0375376286861116,
-0.0136758532865582));
#46395=CARTESIAN_POINT('Ctrl Pts',(-0.012133343711675,-0.0375473558415515,
-0.0136419883463988));
#46396=CARTESIAN_POINT('Ctrl Pts',(-0.0117782621206025,-0.0375682353262687,
-0.0135053462531493));
#46397=CARTESIAN_POINT('Ctrl Pts',(-0.0116108124726789,-0.0375792263096031,
-0.013399702151021));
#46398=CARTESIAN_POINT('Ctrl Pts',(-0.011330508950688,-0.0376000880992964,
-0.0131341776636912));
#46399=CARTESIAN_POINT('Ctrl Pts',(-0.011218681662231,-0.0376091807461351,
-0.0129785388738239));
#46400=CARTESIAN_POINT('Ctrl Pts',(-0.0110552843729969,-0.037628783312591,
-0.012625692677619));
#46401=CARTESIAN_POINT('Ctrl Pts',(-0.0110084428972583,-0.0376396327203533,
-0.0124304033378973));
#46402=CARTESIAN_POINT('Ctrl Pts',(-0.0109938224843649,-0.0376614343692014,
-0.0120379736586325));
#46403=CARTESIAN_POINT('Ctrl Pts',(-0.011024227833506,-0.037672174172713,
-0.0118446571954231));
#46404=CARTESIAN_POINT('Ctrl Pts',(-0.0111564412509518,-0.0376923393834609,
-0.0114816834019601));
#46405=CARTESIAN_POINT('Ctrl Pts',(-0.0112564475347326,-0.0377011823196947,
-0.0113152717612241));
#46406=CARTESIAN_POINT('Ctrl Pts',(-0.0115184458539515,-0.0377218720620583,
-0.0110242354365176));
#46407=CARTESIAN_POINT('Ctrl Pts',(-0.0116798580306075,-0.0377329715285701,
-0.0109042287330237));
#46408=CARTESIAN_POINT('Ctrl Pts',(-0.0120332870355569,-0.037754607658306,
-0.0107374850559715));
#46409=CARTESIAN_POINT('Ctrl Pts',(-0.0122207019429658,-0.0377649528308088,
-0.0106896709875991));
#46410=CARTESIAN_POINT('Ctrl Pts',(-0.01261040128369,-0.0377843379555074,
-0.0106667855562598));
#46411=CARTESIAN_POINT('Ctrl Pts',(-0.0128091093455027,-0.0377941686547767,
-0.010694653731616));
#46412=CARTESIAN_POINT('Ctrl Pts',(-0.0131822307660401,-0.0378157572561895,
-0.0108255781247143));
#46413=CARTESIAN_POINT('Ctrl Pts',(-0.0133532089612384,-0.0378267886845521,
-0.0109265666246989));
#46414=CARTESIAN_POINT('Ctrl Pts',(-0.0136414241920234,-0.0378478139616304,
-0.0111842731762835));
#46415=CARTESIAN_POINT('Ctrl Pts',(-0.0137576579952084,-0.0378571489746186,
-0.0113365958119946));
#46416=CARTESIAN_POINT('Ctrl Pts',(-0.013931126525451,-0.0378764771209369,
-0.0116845024457244));
#46417=CARTESIAN_POINT('Ctrl Pts',(-0.0139835788430444,-0.0378872453353139,
-0.0118783303045099));
#46418=CARTESIAN_POINT('Ctrl Pts',(-0.0140095691307863,-0.0379090426930424,
-0.0122706827436235));
#46419=CARTESIAN_POINT('Ctrl Pts',(-0.0139845887701048,-0.0379198565875163,
-0.0124653328441524));
#46420=CARTESIAN_POINT('Ctrl Pts',(-0.0138626551541139,-0.037940197651112,
-0.012831471988875));
#46421=CARTESIAN_POINT('Ctrl Pts',(-0.0137679446581723,-0.0379489926709229,
-0.0129998559735247));
#46422=CARTESIAN_POINT('Ctrl Pts',(-0.0135149225571613,-0.0379694557490269,
-0.0132982796508804));
#46423=CARTESIAN_POINT('Ctrl Pts',(-0.013356593807172,-0.0379805463489167,
-0.0134233078076331));
#46424=CARTESIAN_POINT('Ctrl Pts',(-0.0130070717177654,-0.0380022865563384,
-0.0136005652575964));
#46425=CARTESIAN_POINT('Ctrl Pts',(-0.0128205515789315,-0.0380127379884413,
-0.0136537544562052));
#46426=CARTESIAN_POINT('Ctrl Pts',(-0.0125860660101643,-0.0380245821562937,
-0.0136740035801463));
#46427=CARTESIAN_POINT('Ctrl Pts',(-0.0125430091945582,-0.0380267051090342,
-0.0136758532865581));
#46428=CARTESIAN_POINT('Ctrl Pts',(-0.0125000000000002,-0.0380287743898722,
-0.0136758532865581));
#46429=CARTESIAN_POINT('Ctrl Pts',(-0.0125000000000002,-0.0380912743898722,
-0.0136758532865581));
#46430=CARTESIAN_POINT('Ctrl Pts',(-0.0125318766297121,-0.0380897407248101,
-0.0136758532865581));
#46431=CARTESIAN_POINT('Ctrl Pts',(-0.0125637850048779,-0.0380881773075196,
-0.0136748371910692));
#46432=CARTESIAN_POINT('Ctrl Pts',(-0.0127870750712986,-0.0380770378262157,
-0.0136605656039966));
#46433=CARTESIAN_POINT('Ctrl Pts',(-0.0129743333509333,-0.0380666720839346,
-0.0136117397363397));
#46434=CARTESIAN_POINT('Ctrl Pts',(-0.0133270509590668,-0.0380450150808707,
-0.0134430124440513));
#46435=CARTESIAN_POINT('Ctrl Pts',(-0.0134878948346635,-0.0380339165703657,
-0.0133220558304902));
#46436=CARTESIAN_POINT('Ctrl Pts',(-0.0137482102722622,-0.0380132689682407,
-0.0130296217179064));
#46437=CARTESIAN_POINT('Ctrl Pts',(-0.0138472176633938,-0.0380044404119239,
-0.0128628416834866));
#46438=CARTESIAN_POINT('Ctrl Pts',(-0.0139775095350967,-0.0379842420100572,
-0.0124992704498853));
#46439=CARTESIAN_POINT('Ctrl Pts',(-0.0140069048435702,-0.0379734877277754,
-0.0123056933688139));
#46440=CARTESIAN_POINT('Ctrl Pts',(-0.0139901601365045,-0.0379516854820057,
-0.0119132529449597));
#46441=CARTESIAN_POINT('Ctrl Pts',(-0.0139422664741222,-0.0379408505493004,
-0.0117182241562649));
#46442=CARTESIAN_POINT('Ctrl Pts',(-0.0137769821896819,-0.037921298859816,
-0.0113662937455464));
#46443=CARTESIAN_POINT('Ctrl Pts',(-0.0136643363738046,-0.0379121664429356,
-0.0112112774403091));
#46444=CARTESIAN_POINT('Ctrl Pts',(-0.0133825592776287,-0.0378912739307356,
-0.0109471992480974));
#46445=CARTESIAN_POINT('Ctrl Pts',(-0.0132144446938143,-0.0378802747382287,
-0.0108424113185088));
#46446=CARTESIAN_POINT('Ctrl Pts',(-0.0128435550131623,-0.0378585312368616,
-0.0107020450401858));
#46447=CARTESIAN_POINT('Ctrl Pts',(-0.0126439075086321,-0.0378483773262782,
-0.0106694026924819));
#46448=CARTESIAN_POINT('Ctrl Pts',(-0.0122526357967572,-0.0378291446963842,
-0.0106840748841354));
#46449=CARTESIAN_POINT('Ctrl Pts',(-0.0120646357701901,-0.0378188865762998,
-0.0107277416093345));
#46450=CARTESIAN_POINT('Ctrl Pts',(-0.0117084066167368,-0.0377973421874111,
-0.0108863326164094));
#46451=CARTESIAN_POINT('Ctrl Pts',(-0.011544723362927,-0.0377862422388562,
-0.0110024230524411));
#46452=CARTESIAN_POINT('Ctrl Pts',(-0.0112758587586708,-0.0377653823997635,
-0.0112876901048509));
#46453=CARTESIAN_POINT('Ctrl Pts',(-0.0111717434886811,-0.0377564548055052,
-0.0114526058051654));
#46454=CARTESIAN_POINT('Ctrl Pts',(-0.0110317145148108,-0.0377364262054051,
-0.0118131206069678));
#46455=CARTESIAN_POINT('Ctrl Pts',(-0.0109972217211189,-0.037725748241553,
-0.0120053239563055));
#46456=CARTESIAN_POINT('Ctrl Pts',(-0.011003210473034,-0.0377039556384248,
-0.012397590812612));
#46457=CARTESIAN_POINT('Ctrl Pts',(-0.0110457582473621,-0.0376930507076776,
-0.0125938795660615));
#46458=CARTESIAN_POINT('Ctrl Pts',(-0.0112014588956732,-0.037673243245692,
-0.0129504138818026));
#46459=CARTESIAN_POINT('Ctrl Pts',(-0.01130997920573,-0.0376642863833723,
-0.0131085979982951));
#46460=CARTESIAN_POINT('Ctrl Pts',(-0.0115843144457518,-0.0376435502570075,
-0.0133799359734051));
#46461=CARTESIAN_POINT('Ctrl Pts',(-0.0117490362736719,-0.0376325956333979,
-0.0134889958482765));
#46462=CARTESIAN_POINT('Ctrl Pts',(-0.0121109673025152,-0.0376110523351543,
-0.0136376716542548));
#46463=CARTESIAN_POINT('Ctrl Pts',(-0.0123045998806578,-0.0376006755826408,
-0.0136758532813938));
#46464=CARTESIAN_POINT('Ctrl Pts',(-0.0124999999603558,-0.0375912743917796,
-0.0136758532865582));
#46465=CARTESIAN_POINT('Origin',(-0.0125,-0.0332787743898722,-0.0121758532865583));
#46466=CARTESIAN_POINT('',(-0.0125,-0.0370287743898722,-0.0136758532865582));
#46467=CARTESIAN_POINT('',(-0.0124999999999999,-0.0370912743898722,-0.0136758532865582));
#46468=CARTESIAN_POINT('',(-0.0125,-0.0332787743898722,-0.0136758532865583));
#46469=CARTESIAN_POINT('Ctrl Pts',(-0.0124999999999999,-0.0370287743898722,
-0.0136758532865582));
#46470=CARTESIAN_POINT('Ctrl Pts',(-0.0124805219657667,-0.0370297115272312,
-0.0136758532865582));
#46471=CARTESIAN_POINT('Ctrl Pts',(-0.0124610298195439,-0.0370306598821878,
-0.013675473895722));
#46472=CARTESIAN_POINT('Ctrl Pts',(-0.0122503614464783,-0.0370410239320082,
-0.0136672564278871));
#46473=CARTESIAN_POINT('Ctrl Pts',(-0.0120624000233708,-0.0370512883889477,
-0.01362329471275));
#46474=CARTESIAN_POINT('Ctrl Pts',(-0.0117063638989342,-0.037072839630674,
-0.0134641226674579));
#46475=CARTESIAN_POINT('Ctrl Pts',(-0.0115428390887165,-0.037083939727006,
-0.0133477524790992));
#46476=CARTESIAN_POINT('Ctrl Pts',(-0.0112744612341667,-0.0371047876072881,
-0.0130620728686492));
#46477=CARTESIAN_POINT('Ctrl Pts',(-0.0111706390738156,-0.0371137078262836,
-0.0128970514311515));
#46478=CARTESIAN_POINT('Ctrl Pts',(-0.0110311629065429,-0.0371337461738722,
-0.0125363611745579));
#46479=CARTESIAN_POINT('Ctrl Pts',(-0.0109969580789391,-0.0371444286662987,
-0.0123440763108809));
#46480=CARTESIAN_POINT('Ctrl Pts',(-0.0110035567944185,-0.0371662222578953,
-0.011951791662141));
#46481=CARTESIAN_POINT('Ctrl Pts',(-0.0110464089534472,-0.0371771234389558,
-0.0117555704030513));
#46482=CARTESIAN_POINT('Ctrl Pts',(-0.0112026551375385,-0.0371969165177683,
-0.0113992949844256));
#46483=CARTESIAN_POINT('Ctrl Pts',(-0.0113114082349763,-0.0372058816211278,
-0.0112412916348739));
#46484=CARTESIAN_POINT('Ctrl Pts',(-0.0115861642794054,-0.0372266266711798,
-0.0109703612616427));
#46485=CARTESIAN_POINT('Ctrl Pts',(-0.0117510802187798,-0.0372375840203846,
-0.0108615394762437));
#46486=CARTESIAN_POINT('Ctrl Pts',(-0.0121162858873101,-0.0372593035509491,
-0.0107121911490276));
#46487=CARTESIAN_POINT('Ctrl Pts',(-0.012313420021904,-0.0372697542965391,
-0.0106742959283085));
#46488=CARTESIAN_POINT('Ctrl Pts',(-0.0127028546731965,-0.0372885784314582,
-0.0106774441831272));
#46489=CARTESIAN_POINT('Ctrl Pts',(-0.0128915164495543,-0.0372987083579849,
-0.0107153497559918));
#46490=CARTESIAN_POINT('Ctrl Pts',(-0.0132513277654239,-0.0373201088947214,
-0.0108625575982811));
#46491=CARTESIAN_POINT('Ctrl Pts',(-0.0134180109124625,-0.0373312003917612,
-0.0109731478122762));
#46492=CARTESIAN_POINT('Ctrl Pts',(-0.0136963350140692,-0.0373522894961551,
-0.0112502840855021));
#46493=CARTESIAN_POINT('Ctrl Pts',(-0.0138062052478684,-0.0373614019821378,
-0.0114131499473394));
#46494=CARTESIAN_POINT('Ctrl Pts',(-0.0139569437368682,-0.0373812392034485,
-0.0117702199309313));
#46495=CARTESIAN_POINT('Ctrl Pts',(-0.0139969777988742,-0.0373918248627651,
-0.0119607617986294));
#46496=CARTESIAN_POINT('Ctrl Pts',(-0.0140028065907852,-0.0374136808391922,
-0.0123541693743183));
#46497=CARTESIAN_POINT('Ctrl Pts',(-0.0139655282866358,-0.0374247437817464,
-0.0125533023402924));
#46498=CARTESIAN_POINT('Ctrl Pts',(-0.0138186270954199,-0.0374448827113351,
-0.0129158030728906));
#46499=CARTESIAN_POINT('Ctrl Pts',(-0.0137140942408266,-0.0374537297954097,
-0.0130771207993225));
#46500=CARTESIAN_POINT('Ctrl Pts',(-0.0134446521312873,-0.037474490623306,
-0.0133578231799252));
#46501=CARTESIAN_POINT('Ctrl Pts',(-0.0132800878972543,-0.0374855892255531,
-0.013472339243484));
#46502=CARTESIAN_POINT('Ctrl Pts',(-0.0129227921909198,-0.037507094202374,
-0.0136276640923396));
#46503=CARTESIAN_POINT('Ctrl Pts',(-0.0127345839372821,-0.0375173163258038,
-0.0136696742781088));
#46504=CARTESIAN_POINT('Ctrl Pts',(-0.0125290175939898,-0.0375273724361939,
-0.0136756429012426));
#46505=CARTESIAN_POINT('Ctrl Pts',(-0.0125145046942967,-0.0375280765324425,
-0.0136758532865582));
#46506=CARTESIAN_POINT('Ctrl Pts',(-0.0125,-0.0375287743898722,-0.0136758532865582));
#46507=CARTESIAN_POINT('Ctrl Pts',(-0.0124999999603558,-0.0375912743917796,
-0.0136758532865582));
#46508=CARTESIAN_POINT('Ctrl Pts',(-0.0125032493611257,-0.0375911180549098,
-0.013675853286644));
#46509=CARTESIAN_POINT('Ctrl Pts',(-0.0125064992227011,-0.0375909614025844,
-0.0136758427281261));
#46510=CARTESIAN_POINT('Ctrl Pts',(-0.0127004506407383,-0.0375815948927042,
-0.013674582082679));
#46511=CARTESIAN_POINT('Ctrl Pts',(-0.0128891431155838,-0.0375714721149941,
-0.0136369870385509));
#46512=CARTESIAN_POINT('Ctrl Pts',(-0.013249137391045,-0.0375500798720693,
-0.013490394668792));
#46513=CARTESIAN_POINT('Ctrl Pts',(-0.0134159771391333,-0.0375389891306121,
-0.0133801028967398));
#46514=CARTESIAN_POINT('Ctrl Pts',(-0.0136948086964579,-0.037517887901,
-0.0131034090547456));
#46515=CARTESIAN_POINT('Ctrl Pts',(-0.0138049909252382,-0.0375087632650271,
-0.012940653039345));
#46516=CARTESIAN_POINT('Ctrl Pts',(-0.0139563022466104,-0.0374889364163352,
-0.0125837697628913));
#46517=CARTESIAN_POINT('Ctrl Pts',(-0.0139966305884438,-0.0374783559366218,
-0.0123933211280314));
#46518=CARTESIAN_POINT('Ctrl Pts',(-0.0140029748889338,-0.0374568959234863,
-0.0120070408915934));
#46519=CARTESIAN_POINT('Ctrl Pts',(-0.0139686964613012,-0.0374462145860024,
-0.0118147768169018));
#46520=CARTESIAN_POINT('Ctrl Pts',(-0.0138290790375217,-0.0374261787279252,
-0.0114541313715126));
#46521=CARTESIAN_POINT('Ctrl Pts',(-0.013725182016287,-0.0374172566445162,
-0.0112891369530126));
#46522=CARTESIAN_POINT('Ctrl Pts',(-0.013456679799678,-0.037396405707353,
-0.011003562696253));
#46523=CARTESIAN_POINT('Ctrl Pts',(-0.0132931144705065,-0.0373853056461237,
-0.0108872639524797));
#46524=CARTESIAN_POINT('Ctrl Pts',(-0.0129370289480666,-0.037363756150175,
-0.0107282403150346));
#46525=CARTESIAN_POINT('Ctrl Pts',(-0.0127490576199794,-0.0373534933098602,
-0.0106843539543152));
#46526=CARTESIAN_POINT('Ctrl Pts',(-0.0123578682010972,-0.0373342525252803,
-0.0106692456583258));
#46527=CARTESIAN_POINT('Ctrl Pts',(-0.0121582709968624,-0.0373241168536264,
-0.0107016325955487));
#46528=CARTESIAN_POINT('Ctrl Pts',(-0.0117872594786064,-0.0373023814590014,
-0.0108414960022373));
#46529=CARTESIAN_POINT('Ctrl Pts',(-0.0116189904163143,-0.0372913803973135,
-0.0109460836577695));
#46530=CARTESIAN_POINT('Ctrl Pts',(-0.0113368698709304,-0.0372704807421901,
-0.0112098241237532));
#46531=CARTESIAN_POINT('Ctrl Pts',(-0.0112240331471482,-0.0372613387017296,
-0.0113646956731273));
#46532=CARTESIAN_POINT('Ctrl Pts',(-0.0110583098028844,-0.0372417988860765,
-0.0117164123548818));
#46533=CARTESIAN_POINT('Ctrl Pts',(-0.0110101713675452,-0.0372309673701446,
-0.0119113796416551));
#46534=CARTESIAN_POINT('Ctrl Pts',(-0.0109929319633865,-0.0372091650776687,
-0.0123038209062213));
#46535=CARTESIAN_POINT('Ctrl Pts',(-0.0110220918246519,-0.037198407465585,
-0.0124974579237282));
#46536=CARTESIAN_POINT('Ctrl Pts',(-0.0111519362910508,-0.037178201358147,
-0.0128611678576125));
#46537=CARTESIAN_POINT('Ctrl Pts',(-0.0112507117349764,-0.0371693757875885,
-0.0130280337170929));
#46538=CARTESIAN_POINT('Ctrl Pts',(-0.0115106356485122,-0.0371487380142908,
-0.0133207921314658));
#46539=CARTESIAN_POINT('Ctrl Pts',(-0.011671346658901,-0.0371376397731738,
-0.0134419691763465));
#46540=CARTESIAN_POINT('Ctrl Pts',(-0.0120238973594344,-0.0371159780044628,
-0.0136111571243781));
#46541=CARTESIAN_POINT('Ctrl Pts',(-0.0122111184598395,-0.0371056075197522,
-0.0136602181158069));
#46542=CARTESIAN_POINT('Ctrl Pts',(-0.0124350149926267,-0.0370944302790649,
-0.013674798610125));
#46543=CARTESIAN_POINT('Ctrl Pts',(-0.0124675238174636,-0.037092836900933,
-0.0136758532865582));
#46544=CARTESIAN_POINT('Ctrl Pts',(-0.0124999999999998,-0.0370912743898722,
-0.0136758532865582));
#46545=CARTESIAN_POINT('Origin',(-0.0125,-0.0332787743898722,-0.0121758532865583));
#46546=CARTESIAN_POINT('',(-0.0124999999999999,-0.0365287743898722,-0.0136758532865582));
#46547=CARTESIAN_POINT('',(-0.0124999999999999,-0.0365912743898722,-0.0136758532865582));
#46548=CARTESIAN_POINT('',(-0.0125,-0.0332787743898722,-0.0136758532865583));
#46549=CARTESIAN_POINT('Ctrl Pts',(-0.0124999999999997,-0.0365287743898722,
-0.0136758532865582));
#46550=CARTESIAN_POINT('Ctrl Pts',(-0.0124535093249928,-0.0365310111735164,
-0.0136758532865582));
#46551=CARTESIAN_POINT('Ctrl Pts',(-0.012406966782071,-0.0365333104878328,
-0.0136736920202203));
#46552=CARTESIAN_POINT('Ctrl Pts',(-0.0121690102954786,-0.0365453764787804,
-0.0136514690708763));
#46553=CARTESIAN_POINT('Ctrl Pts',(-0.0119827417180806,-0.0365558536735853,
-0.0135969166978075));
#46554=CARTESIAN_POINT('Ctrl Pts',(-0.0116342606295698,-0.0365776175990539,
-0.0134170023317158));
#46555=CARTESIAN_POINT('Ctrl Pts',(-0.0114767391645149,-0.036588704461173,
-0.0132907104761859));
#46556=CARTESIAN_POINT('Ctrl Pts',(-0.0112260082151735,-0.0366091089558757,
-0.0129904274101747));
#46557=CARTESIAN_POINT('Ctrl Pts',(-0.0111326373314,-0.0366179030978354,
-0.0128215365432175));
#46558=CARTESIAN_POINT('Ctrl Pts',(-0.0110133402329699,-0.0366382885824072,
-0.0124545978209253));
#46559=CARTESIAN_POINT('Ctrl Pts',(-0.0109897592263766,-0.0366491201358768,
-0.0122596298584732));
#46560=CARTESIAN_POINT('Ctrl Pts',(-0.0110186665446301,-0.036670913425847,
-0.0118673506390097));
#46561=CARTESIAN_POINT('Ctrl Pts',(-0.0110725501203965,-0.036681659337187,
-0.0116739242348894));
#46562=CARTESIAN_POINT('Ctrl Pts',(-0.0112485922780147,-0.0367009162315802,
-0.0113273001358099));
#46563=CARTESIAN_POINT('Ctrl Pts',(-0.0113659676935067,-0.0367103251945031,
-0.0111758227475674));
#46564=CARTESIAN_POINT('Ctrl Pts',(-0.0116562231892481,-0.0367313920343304,
-0.0109201537795875));
#46565=CARTESIAN_POINT('Ctrl Pts',(-0.0118280943561151,-0.0367424324307944,
-0.0108203891002514));
#46566=CARTESIAN_POINT('Ctrl Pts',(-0.0122019002970657,-0.0367639706655118,
-0.0106924635323234));
#46567=CARTESIAN_POINT('Ctrl Pts',(-0.012400312647355,-0.0367737073272017,
-0.0106661025900807));
#46568=CARTESIAN_POINT('Ctrl Pts',(-0.0127895004386877,-0.0367931406180201,
-0.0106916080312694));
#46569=CARTESIAN_POINT('Ctrl Pts',(-0.0129767087322032,-0.0368035127244026,
-0.0107407495850726));
#46570=CARTESIAN_POINT('Ctrl Pts',(-0.0133292021056302,-0.0368251761186331,
-0.0109100953452619));
#46571=CARTESIAN_POINT('Ctrl Pts',(-0.0134898675216707,-0.0368362742633472,
-0.0110313478913681));
#46572=CARTESIAN_POINT('Ctrl Pts',(-0.0137496572444568,-0.0368569086657708,
-0.0113242173794656));
#46573=CARTESIAN_POINT('Ctrl Pts',(-0.0138483532293192,-0.0368657332442425,
-0.0114911126652259));
#46574=CARTESIAN_POINT('Ctrl Pts',(-0.0139780443210008,-0.0368859419912625,
-0.0118548701115842));
#46575=CARTESIAN_POINT('Ctrl Pts',(-0.0140071234453432,-0.0368967007412299,
-0.0120485276109984));
#46576=CARTESIAN_POINT('Ctrl Pts',(-0.0139897144477836,-0.036918503041693,
-0.0124409690193337));
#46577=CARTESIAN_POINT('Ctrl Pts',(-0.0139414921209812,-0.0369293333822894,
-0.0126359151500683));
#46578=CARTESIAN_POINT('Ctrl Pts',(-0.0137756182890593,-0.0369488691250739,
-0.0129875585201895));
#46579=CARTESIAN_POINT('Ctrl Pts',(-0.0136627160916694,-0.0369580144962438,
-0.0131423804614874));
#46580=CARTESIAN_POINT('Ctrl Pts',(-0.0133804777785285,-0.0369789165991125,
-0.013406005066556));
#46581=CARTESIAN_POINT('Ctrl Pts',(-0.0132121557897494,-0.0369899182978853,
-0.0135105239857802));
#46582=CARTESIAN_POINT('Ctrl Pts',(-0.0128593701136842,-0.037010580977242,
-0.0136433377274973));
#46583=CARTESIAN_POINT('Ctrl Pts',(-0.012680332605693,-0.0370200981333355,
-0.0136758532865582));
#46584=CARTESIAN_POINT('Ctrl Pts',(-0.0124999999999999,-0.0370287743898722,
-0.0136758532865582));
#46585=CARTESIAN_POINT('Ctrl Pts',(-0.0124999999999998,-0.0370912743898722,
-0.0136758532865582));
#46586=CARTESIAN_POINT('Ctrl Pts',(-0.0126652476264479,-0.0370833239097378,
-0.0136758532865582));
#46587=CARTESIAN_POINT('Ctrl Pts',(-0.012829577798866,-0.0370746592126169,
-0.0136485523980478));
#46588=CARTESIAN_POINT('Ctrl Pts',(-0.0131725324316519,-0.037054893602503,
-0.0135310052826243));
#46589=CARTESIAN_POINT('Ctrl Pts',(-0.0133443497294871,-0.0370438537318456,
-0.0134311662284271));
#46590=CARTESIAN_POINT('Ctrl Pts',(-0.0136344816805116,-0.0370227894016187,
-0.013175373620329));
#46591=CARTESIAN_POINT('Ctrl Pts',(-0.0137517878987089,-0.0370133850494514,
-0.0130238451589815));
#46592=CARTESIAN_POINT('Ctrl Pts',(-0.0139276744830711,-0.0369941238350818,
-0.0126771433003291));
#46593=CARTESIAN_POINT('Ctrl Pts',(-0.0139814715786065,-0.0369833765575813,
-0.0124836923053207));
#46594=CARTESIAN_POINT('Ctrl Pts',(-0.0140102024472209,-0.0369615829871331,
-0.0120914080372542));
#46595=CARTESIAN_POINT('Ctrl Pts',(-0.013986536706735,-0.0369507524861803,
-0.0118964590201025));
#46596=CARTESIAN_POINT('Ctrl Pts',(-0.0138670801188791,-0.0369303696802525,
-0.0115295685134022));
#46597=CARTESIAN_POINT('Ctrl Pts',(-0.0137736284195215,-0.0369215756173142,
-0.0113607083418922));
#46598=CARTESIAN_POINT('Ctrl Pts',(-0.0135227590025235,-0.0369011675735817,
-0.0110605373438294));
#46599=CARTESIAN_POINT('Ctrl Pts',(-0.013365188521414,-0.0368900804687017,
-0.0109343216472075));
#46600=CARTESIAN_POINT('Ctrl Pts',(-0.0130166440242008,-0.0368683179439088,
-0.0107545675325336));
#46601=CARTESIAN_POINT('Ctrl Pts',(-0.0128303599796439,-0.0368578422903703,
-0.0107000974349616));
#46602=CARTESIAN_POINT('Ctrl Pts',(-0.0124432664521831,-0.0368382186202807,
-0.0106641109685799));
#46603=CARTESIAN_POINT('Ctrl Pts',(-0.0122460134054272,-0.0368288138396488,
-0.0106845154083571));
#46604=CARTESIAN_POINT('Ctrl Pts',(-0.011869596414965,-0.0368074813678198,
-0.010800511041888));
#46605=CARTESIAN_POINT('Ctrl Pts',(-0.0116942542727957,-0.0367964114250926,
-0.0108953274811244));
#46606=CARTESIAN_POINT('Ctrl Pts',(-0.0113959034381422,-0.0367751822121979,
-0.0111428203412331));
#46607=CARTESIAN_POINT('Ctrl Pts',(-0.0112739723597906,-0.0367654340214763,
-0.0112909799176879));
#46608=CARTESIAN_POINT('Ctrl Pts',(-0.0110878097215295,-0.0367464616705573,
-0.0116324822342288));
#46609=CARTESIAN_POINT('Ctrl Pts',(-0.0110283132596915,-0.0367358095895788,
-0.0118242196918422));
#46610=CARTESIAN_POINT('Ctrl Pts',(-0.0109878992504014,-0.0367140441641329,
-0.0122159973498669));
#46611=CARTESIAN_POINT('Ctrl Pts',(-0.0110059300757061,-0.0367031483334851,
-0.0124121223015279));
#46612=CARTESIAN_POINT('Ctrl Pts',(-0.0111148202181895,-0.0366825904386729,
-0.0127821644081477));
#46613=CARTESIAN_POINT('Ctrl Pts',(-0.0112029772453076,-0.0366737547753834,
-0.0129530687178596));
#46614=CARTESIAN_POINT('Ctrl Pts',(-0.0114447104426529,-0.036653583173973,
-0.013260552188956));
#46615=CARTESIAN_POINT('Ctrl Pts',(-0.0115989854789676,-0.0366425166922058,
-0.0133917333313388));
#46616=CARTESIAN_POINT('Ctrl Pts',(-0.0119432119671359,-0.0366206707177402,
-0.0135819706452803));
#46617=CARTESIAN_POINT('Ctrl Pts',(-0.0121284036297215,-0.0366100976904278,
-0.013641838259792));
#46618=CARTESIAN_POINT('Ctrl Pts',(-0.0123797614962902,-0.0365971596534063,
-0.0136722429967861));
#46619=CARTESIAN_POINT('Ctrl Pts',(-0.0124399115641857,-0.0365941653960882,
-0.0136758532865582));
#46620=CARTESIAN_POINT('Ctrl Pts',(-0.0124999999999998,-0.0365912743898722,
-0.0136758532865582));
#46621=CARTESIAN_POINT('Origin',(-0.0125,-0.0332787743898722,-0.0121758532865583));
#46622=CARTESIAN_POINT('',(-0.0125,-0.0360287743898722,-0.0136758532865582));
#46623=CARTESIAN_POINT('',(-0.0125,-0.0360912743898722,-0.0136758532865582));
#46624=CARTESIAN_POINT('',(-0.0125,-0.0332787743898722,-0.0136758532865583));
#46625=CARTESIAN_POINT('Ctrl Pts',(-0.0125,-0.0360287743898722,-0.0136758532865582));
#46626=CARTESIAN_POINT('Ctrl Pts',(-0.01242444109938,-0.0360324097191733,
-0.0136758532865582));
#46627=CARTESIAN_POINT('Ctrl Pts',(-0.0123488306048482,-0.0360362060960539,
-0.0136701449369665));
#46628=CARTESIAN_POINT('Ctrl Pts',(-0.0120825640737028,-0.0360501450852568,
-0.0136295284859621));
#46629=CARTESIAN_POINT('Ctrl Pts',(-0.0118987796343164,-0.0360608177353903,
-0.0135636370678137));
#46630=CARTESIAN_POINT('Ctrl Pts',(-0.0115617241681493,-0.0360826091181342,
-0.0133629444814025));
#46631=CARTESIAN_POINT('Ctrl Pts',(-0.0114127616918364,-0.0360935183899258,
-0.0132282212743018));
#46632=CARTESIAN_POINT('Ctrl Pts',(-0.011181264564215,-0.0361133426135339,
-0.0129155140112531));
#46633=CARTESIAN_POINT('Ctrl Pts',(-0.011098214750844,-0.036122290120798,
-0.0127425701298929));
#46634=CARTESIAN_POINT('Ctrl Pts',(-0.0109997401142268,-0.0361430158280654,
-0.0123695073990797));
#46635=CARTESIAN_POINT('Ctrl Pts',(-0.0109872990402609,-0.0361539672422251,
-0.0121723819442055));
#46636=CARTESIAN_POINT('Ctrl Pts',(-0.0110392177022437,-0.0361756929000075,
-0.0117813201041219));
#46637=CARTESIAN_POINT('Ctrl Pts',(-0.0111043157059502,-0.0361861917332313,
-0.0115914328170068));
#46638=CARTESIAN_POINT('Ctrl Pts',(-0.0113005680489685,-0.0362049754743923,
-0.0112551371644226));
#46639=CARTESIAN_POINT('Ctrl Pts',(-0.0114271766305707,-0.036215089887779,
-0.0111103107785103));
#46640=CARTESIAN_POINT('Ctrl Pts',(-0.0117336109130104,-0.036236472392845,
-0.0108713003425021));
#46641=CARTESIAN_POINT('Ctrl Pts',(-0.0119123357012763,-0.0362475622148453,
-0.0107816271643373));
#46642=CARTESIAN_POINT('Ctrl Pts',(-0.0122912238587956,-0.036268677548959,
-0.0106777286754561));
#46643=CARTESIAN_POINT('Ctrl Pts',(-0.012487336948627,-0.0362778166274809,
-0.0106633068888324));
#46644=CARTESIAN_POINT('Ctrl Pts',(-0.0128722075965176,-0.0362976313768669,
-0.0107100223502403));
#46645=CARTESIAN_POINT('Ctrl Pts',(-0.0130573818425314,-0.0363082057927803,
-0.0107699701207729));
#46646=CARTESIAN_POINT('Ctrl Pts',(-0.013401541774164,-0.0363300528768179,
-0.0109603626586073));
#46647=CARTESIAN_POINT('Ctrl Pts',(-0.0135557666436706,-0.0363411189801075,
-0.0110916170672557));
#46648=CARTESIAN_POINT('Ctrl Pts',(-0.0137973633312287,-0.0363612870144914,
-0.0113992085672866));
#46649=CARTESIAN_POINT('Ctrl Pts',(-0.0138854417969202,-0.0363701238590329,
-0.011570143731452));
#46650=CARTESIAN_POINT('Ctrl Pts',(-0.0139941733700868,-0.0363906843444493,
-0.0119402324689471));
#46651=CARTESIAN_POINT('Ctrl Pts',(-0.0140121193322341,-0.0364015810871345,
-0.0121363738372794));
#46652=CARTESIAN_POINT('Ctrl Pts',(-0.013971530159525,-0.0364233459425802,
-0.0125281412353024));
#46653=CARTESIAN_POINT('Ctrl Pts',(-0.0139119486611866,-0.036433996523078,
-0.0127198516842618));
#46654=CARTESIAN_POINT('Ctrl Pts',(-0.0137256322874889,-0.0364529644987118,
-0.01306127524567));
#46655=CARTESIAN_POINT('Ctrl Pts',(-0.0136036311559106,-0.0364627184441798,
-0.0132093844764852));
#46656=CARTESIAN_POINT('Ctrl Pts',(-0.0133051564697893,-0.0364839501087037,
-0.0134567510782099));
#46657=CARTESIAN_POINT('Ctrl Pts',(-0.0131297621407755,-0.0364950204278691,
-0.0135514906789523));
#46658=CARTESIAN_POINT('Ctrl Pts',(-0.0127979006941046,-0.0365138230573143,
-0.0136535844522717));
#46659=CARTESIAN_POINT('Ctrl Pts',(-0.012649247406269,-0.0365215937206901,
-0.0136758532865582));
#46660=CARTESIAN_POINT('Ctrl Pts',(-0.0124999999999997,-0.0365287743898722,
-0.0136758532865582));
#46661=CARTESIAN_POINT('Ctrl Pts',(-0.0124999999999998,-0.0365912743898722,
-0.0136758532865582));
#46662=CARTESIAN_POINT('Ctrl Pts',(-0.0126339852058531,-0.03658482802365,
-0.0136758532865582));
#46663=CARTESIAN_POINT('Ctrl Pts',(-0.0127676156499676,-0.0365779001980971,
-0.0136579062852937));
#46664=CARTESIAN_POINT('Ctrl Pts',(-0.0130882901520083,-0.0365600247360929,
-0.0135698141833699));
#46665=CARTESIAN_POINT('Ctrl Pts',(-0.0132669667741575,-0.0365489351298924,
-0.0134800653478386));
#46666=CARTESIAN_POINT('Ctrl Pts',(-0.0135732831917688,-0.0365275548590379,
-0.0132409311955683));
#46667=CARTESIAN_POINT('Ctrl Pts',(-0.0136998241499775,-0.0365174423603507,
-0.0130960566116852));
#46668=CARTESIAN_POINT('Ctrl Pts',(-0.0138959299193217,-0.0364986635982211,
-0.0127596863311846));
#46669=CARTESIAN_POINT('Ctrl Pts',(-0.0139609478795168,-0.0364881587948206,
-0.0125697725756292));
#46670=CARTESIAN_POINT('Ctrl Pts',(-0.0140127012380386,-0.0364664324003575,
-0.0121786974752932));
#46671=CARTESIAN_POINT('Ctrl Pts',(-0.0140001794909881,-0.0364554817239551,
-0.0119815853000501));
#46672=CARTESIAN_POINT('Ctrl Pts',(-0.0139015549098239,-0.0364347583984683,
-0.0116085654412878));
#46673=CARTESIAN_POINT('Ctrl Pts',(-0.0138184323132252,-0.0364258129894517,
-0.0114356511185721));
#46674=CARTESIAN_POINT('Ctrl Pts',(-0.0135868027609335,-0.036405984938985,
-0.0111230354548772));
#46675=CARTESIAN_POINT('Ctrl Pts',(-0.0134377843005641,-0.0363950746804312,
-0.0109883736915671));
#46676=CARTESIAN_POINT('Ctrl Pts',(-0.0131006520467281,-0.0363732835866736,
-0.0107878245088091));
#46677=CARTESIAN_POINT('Ctrl Pts',(-0.012916848257935,-0.0363626121552087,
-0.0107220104768881));
#46678=CARTESIAN_POINT('Ctrl Pts',(-0.0125344407406388,-0.0363425975504287,
-0.0106638339539603));
#46679=CARTESIAN_POINT('Ctrl Pts',(-0.0123394827638854,-0.0363336590140195,
-0.0106719828088111));
#46680=CARTESIAN_POINT('Ctrl Pts',(-0.0119581661425258,-0.03631278205237,
-0.0107630936662273));
#46681=CARTESIAN_POINT('Ctrl Pts',(-0.0117760219033341,-0.0363016823644665,
-0.0108471993541692));
#46682=CARTESIAN_POINT('Ctrl Pts',(-0.011461148124963,-0.0362801478962951,
-0.0110770628262301));
#46683=CARTESIAN_POINT('Ctrl Pts',(-0.0113296709011859,-0.0362698989078036,
-0.0112183011803048));
#46684=CARTESIAN_POINT('Ctrl Pts',(-0.0111219776131219,-0.0362506820193385,
-0.0115503738377329));
#46685=CARTESIAN_POINT('Ctrl Pts',(-0.011050801427276,-0.0362404926029528,
-0.0117399254511084));
#46686=CARTESIAN_POINT('Ctrl Pts',(-0.0109878754452061,-0.036218733509438,
-0.0121315891343748));
#46687=CARTESIAN_POINT('Ctrl Pts',(-0.0109950504691957,-0.0362077379708741,
-0.0123295088285253));
#46688=CARTESIAN_POINT('Ctrl Pts',(-0.0110837554713219,-0.0361868592603589,
-0.012705325617798));
#46689=CARTESIAN_POINT('Ctrl Pts',(-0.0111621069339057,-0.0361777450344641,
-0.0128802088468219));
#46690=CARTESIAN_POINT('Ctrl Pts',(-0.011385026356248,-0.0361581704503927,
-0.0131987861079011));
#46691=CARTESIAN_POINT('Ctrl Pts',(-0.0115303178694841,-0.0361473289706943,
-0.0133374270942092));
#46692=CARTESIAN_POINT('Ctrl Pts',(-0.0118622834508789,-0.0361255269137158,
-0.0135473198920959));
#46693=CARTESIAN_POINT('Ctrl Pts',(-0.0120447500101688,-0.0361147791043814,
-0.0136181996767634));
#46694=CARTESIAN_POINT('Ctrl Pts',(-0.0123231115071583,-0.0361000021471243,
-0.0136680338823606));
#46695=CARTESIAN_POINT('Ctrl Pts',(-0.0124115647816169,-0.0360955292313004,
-0.0136758532865582));
#46696=CARTESIAN_POINT('Ctrl Pts',(-0.0125,-0.0360912743898722,-0.0136758532865582));
#46697=CARTESIAN_POINT('Origin',(-0.0125,-0.0332787743898722,-0.0121758532865583));
#46698=CARTESIAN_POINT('',(-0.0125,-0.0355287743898722,-0.0136758532865582));
#46699=CARTESIAN_POINT('',(-0.0125,-0.0355912743898722,-0.0136758532865582));
#46700=CARTESIAN_POINT('',(-0.0125,-0.0332787743898722,-0.0136758532865583));
#46701=CARTESIAN_POINT('Ctrl Pts',(-0.0125,-0.0355287743898722,-0.0136758532865582));
#46702=CARTESIAN_POINT('Ctrl Pts',(-0.0123973442969718,-0.035533713414687,
-0.0136758532865582));
#46703=CARTESIAN_POINT('Ctrl Pts',(-0.0122947420425006,-0.035538942531353,
-0.0136653174042946));
#46704=CARTESIAN_POINT('Ctrl Pts',(-0.0120033924529855,-0.035554647740067,
-0.0136045621823964));
#46705=CARTESIAN_POINT('Ctrl Pts',(-0.011822534712545,-0.035565470259822,
-0.0135282062665997));
#46706=CARTESIAN_POINT('Ctrl Pts',(-0.0114964777476188,-0.0355872657978458,
-0.0133083141271581));
#46707=CARTESIAN_POINT('Ctrl Pts',(-0.01135535830582,-0.0355980232805698,
-0.0131654707922246));
#46708=CARTESIAN_POINT('Ctrl Pts',(-0.0111419578240932,-0.0356173169465204,
-0.0128405192947112));
#46709=CARTESIAN_POINT('Ctrl Pts',(-0.0110687906194607,-0.0356266871868369,
-0.0126634229411933));
#46710=CARTESIAN_POINT('Ctrl Pts',(-0.010991065366143,-0.0356477326223681,
-0.0122846051016316));
#46711=CARTESIAN_POINT('Ctrl Pts',(-0.0109898247408614,-0.0356587684692245,
-0.0120859598582161));
#46712=CARTESIAN_POINT('Ctrl Pts',(-0.0110644253212016,-0.0356803327561648,
-0.0116978026932913));
#46713=CARTESIAN_POINT('Ctrl Pts',(-0.0111402055168341,-0.0356901174045244,
-0.0115122716263748));
#46714=CARTESIAN_POINT('Ctrl Pts',(-0.0113558489600221,-0.0357095258635238,
-0.011187072502319));
#46715=CARTESIAN_POINT('Ctrl Pts',(-0.0114914712724027,-0.0357198841194876,
-0.0110490800233052));
#46716=CARTESIAN_POINT('Ctrl Pts',(-0.0118134552809888,-0.0357415335636135,
-0.010827392696869));
#46717=CARTESIAN_POINT('Ctrl Pts',(-0.0119984324801342,-0.0357526324616988,
-0.0107482222729592));
#46718=CARTESIAN_POINT('Ctrl Pts',(-0.0123817112461122,-0.0357732954923294,
-0.0106682114663947));
#46719=CARTESIAN_POINT('Ctrl Pts',(-0.0125757163912609,-0.0357821290156334,
-0.0106654751773376));
#46720=CARTESIAN_POINT('Ctrl Pts',(-0.0129558867186165,-0.0358023152945974,
-0.0107337068975336));
#46721=CARTESIAN_POINT('Ctrl Pts',(-0.0131383298476193,-0.0358130643140553,
-0.010804670829092));
#46722=CARTESIAN_POINT('Ctrl Pts',(-0.0134702071915908,-0.0358348664160461,
-0.0110147180791208));
#46723=CARTESIAN_POINT('Ctrl Pts',(-0.0136154357263315,-0.035845706681201,
-0.0111534244238167));
#46724=CARTESIAN_POINT('Ctrl Pts',(-0.0138382097237242,-0.0358652770036945,
-0.011472100151494));
#46725=CARTESIAN_POINT('Ctrl Pts',(-0.0139164817782309,-0.0358743945791995,
-0.0116470166944518));
#46726=CARTESIAN_POINT('Ctrl Pts',(-0.0140050201548324,-0.0358952758616462,
-0.012022879778492));
#46727=CARTESIAN_POINT('Ctrl Pts',(-0.0140121052211236,-0.0359062720853291,
-0.012220811804784));
#46728=CARTESIAN_POINT('Ctrl Pts',(-0.0139490008074887,-0.0359280282804241,
-0.0126124233164942));
#46729=CARTESIAN_POINT('Ctrl Pts',(-0.0138777541279319,-0.0359382110540525,
-0.0128019133469663));
#46730=CARTESIAN_POINT('Ctrl Pts',(-0.0136699400069597,-0.0359574308744097,
-0.013133882263771));
#46731=CARTESIAN_POINT('Ctrl Pts',(-0.0135383996098182,-0.0359676815656632,
-0.0132750724978011));
#46732=CARTESIAN_POINT('Ctrl Pts',(-0.0132234169383219,-0.0359892178877941,
-0.0135048141039771));
#46733=CARTESIAN_POINT('Ctrl Pts',(-0.0130412289705088,-0.0360003176285395,
-0.0135888459540308));
#46734=CARTESIAN_POINT('Ctrl Pts',(-0.0127337078466152,-0.0360171503918094,
-0.0136621832207637));
#46735=CARTESIAN_POINT('Ctrl Pts',(-0.0126169341724723,-0.036023148391876,
-0.0136758532865582));
#46736=CARTESIAN_POINT('Ctrl Pts',(-0.0125,-0.0360287743898722,-0.0136758532865582));
#46737=CARTESIAN_POINT('Ctrl Pts',(-0.0125,-0.0360912743898722,-0.0136758532865582));
#46738=CARTESIAN_POINT('Ctrl Pts',(-0.0126029942953792,-0.0360863190745253,
-0.0136758532865582));
#46739=CARTESIAN_POINT('Ctrl Pts',(-0.0127059354300288,-0.0360810717196226,
-0.0136652477854601));
#46740=CARTESIAN_POINT('Ctrl Pts',(-0.0130022256212186,-0.0360650943354945,
-0.0136032516217705));
#46741=CARTESIAN_POINT('Ctrl Pts',(-0.0131871577799667,-0.0360539953548263,
-0.0135240002126186));
#46742=CARTESIAN_POINT('Ctrl Pts',(-0.0135090278211091,-0.036032347653377,
-0.0133021782251363));
#46743=CARTESIAN_POINT('Ctrl Pts',(-0.013644583361116,-0.0360219911172423,
-0.013164132006828));
#46744=CARTESIAN_POINT('Ctrl Pts',(-0.0138600983406451,-0.0360025857322556,
-0.0128388210416437));
#46745=CARTESIAN_POINT('Ctrl Pts',(-0.0139358046676858,-0.0359927950701439,
-0.012653225531447));
#46746=CARTESIAN_POINT('Ctrl Pts',(-0.0140102176635265,-0.0359712275708235,
-0.0122650105436802));
#46747=CARTESIAN_POINT('Ctrl Pts',(-0.0140088809225687,-0.0359601922981304,
-0.0120663756352049));
#46748=CARTESIAN_POINT('Ctrl Pts',(-0.013930977982065,-0.0359391495157561,
-0.0116876055524676));
#46749=CARTESIAN_POINT('Ctrl Pts',(-0.0138577276307545,-0.0359297839804837,
-0.0115105453092611));
#46750=CARTESIAN_POINT('Ctrl Pts',(-0.0136441741427528,-0.0359104857680691,
-0.0111856951536888));
#46751=CARTESIAN_POINT('Ctrl Pts',(-0.0135029868608712,-0.035899726863706,
-0.0110429181422186));
#46752=CARTESIAN_POINT('Ctrl Pts',(-0.0131768328187235,-0.0358779310697273,
-0.0108231849310812));
#46753=CARTESIAN_POINT('Ctrl Pts',(-0.0129959480223017,-0.0358671096786955,
-0.0107469165116545));
#46754=CARTESIAN_POINT('Ctrl Pts',(-0.0126181581242682,-0.0358467498906632,
-0.0106683154404723));
#46755=CARTESIAN_POINT('Ctrl Pts',(-0.0124250757754456,-0.0358379558073767,
-0.0106655496927537));
#46756=CARTESIAN_POINT('Ctrl Pts',(-0.012039925485056,-0.0358175173530894,
-0.0107342341755916));
#46757=CARTESIAN_POINT('Ctrl Pts',(-0.0118521914988264,-0.0358064282541243,
-0.0108082769358769));
#46758=CARTESIAN_POINT('Ctrl Pts',(-0.0115231692681669,-0.0357846779220503,
-0.0110214056702193));
#46759=CARTESIAN_POINT('Ctrl Pts',(-0.0113834010332159,-0.0357742155777443,
-0.0111559643810162));
#46760=CARTESIAN_POINT('Ctrl Pts',(-0.0111597494657645,-0.0357546168898119,
-0.0114741412685692));
#46761=CARTESIAN_POINT('Ctrl Pts',(-0.0110793951575888,-0.0357451722793311,
-0.0116556912762991));
#46762=CARTESIAN_POINT('Ctrl Pts',(-0.0109931706618282,-0.035723812201625,
-0.0120401726750083));
#46763=CARTESIAN_POINT('Ctrl Pts',(-0.0109884090513756,-0.0357127455908268,
-0.0122393716693753));
#46764=CARTESIAN_POINT('Ctrl Pts',(-0.0110550403015091,-0.0356915375024731,
-0.0126211172597409));
#46765=CARTESIAN_POINT('Ctrl Pts',(-0.0111230610732549,-0.0356818381010433,
-0.0128004878644392));
#46766=CARTESIAN_POINT('Ctrl Pts',(-0.0113269772540736,-0.035662828151014,
-0.0131316528798298));
#46767=CARTESIAN_POINT('Ctrl Pts',(-0.0114638446058427,-0.0356521632461508,
-0.0132785282477472));
#46768=CARTESIAN_POINT('Ctrl Pts',(-0.0117837543913012,-0.0356303930961302,
-0.0135081536462352));
#46769=CARTESIAN_POINT('Ctrl Pts',(-0.0119628602916793,-0.0356195051970148,
-0.0135898974949996));
#46770=CARTESIAN_POINT('Ctrl Pts',(-0.0122666642932065,-0.035602879297975,
-0.0136622258942475));
#46771=CARTESIAN_POINT('Ctrl Pts',(-0.0123832482692233,-0.0355968916101383,
-0.0136758532865582));
#46772=CARTESIAN_POINT('Ctrl Pts',(-0.0125000000000001,-0.0355912743898722,
-0.0136758532865582));
#46773=CARTESIAN_POINT('Origin',(-0.0125,-0.0332787743898722,-0.0121758532865583));
#46774=CARTESIAN_POINT('',(-0.0125000000000001,-0.0350287743898722,-0.0136758532865582));
#46775=CARTESIAN_POINT('',(-0.0125000000000001,-0.0350912743898723,-0.0136758532865582));
#46776=CARTESIAN_POINT('',(-0.0125,-0.0332787743898722,-0.0136758532865583));
#46777=CARTESIAN_POINT('Ctrl Pts',(-0.0125000000000002,-0.0350287743898722,
-0.0136758532865582));
#46778=CARTESIAN_POINT('Ctrl Pts',(-0.0123690260553798,-0.0350350758767208,
-0.0136758532865583));
#46779=CARTESIAN_POINT('Ctrl Pts',(-0.0122383852229765,-0.0350418377063322,
-0.0136587039798108));
#46780=CARTESIAN_POINT('Ctrl Pts',(-0.0119224772799044,-0.0350593906313495,
-0.013573967287105));
#46781=CARTESIAN_POINT('Ctrl Pts',(-0.0117452953091194,-0.0350703356724196,
-0.0134868339841646));
#46782=CARTESIAN_POINT('Ctrl Pts',(-0.0114317811740397,-0.0350920675195657,
-0.0132475098977541));
#46783=CARTESIAN_POINT('Ctrl Pts',(-0.0112993449231415,-0.0351026178745569,
-0.013096670562235));
#46784=CARTESIAN_POINT('Ctrl Pts',(-0.0111050513615919,-0.0351213588999748,
-0.0127593321047111));
#46785=CARTESIAN_POINT('Ctrl Pts',(-0.0110422862343725,-0.0351314568690709,
-0.0125775686609812));
#46786=CARTESIAN_POINT('Ctrl Pts',(-0.0109870935977505,-0.0351528201246496,
-0.0121930300605649));
#46787=CARTESIAN_POINT('Ctrl Pts',(-0.010998029993029,-0.0351639080293944,
-0.0119934477751578));
#46788=CARTESIAN_POINT('Ctrl Pts',(-0.0110960424747355,-0.0351850508379232,
-0.0116128772216393));
#46789=CARTESIAN_POINT('Ctrl Pts',(-0.011181036805097,-0.0351942190108102,
-0.0114353356659036));
#46790=CARTESIAN_POINT('Ctrl Pts',(-0.0114129086325599,-0.0352140100870733,
-0.0111244707064398));
#46791=CARTESIAN_POINT('Ctrl Pts',(-0.0115568922039538,-0.0352245725709683,
-0.0109936081473295));
#46792=CARTESIAN_POINT('Ctrl Pts',(-0.0118929902252958,-0.0352464100411046,
-0.0107895980717107));
#46793=CARTESIAN_POINT('Ctrl Pts',(-0.0120834431656559,-0.0352574793131677,
-0.010720978446593));
#46794=CARTESIAN_POINT('Ctrl Pts',(-0.0124704063087179,-0.0352776778052715,
-0.0106640725552989));
#46795=CARTESIAN_POINT('Ctrl Pts',(-0.0126625876140318,-0.0352865050838931,
-0.0106725482631292));
#46796=CARTESIAN_POINT('Ctrl Pts',(-0.0130377914433727,-0.0353070434015203,
-0.0107620556020949));
#46797=CARTESIAN_POINT('Ctrl Pts',(-0.013216867725968,-0.0353179322870024,
-0.0108438862595647));
#46798=CARTESIAN_POINT('Ctrl Pts',(-0.0135366757238662,-0.0353397018717546,
-0.0110736676096182));
#46799=CARTESIAN_POINT('Ctrl Pts',(-0.0136734733591466,-0.0353503652034107,
-0.0112206070945778));
#46800=CARTESIAN_POINT('Ctrl Pts',(-0.0138772356830381,-0.0353693705207853,
-0.0115518718224145));
#46801=CARTESIAN_POINT('Ctrl Pts',(-0.0139451730544627,-0.0353790758692342,
-0.0117312799150757));
#46802=CARTESIAN_POINT('Ctrl Pts',(-0.0140116230129778,-0.0354002865658375,
-0.012113072453934));
#46803=CARTESIAN_POINT('Ctrl Pts',(-0.0140067633305862,-0.0354113535965583,
-0.0123122790069097));
#46804=CARTESIAN_POINT('Ctrl Pts',(-0.013920350323081,-0.0354327102796505,
-0.0126966993025684));
#46805=CARTESIAN_POINT('Ctrl Pts',(-0.0138399218549572,-0.0354421499161469,
-0.0128781849634066));
#46806=CARTESIAN_POINT('Ctrl Pts',(-0.0136161396278266,-0.0354617516849645,
-0.0131962464536166));
#46807=CARTESIAN_POINT('Ctrl Pts',(-0.0134763040444793,-0.0354722156753386,
-0.0133307477720209));
#46808=CARTESIAN_POINT('Ctrl Pts',(-0.0131471681135012,-0.0354939675247689,
-0.0135437341964632));
#46809=CARTESIAN_POINT('Ctrl Pts',(-0.0129593900056609,-0.0355050563869362,
-0.0136176920111582));
#46810=CARTESIAN_POINT('Ctrl Pts',(-0.0126757376743542,-0.035520104819105,
-0.0136681353197265));
#46811=CARTESIAN_POINT('Ctrl Pts',(-0.0125878596923307,-0.035524547238454,
-0.0136758532865582));
#46812=CARTESIAN_POINT('Ctrl Pts',(-0.0125,-0.0355287743898722,-0.0136758532865582));
#46813=CARTESIAN_POINT('Ctrl Pts',(-0.0125000000000001,-0.0355912743898722,
-0.0136758532865582));
#46814=CARTESIAN_POINT('Ctrl Pts',(-0.0125731215724756,-0.0355877563265762,
-0.0136758532865582));
#46815=CARTESIAN_POINT('Ctrl Pts',(-0.0126462945114834,-0.035584087290529,
-0.01367050723696));
#46816=CARTESIAN_POINT('Ctrl Pts',(-0.0129172360277393,-0.0355699411921168,
-0.0136305321661541));
#46817=CARTESIAN_POINT('Ctrl Pts',(-0.0131076478651028,-0.0355588715366797,
-0.0135618275470965));
#46818=CARTESIAN_POINT('Ctrl Pts',(-0.0134436378156878,-0.0355370352820993,
-0.0133576740474468));
#46819=CARTESIAN_POINT('Ctrl Pts',(-0.0135875566235559,-0.035526474291301,
-0.0132267530660998));
#46820=CARTESIAN_POINT('Ctrl Pts',(-0.0138193014513857,-0.0355066861649722,
-0.0129157743344553));
#46821=CARTESIAN_POINT('Ctrl Pts',(-0.013904224462027,-0.0354975142893684,
-0.0127381714774883));
#46822=CARTESIAN_POINT('Ctrl Pts',(-0.0140020559383961,-0.0354763680685431,
-0.0123575395026348));
#46823=CARTESIAN_POINT('Ctrl Pts',(-0.0140128968929006,-0.0354652804136489,
-0.0121579617145387));
#46824=CARTESIAN_POINT('Ctrl Pts',(-0.0139575274879115,-0.0354439195749494,
-0.0117734666179479));
#46825=CARTESIAN_POINT('Ctrl Pts',(-0.0138946820051359,-0.0354338236622805,
-0.011591740189908));
#46826=CARTESIAN_POINT('Ctrl Pts',(-0.0137002418276673,-0.035415087971294,
-0.0112544977521507));
#46827=CARTESIAN_POINT('Ctrl Pts',(-0.0135677386958255,-0.0354045311341893,
-0.0111037184115987));
#46828=CARTESIAN_POINT('Ctrl Pts',(-0.0132541247299294,-0.0353827985347396,
-0.0108645401543042));
#46829=CARTESIAN_POINT('Ctrl Pts',(-0.0130769123191492,-0.035371854296484,
-0.0107774884763052));
#46830=CARTESIAN_POINT('Ctrl Pts',(-0.0127042296422369,-0.0353511515527453,
-0.010677695033225));
#46831=CARTESIAN_POINT('Ctrl Pts',(-0.0125128264173641,-0.0353422236530032,
-0.0106638958203951));
#46832=CARTESIAN_POINT('Ctrl Pts',(-0.0121263928261186,-0.0353223626077001,
-0.0107095708375193));
#46833=CARTESIAN_POINT('Ctrl Pts',(-0.0119354822516037,-0.0353114439086704,
-0.0107719771878248));
#46834=CARTESIAN_POINT('Ctrl Pts',(-0.0115939785841702,-0.0352896554669203,
-0.0109648593878639));
#46835=CARTESIAN_POINT('Ctrl Pts',(-0.0114455760355385,-0.0352789946276801,
-0.0110916088463094));
#46836=CARTESIAN_POINT('Ctrl Pts',(-0.0112049775822295,-0.0352590025567665,
-0.011394594653846));
#46837=CARTESIAN_POINT('Ctrl Pts',(-0.0111151053160591,-0.0352500455327326,
-0.011567972715073));
#46838=CARTESIAN_POINT('Ctrl Pts',(-0.0110047390885022,-0.0352291411203124,
-0.0119442521386352));
#46839=CARTESIAN_POINT('Ctrl Pts',(-0.0109872461493976,-0.0352180419718032,
-0.0121440368118008));
#46840=CARTESIAN_POINT('Ctrl Pts',(-0.0110302588603089,-0.0351965236781261,
-0.0125313660979891));
#46841=CARTESIAN_POINT('Ctrl Pts',(-0.0110874688325119,-0.0351862894743138,
-0.0127155817666109));
#46842=CARTESIAN_POINT('Ctrl Pts',(-0.011272504754752,-0.0351670979784338,
-0.0130610286924501));
#46843=CARTESIAN_POINT('Ctrl Pts',(-0.0114018404118615,-0.0351568504650813,
-0.0132171827805111));
#46844=CARTESIAN_POINT('Ctrl Pts',(-0.0117107302579797,-0.035135066377573,
-0.0134663970233921));
#46845=CARTESIAN_POINT('Ctrl Pts',(-0.0118860163787744,-0.0351240768597058,
-0.0135584151995339));
#46846=CARTESIAN_POINT('Ctrl Pts',(-0.0122125627321767,-0.0351056794412658,
-0.0136551273882549));
#46847=CARTESIAN_POINT('Ctrl Pts',(-0.0123560152331419,-0.0350982018601977,
-0.0136758532865583));
#46848=CARTESIAN_POINT('Ctrl Pts',(-0.0125000000000002,-0.0350912743898723,
-0.0136758532865582));
#46849=CARTESIAN_POINT('Origin',(-0.0125,-0.0332787743898722,-0.0121758532865583));
#46850=CARTESIAN_POINT('',(-0.0125000000000001,-0.0345287743898722,-0.0136758532865583));
#46851=CARTESIAN_POINT('',(-0.0125,-0.0345912743898723,-0.0136758532865583));
#46852=CARTESIAN_POINT('',(-0.0125,-0.0332787743898722,-0.0136758532865583));
#46853=CARTESIAN_POINT('Ctrl Pts',(-0.0125000000000001,-0.0345287743898722,
-0.0136758532865583));
#46854=CARTESIAN_POINT('Ctrl Pts',(-0.0123412969419184,-0.0345364099943143,
-0.0136758532865583));
#46855=CARTESIAN_POINT('Ctrl Pts',(-0.0121834096834421,-0.0345447058197249,
-0.0136506723253203));
#46856=CARTESIAN_POINT('Ctrl Pts',(-0.0118453588160428,-0.0345640523957705,
-0.0135397168655593));
#46857=CARTESIAN_POINT('Ctrl Pts',(-0.0116723716475794,-0.0345750832202484,
-0.0134422297491893));
#46858=CARTESIAN_POINT('Ctrl Pts',(-0.0113722808018559,-0.0345966750745294,
-0.0131846955867555));
#46859=CARTESIAN_POINT('Ctrl Pts',(-0.0112486976652099,-0.0346065120281936,
-0.0130265757967733));
#46860=CARTESIAN_POINT('Ctrl Pts',(-0.0110735036067596,-0.0346258940193351,
-0.0126776999562268));
#46861=CARTESIAN_POINT('Ctrl Pts',(-0.0110211232741819,-0.0346362374298867,
-0.0124915185662973));
#46862=CARTESIAN_POINT('Ctrl Pts',(-0.0109886368102513,-0.0346578717566075,
-0.0121021006853227));
#46863=CARTESIAN_POINT('Ctrl Pts',(-0.0110117654649977,-0.0346689712892342,
-0.0119023090980412));
#46864=CARTESIAN_POINT('Ctrl Pts',(-0.0111326365248452,-0.0346896646047389,
-0.0115298294189562));
#46865=CARTESIAN_POINT('Ctrl Pts',(-0.0112266804936695,-0.0346985088786647,
-0.0113599576107925));
#46866=CARTESIAN_POINT('Ctrl Pts',(-0.0114747926668439,-0.0347186712634827,
-0.0110638546472576));
#46867=CARTESIAN_POINT('Ctrl Pts',(-0.0116269447426416,-0.0347294098241466,
-0.0109408015891161));
#46868=CARTESIAN_POINT('Ctrl Pts',(-0.0119740175823262,-0.0347512113926894,
-0.0107570929138376));
#46869=CARTESIAN_POINT('Ctrl Pts',(-0.0121665380678273,-0.0347620620147946,
-0.0106999257804346));
#46870=CARTESIAN_POINT('Ctrl Pts',(-0.0125537975209007,-0.0347816688929276,
-0.0106648312160837));
#46871=CARTESIAN_POINT('Ctrl Pts',(-0.0127445094384567,-0.0347907582789375,
-0.0106837705225737));
#46872=CARTESIAN_POINT('Ctrl Pts',(-0.0131146557349637,-0.0348116174562792,
-0.01079358871509));
#46873=CARTESIAN_POINT('Ctrl Pts',(-0.0132899054570147,-0.0348226077289797,
-0.010885697109702));
#46874=CARTESIAN_POINT('Ctrl Pts',(-0.0135986514145666,-0.0348443887285896,
-0.0111350494105482));
#46875=CARTESIAN_POINT('Ctrl Pts',(-0.0137278919511177,-0.0348546289848604,
-0.0112912359963488));
#46876=CARTESIAN_POINT('Ctrl Pts',(-0.0139127670204282,-0.0348738236286432,
-0.011636739584438));
#46877=CARTESIAN_POINT('Ctrl Pts',(-0.0139698987575697,-0.0348840596689156,
-0.0118209883093416));
#46878=CARTESIAN_POINT('Ctrl Pts',(-0.0140127404949898,-0.0349055799791375,
-0.0122083538933346));
#46879=CARTESIAN_POINT('Ctrl Pts',(-0.0139951557924346,-0.0349166792024432,
-0.0124081399128387));
#46880=CARTESIAN_POINT('Ctrl Pts',(-0.013884617730595,-0.0349375802231589,
-0.0127843582857208));
#46881=CARTESIAN_POINT('Ctrl Pts',(-0.0137946774333669,-0.0349465348996107,
-0.0129576787311508));
#46882=CARTESIAN_POINT('Ctrl Pts',(-0.0135539567695427,-0.0349665297612131,
-0.0132605533286652));
#46883=CARTESIAN_POINT('Ctrl Pts',(-0.0134054928017999,-0.034977191917188,
-0.0133872438085349));
#46884=CARTESIAN_POINT('Ctrl Pts',(-0.0130638970009965,-0.0349989807021439,
-0.0135799787843043));
#46885=CARTESIAN_POINT('Ctrl Pts',(-0.0128729591856066,-0.0350098983650578,
-0.0136423006518634));
#46886=CARTESIAN_POINT('Ctrl Pts',(-0.0126170802693561,-0.0350230462712982,
-0.0136724299929882));
#46887=CARTESIAN_POINT('Ctrl Pts',(-0.0125585115005907,-0.0350259592539875,
-0.0136758532865582));
#46888=CARTESIAN_POINT('Ctrl Pts',(-0.0125000000000002,-0.0350287743898722,
-0.0136758532865582));
#46889=CARTESIAN_POINT('Ctrl Pts',(-0.0125000000000002,-0.0350912743898723,
-0.0136758532865582));
#46890=CARTESIAN_POINT('Ctrl Pts',(-0.0125453666337599,-0.0350890916866878,
-0.0136758532865582));
#46891=CARTESIAN_POINT('Ctrl Pts',(-0.0125907806026629,-0.0350868495387351,
-0.0136737952617678));
#46892=CARTESIAN_POINT('Ctrl Pts',(-0.0128341782074428,-0.0350745230540291,
-0.0136516188302729));
#46893=CARTESIAN_POINT('Ctrl Pts',(-0.0130266713454518,-0.0350636711485182,
-0.0135943581270203));
#46894=CARTESIAN_POINT('Ctrl Pts',(-0.0133736472785106,-0.0350418696700696,
-0.0134104848479301));
#46895=CARTESIAN_POINT('Ctrl Pts',(-0.013525733439843,-0.0350311324278077,
-0.0132873650850583));
#46896=CARTESIAN_POINT('Ctrl Pts',(-0.0137737125400177,-0.0350109730368056,
-0.0129911394096996));
#46897=CARTESIAN_POINT('Ctrl Pts',(-0.0138676827913623,-0.0350021273263903,
-0.0128212061438837));
#46898=CARTESIAN_POINT('Ctrl Pts',(-0.0139883688579959,-0.0349814302279859,
-0.0124486583726053));
#46899=CARTESIAN_POINT('Ctrl Pts',(-0.0140113978320624,-0.0349703306279255,
-0.012248865571518));
#46900=CARTESIAN_POINT('Ctrl Pts',(-0.0139787247326922,-0.034948698215745,
-0.0118594821522697));
#46901=CARTESIAN_POINT('Ctrl Pts',(-0.0139262585401305,-0.0349383566736314,
-0.0116733343942244));
#46902=CARTESIAN_POINT('Ctrl Pts',(-0.0137508910171738,-0.0349189780031595,
-0.0113245183257306));
#46903=CARTESIAN_POINT('Ctrl Pts',(-0.0136272076737551,-0.0349091344035578,
-0.011166432817616));
#46904=CARTESIAN_POINT('Ctrl Pts',(-0.0133269618621611,-0.0348875391053575,
-0.0109090430828455));
#46905=CARTESIAN_POINT('Ctrl Pts',(-0.0131539329313619,-0.034876508923537,
-0.0108116514366314));
#46906=CARTESIAN_POINT('Ctrl Pts',(-0.0127865458186418,-0.0348554892298485,
-0.010691275609122));
#46907=CARTESIAN_POINT('Ctrl Pts',(-0.0125964917176874,-0.0348461637623236,
-0.0106669644358509));
#46908=CARTESIAN_POINT('Ctrl Pts',(-0.0122084856345947,-0.0348268260914603,
-0.0106910743373682));
#46909=CARTESIAN_POINT('Ctrl Pts',(-0.0120144497898953,-0.0348160549330611,
-0.0107427560982287));
#46910=CARTESIAN_POINT('Ctrl Pts',(-0.0116618559123739,-0.0347942571221303,
-0.0109167667814345));
#46911=CARTESIAN_POINT('Ctrl Pts',(-0.0115059053870387,-0.0347834456367045,
-0.011035866023415));
#46912=CARTESIAN_POINT('Ctrl Pts',(-0.0112500562699438,-0.0347631105501135,
-0.0113247854708115));
#46913=CARTESIAN_POINT('Ctrl Pts',(-0.0111517355574426,-0.0347543150584318,
-0.0114911212524865));
#46914=CARTESIAN_POINT('Ctrl Pts',(-0.0110201746530845,-0.0347338441417561,
-0.0118595977526482));
#46915=CARTESIAN_POINT('Ctrl Pts',(-0.010991262683756,-0.0347227530855843,
-0.0120592367637407));
#46916=CARTESIAN_POINT('Ctrl Pts',(-0.011012892971429,-0.0347010161488557,
-0.0124505016248565));
#46917=CARTESIAN_POINT('Ctrl Pts',(-0.0110602650401685,-0.0346905682161076,
-0.012638564414322));
#46918=CARTESIAN_POINT('Ctrl Pts',(-0.0112254272227659,-0.0346709963974586,
-0.012990857150003));
#46919=CARTESIAN_POINT('Ctrl Pts',(-0.0113432864704596,-0.0346615076722981,
-0.0131509417221946));
#46920=CARTESIAN_POINT('Ctrl Pts',(-0.0116344264112255,-0.0346401181066647,
-0.0134166969154794));
#46921=CARTESIAN_POINT('Ctrl Pts',(-0.0118049253211228,-0.034629055265261,
-0.0135196464314357));
#46922=CARTESIAN_POINT('Ctrl Pts',(-0.0121540050125187,-0.0346087579314118,
-0.0136457266886208));
#46923=CARTESIAN_POINT('Ctrl Pts',(-0.0123264187636525,-0.0345996258209999,
-0.0136758532865583));
#46924=CARTESIAN_POINT('Ctrl Pts',(-0.0125,-0.0345912743898723,-0.0136758532865583));
#46925=CARTESIAN_POINT('Origin',(-0.0125,-0.0332787743898722,-0.0121758532865583));
#46926=CARTESIAN_POINT('',(-0.0124999999921269,-0.0340287743906298,-0.0136758532865583));
#46927=CARTESIAN_POINT('',(-0.0125,-0.0340912743898723,-0.0136758532865583));
#46928=CARTESIAN_POINT('',(-0.0125,-0.0332787743898722,-0.0136758532865583));
#46929=CARTESIAN_POINT('Ctrl Pts',(-0.0124999999842539,-0.0340287743906298,
-0.0136758532865583));
#46930=CARTESIAN_POINT('Ctrl Pts',(-0.0123110245217949,-0.0340378664768616,
-0.0136758532845745));
#46931=CARTESIAN_POINT('Ctrl Pts',(-0.0121236512499408,-0.0340478734955391,
-0.0136401406390158));
#46932=CARTESIAN_POINT('Ctrl Pts',(-0.0117638250240851,-0.0340691432052548,
-0.0134976683943288));
#46933=CARTESIAN_POINT('Ctrl Pts',(-0.0115960720806594,-0.0340802288666755,
-0.013389141204316));
#46934=CARTESIAN_POINT('Ctrl Pts',(-0.0113142518625794,-0.0341014011359788,
-0.0131150664457129));
#46935=CARTESIAN_POINT('Ctrl Pts',(-0.0112022250916371,-0.0341106019315912,
-0.0129529575356181));
#46936=CARTESIAN_POINT('Ctrl Pts',(-0.0110475431979664,-0.0341303674670227,
-0.0125971778978506));
#46937=CARTESIAN_POINT('Ctrl Pts',(-0.0110054879022801,-0.0341409169782053,
-0.0124072866965642));
#46938=CARTESIAN_POINT('Ctrl Pts',(-0.010995318766936,-0.0341627437959899,
-0.0120144039764405));
#46939=CARTESIAN_POINT('Ctrl Pts',(-0.0110303050087293,-0.034173816303497,
-0.0118150988413109));
#46940=CARTESIAN_POINT('Ctrl Pts',(-0.0111730157058391,-0.0341940474243758,
-0.0114509386654922));
#46941=CARTESIAN_POINT('Ctrl Pts',(-0.0112758407392223,-0.0342028657695953,
-0.0112882575802964));
#46942=CARTESIAN_POINT('Ctrl Pts',(-0.0115398596303183,-0.0342233802192822,
-0.011007031525106));
#46943=CARTESIAN_POINT('Ctrl Pts',(-0.0116997428790087,-0.0342342605120498,
-0.0108922668954815));
#46944=CARTESIAN_POINT('Ctrl Pts',(-0.0120579139564312,-0.0342560348160953,
-0.0107287624537415));
#46945=CARTESIAN_POINT('Ctrl Pts',(-0.012253386118002,-0.0342667116541822,
-0.0106829639979216));
#46946=CARTESIAN_POINT('Ctrl Pts',(-0.0126420686172139,-0.0342857569317473,
-0.0106705518422238));
#46947=CARTESIAN_POINT('Ctrl Pts',(-0.0128314895662413,-0.0342954115800285,
-0.0107006353612827));
#46948=CARTESIAN_POINT('Ctrl Pts',(-0.0131957868781216,-0.0343165997280838,
-0.0108324272380366));
#46949=CARTESIAN_POINT('Ctrl Pts',(-0.0133662400961577,-0.0343276630498013,
-0.0109354731859148));
#46950=CARTESIAN_POINT('Ctrl Pts',(-0.013657220492716,-0.0343490489513218,
-0.0112013728098045));
#46951=CARTESIAN_POINT('Ctrl Pts',(-0.01377497883035,-0.034358532105937,
-0.0113614921757279));
#46952=CARTESIAN_POINT('Ctrl Pts',(-0.0139399619394467,-0.0343781072737967,
-0.0117138451972016));
#46953=CARTESIAN_POINT('Ctrl Pts',(-0.0139872438660849,-0.0343885570083426,
-0.0119019404190269));
#46954=CARTESIAN_POINT('Ctrl Pts',(-0.0140086792973725,-0.0344102956305679,
-0.0122932356190815));
#46955=CARTESIAN_POINT('Ctrl Pts',(-0.0139796637894866,-0.0344213864533069,
-0.0124928704283847));
#46956=CARTESIAN_POINT('Ctrl Pts',(-0.0138479122117746,-0.034441853337423,
-0.0128612743424733));
#46957=CARTESIAN_POINT('Ctrl Pts',(-0.0137495149095708,-0.0344506485758436,
-0.0130275472897237));
#46958=CARTESIAN_POINT('Ctrl Pts',(-0.0134935269297074,-0.0344709867383029,
-0.013316336951008));
#46959=CARTESIAN_POINT('Ctrl Pts',(-0.0133375088719449,-0.0344817994644339,
-0.0134353638887793));
#46960=CARTESIAN_POINT('Ctrl Pts',(-0.0129848179956392,-0.0345035970449082,
-0.013609198268725));
#46961=CARTESIAN_POINT('Ctrl Pts',(-0.0127907563166154,-0.0345143666899402,
-0.0136607808020066));
#46962=CARTESIAN_POINT('Ctrl Pts',(-0.012561509598585,-0.0345257887586781,
-0.0136749083134762));
#46963=CARTESIAN_POINT('Ctrl Pts',(-0.0125307407466012,-0.0345272953750118,
-0.0136758532865583));
#46964=CARTESIAN_POINT('Ctrl Pts',(-0.0125000000000001,-0.0345287743898722,
-0.0136758532865583));
#46965=CARTESIAN_POINT('Ctrl Pts',(-0.0125,-0.0345912743898723,-0.0136758532865583));
#46966=CARTESIAN_POINT('Ctrl Pts',(-0.01251620762298,-0.0345904946002481,
-0.0136758532865583));
#46967=CARTESIAN_POINT('Ctrl Pts',(-0.0125324247338042,-0.034589707057313,
-0.0136755906007887));
#46968=CARTESIAN_POINT('Ctrl Pts',(-0.0127473797303576,-0.034579171289561,
-0.0136686159370902));
#46969=CARTESIAN_POINT('Ctrl Pts',(-0.0129428289865807,-0.0345684927632912,
-0.0136227170334578));
#46970=CARTESIAN_POINT('Ctrl Pts',(-0.0133009077920266,-0.0345467178909423,
-0.0134590323130444));
#46971=CARTESIAN_POINT('Ctrl Pts',(-0.0134607251051158,-0.0345358386922668,
-0.0133441928669241));
#46972=CARTESIAN_POINT('Ctrl Pts',(-0.0137246055465384,-0.0345153272546697,
-0.0130628354450979));
#46973=CARTESIAN_POINT('Ctrl Pts',(-0.0138273542447476,-0.0345065099366744,
-0.0129000931289942));
#46974=CARTESIAN_POINT('Ctrl Pts',(-0.0139698771363575,-0.0344862747102172,
-0.0125358590527656));
#46975=CARTESIAN_POINT('Ctrl Pts',(-0.0140047607596412,-0.0344752018073557,
-0.0123365468012601));
#46976=CARTESIAN_POINT('Ctrl Pts',(-0.0139943975013312,-0.0344533763559891,
-0.0119436886766608));
#46977=CARTESIAN_POINT('Ctrl Pts',(-0.0139522519045707,-0.034442828491156,
-0.0117538271096656));
#46978=CARTESIAN_POINT('Ctrl Pts',(-0.0137973933362267,-0.0344230661827964,
-0.0113981055591923));
#46979=CARTESIAN_POINT('Ctrl Pts',(-0.0136852694656437,-0.0344138611748065,
-0.0112360306090336));
#46980=CARTESIAN_POINT('Ctrl Pts',(-0.0134032924649268,-0.034392685196546,
-0.0109620938834637));
#46981=CARTESIAN_POINT('Ctrl Pts',(-0.0132354920479945,-0.0343815998314314,
-0.0108536595869972));
#46982=CARTESIAN_POINT('Ctrl Pts',(-0.0128742859884516,-0.034360254469438,
-0.0107108538023672));
#46983=CARTESIAN_POINT('Ctrl Pts',(-0.0126854032092023,-0.0343502120395477,
-0.0106752256764677));
#46984=CARTESIAN_POINT('Ctrl Pts',(-0.0122961866848581,-0.0343314497403325,
-0.0106765256529042));
#46985=CARTESIAN_POINT('Ctrl Pts',(-0.0120995215228156,-0.034320871585718,
-0.0107167051662914));
#46986=CARTESIAN_POINT('Ctrl Pts',(-0.0117363500058537,-0.0342991382017244,
-0.010870075470822));
#46987=CARTESIAN_POINT('Ctrl Pts',(-0.0115728444058113,-0.0342882011203275,
-0.0109806103945126));
#46988=CARTESIAN_POINT('Ctrl Pts',(-0.0113011329345216,-0.034267520847394,
-0.0112544821468481));
#46989=CARTESIAN_POINT('Ctrl Pts',(-0.0111940630273294,-0.0342586107963544,
-0.0114137979698795));
#46990=CARTESIAN_POINT('Ctrl Pts',(-0.011040978195299,-0.0342386099278618,
-0.0117738136027466));
#46991=CARTESIAN_POINT('Ctrl Pts',(-0.0110003103750975,-0.0342275637077669,
-0.0119726455644544));
#46992=CARTESIAN_POINT('Ctrl Pts',(-0.0109997050066188,-0.034205669388615,
-0.0123667433091882));
#46993=CARTESIAN_POINT('Ctrl Pts',(-0.0110367350121909,-0.034195032464366,
-0.0125582079456697));
#46994=CARTESIAN_POINT('Ctrl Pts',(-0.0111816501095527,-0.0341750905799763,
-0.0129171618646849));
#46995=CARTESIAN_POINT('Ctrl Pts',(-0.0112883728258302,-0.0341660885615832,
-0.013081142930457));
#46996=CARTESIAN_POINT('Ctrl Pts',(-0.0115615464491464,-0.0341451235360998,
-0.0133627332529875));
#46997=CARTESIAN_POINT('Ctrl Pts',(-0.0117266150624285,-0.0341340261166963,
-0.0134763331265757));
#46998=CARTESIAN_POINT('Ctrl Pts',(-0.0120845161041907,-0.0341125447318022,
-0.0136297601943475));
#46999=CARTESIAN_POINT('Ctrl Pts',(-0.0122728385334754,-0.0341023438157408,
-0.0136708091568324));
#47000=CARTESIAN_POINT('Ctrl Pts',(-0.0124758844978791,-0.0340924386841435,
-0.0136757079677189));
#47001=CARTESIAN_POINT('Ctrl Pts',(-0.0124879451577319,-0.0340918543787413,
-0.0136758532865583));
#47002=CARTESIAN_POINT('Ctrl Pts',(-0.0125,-0.0340912743898723,-0.0136758532865583));
#47003=CARTESIAN_POINT('Origin',(-0.0125,-0.0332787743898722,-0.0121758532865583));
#47004=CARTESIAN_POINT('',(-0.0125000000000001,-0.0335912743898723,-0.0110006128129775));
#47005=CARTESIAN_POINT('',(-0.0124999999999998,-0.0335287743898722,-0.0110006128129775));
#47006=CARTESIAN_POINT('',(-0.0125,-0.0332787743898722,-0.0110006128129775));
#47007=CARTESIAN_POINT('',(-0.0126906536866924,-0.033329014863453,-0.013335526232907));
#47008=CARTESIAN_POINT('Ctrl Pts',(-0.0125000000000001,-0.0335912743898723,
-0.0110006128129775));
#47009=CARTESIAN_POINT('Ctrl Pts',(-0.0123606182656347,-0.0335827152817934,
-0.0110006128129774));
#47010=CARTESIAN_POINT('Ctrl Pts',(-0.0122221996424511,-0.0335733364717449,
-0.011025401296828));
#47011=CARTESIAN_POINT('Ctrl Pts',(-0.0119468498475538,-0.0335528060058356,
-0.0111275590896844));
#47012=CARTESIAN_POINT('Ctrl Pts',(-0.0118144159874647,-0.0335417874032893,
-0.0112089650995605));
#47013=CARTESIAN_POINT('Ctrl Pts',(-0.0115921511920793,-0.033520840775346,
-0.0114148069798741));
#47014=CARTESIAN_POINT('Ctrl Pts',(-0.0115031316668629,-0.0335116561249178,
-0.0115358398651166));
#47015=CARTESIAN_POINT('Ctrl Pts',(-0.0113719732613067,-0.0334921407827157,
-0.011811062505257));
#47016=CARTESIAN_POINT('Ctrl Pts',(-0.011333585454047,-0.0334813115339317,
-0.0119637861628906));
#47017=CARTESIAN_POINT('Ctrl Pts',(-0.0113188148773676,-0.0334594912885804,
-0.0122715145886542));
#47018=CARTESIAN_POINT('Ctrl Pts',(-0.0113411116867082,-0.033448712895394,
-0.0124235210356094));
#47019=CARTESIAN_POINT('Ctrl Pts',(-0.0114419111410691,-0.0334284655664098,
-0.0127090668016587));
#47020=CARTESIAN_POINT('Ctrl Pts',(-0.0115188437531633,-0.0334196421390437,
-0.0128400834142289));
#47021=CARTESIAN_POINT('Ctrl Pts',(-0.0117218265531614,-0.0333990144974729,
-0.0130703254335343));
#47022=CARTESIAN_POINT('Ctrl Pts',(-0.0118475770209433,-0.0333879080103003,
-0.0131657862721312));
#47023=CARTESIAN_POINT('Ctrl Pts',(-0.0120986057939069,-0.0333681883958016,
-0.0132871986211697));
#47024=CARTESIAN_POINT('Ctrl Pts',(-0.0122166059982005,-0.0333596736347119,
-0.0133229816765623));
#47025=CARTESIAN_POINT('Ctrl Pts',(-0.0124551250412871,-0.0333438499456641,
-0.0133561739308117));
#47026=CARTESIAN_POINT('Ctrl Pts',(-0.0125739752653183,-0.0333368598974044,
-0.0133547085129306));
#47027=CARTESIAN_POINT('Ctrl Pts',(-0.0126906536866942,-0.0333290148634529,
-0.0133355262329067));
#47028=CARTESIAN_POINT('',(-0.0118107823295574,-0.033329014863453,-0.013127782471683));
#47029=CARTESIAN_POINT('Origin',(-0.0125,-0.0333290148634431,-0.0121758532865683));
#47030=CARTESIAN_POINT('Ctrl Pts',(-0.0118107823295574,-0.033329014863453,
-0.013127782471683));
#47031=CARTESIAN_POINT('Ctrl Pts',(-0.0117328566913963,-0.0333358003910761,
-0.0130713625954565));
#47032=CARTESIAN_POINT('Ctrl Pts',(-0.0116621427476965,-0.0333424750213042,
-0.0130055796445843));
#47033=CARTESIAN_POINT('Ctrl Pts',(-0.0115406222582317,-0.0333550646124425,
-0.0128609601772603));
#47034=CARTESIAN_POINT('Ctrl Pts',(-0.0114896421085979,-0.0333607045471329,
-0.0127832623550946));
#47035=CARTESIAN_POINT('Ctrl Pts',(-0.0113811872311915,-0.0333761238757399,
-0.0125658053264422));
#47036=CARTESIAN_POINT('Ctrl Pts',(-0.011340535452318,-0.033386489009944,
-0.012419627023673));
#47037=CARTESIAN_POINT('Ctrl Pts',(-0.0113160342671908,-0.0334081534624427,
-0.0121140957267005));
#47038=CARTESIAN_POINT('Ctrl Pts',(-0.0113347125284062,-0.0334192615619009,
-0.0119574394698863));
#47039=CARTESIAN_POINT('Ctrl Pts',(-0.0114305459831103,-0.0334399437325939,
-0.0116657611809258));
#47040=CARTESIAN_POINT('Ctrl Pts',(-0.0115047157059423,-0.0334487832102545,
-0.0115329427712829));
#47041=CARTESIAN_POINT('Ctrl Pts',(-0.0117001104984668,-0.0334689877424058,
-0.0113014920650536));
#47042=CARTESIAN_POINT('Ctrl Pts',(-0.0118198666538377,-0.0334797477308066,
-0.011205422037943));
#47043=CARTESIAN_POINT('Ctrl Pts',(-0.0120926769324657,-0.033501567971333,
-0.0110624865859171));
#47044=CARTESIAN_POINT('Ctrl Pts',(-0.0122438352623582,-0.0335124163458775,
-0.0110183137211824));
#47045=CARTESIAN_POINT('Ctrl Pts',(-0.0124327970500069,-0.0335245965763909,
-0.0110020523410354));
#47046=CARTESIAN_POINT('Ctrl Pts',(-0.0124664153270286,-0.0335267120332294,
-0.0110006128129775));
#47047=CARTESIAN_POINT('Ctrl Pts',(-0.0124999999999996,-0.0335287743898722,
-0.0110006128129775));
#47048=CARTESIAN_POINT('Origin',(-0.0125,-0.0332787743898722,-0.0121758532865583));
#47049=CARTESIAN_POINT('',(-0.0125,-0.0340912743898723,-0.0110006128129774));
#47050=CARTESIAN_POINT('',(-0.0124999999999999,-0.0340287743898722,-0.0110006128129774));
#47051=CARTESIAN_POINT('',(-0.0125,-0.0332787743898722,-0.0110006128129775));
#47052=CARTESIAN_POINT('Ctrl Pts',(-0.0125,-0.0340912743898723,-0.0110006128129774));
#47053=CARTESIAN_POINT('Ctrl Pts',(-0.0124960756575115,-0.0340910334051288,
-0.0110006128129774));
#47054=CARTESIAN_POINT('Ctrl Pts',(-0.0124921505656907,-0.034090791677487,
-0.0110006324691183));
#47055=CARTESIAN_POINT('Ctrl Pts',(-0.0123323264010234,-0.0340809204712669,
-0.0110022338813871));
#47056=CARTESIAN_POINT('Ctrl Pts',(-0.0121783321910986,-0.0340703094181835,
-0.0110348010229487));
#47057=CARTESIAN_POINT('Ctrl Pts',(-0.0118945028923491,-0.03404854722475,
-0.0111570137092445));
#47058=CARTESIAN_POINT('Ctrl Pts',(-0.0117669768468642,-0.0340376130145685,
-0.0112445399516225));
#47059=CARTESIAN_POINT('Ctrl Pts',(-0.0115554391496173,-0.0340169553720472,
-0.0114608106541898));
#47060=CARTESIAN_POINT('Ctrl Pts',(-0.0114723627009985,-0.0340080699165182,
-0.0115864157522107));
#47061=CARTESIAN_POINT('Ctrl Pts',(-0.0113544964578955,-0.0339879909906153,
-0.0118695865488572));
#47062=CARTESIAN_POINT('Ctrl Pts',(-0.0113238269325546,-0.0339769287177227,
-0.0120255965188557));
#47063=CARTESIAN_POINT('Ctrl Pts',(-0.0113256989701605,-0.0339550347126428,
-0.0123343651696396));
#47064=CARTESIAN_POINT('Ctrl Pts',(-0.0113558598489915,-0.0339444113894496,
-0.0124841846822066));
#47065=CARTESIAN_POINT('Ctrl Pts',(-0.0114717278904493,-0.0339245026676132,
-0.0127649551103596));
#47066=CARTESIAN_POINT('Ctrl Pts',(-0.0115566133573988,-0.0339154439189668,
-0.0128930785763459));
#47067=CARTESIAN_POINT('Ctrl Pts',(-0.0117728436441561,-0.0338943996582683,
-0.0131121263393762));
#47068=CARTESIAN_POINT('Ctrl Pts',(-0.0119029408615713,-0.0338832952199362,
-0.0132000005976338));
#47069=CARTESIAN_POINT('Ctrl Pts',(-0.0121843786053174,-0.0338618376170957,
-0.0133177643660779));
#47070=CARTESIAN_POINT('Ctrl Pts',(-0.0123322121926354,-0.0338516645398618,
-0.0133486485723279));
#47071=CARTESIAN_POINT('Ctrl Pts',(-0.0126376803750815,-0.0338327396235902,
-0.0133533540217116));
#47072=CARTESIAN_POINT('Ctrl Pts',(-0.0127924795143073,-0.0338223800324146,
-0.0133247532125323));
#47073=CARTESIAN_POINT('Ctrl Pts',(-0.0130798021287743,-0.0338006531586729,
-0.0132095873456977));
#47074=CARTESIAN_POINT('Ctrl Pts',(-0.013209789910203,-0.0337896738409785,
-0.0131250526628537));
#47075=CARTESIAN_POINT('Ctrl Pts',(-0.013426646557467,-0.0337688716315349,
-0.0129139170303992));
#47076=CARTESIAN_POINT('Ctrl Pts',(-0.0135126638660378,-0.033759864506462,
-0.012790599717729));
#47077=CARTESIAN_POINT('Ctrl Pts',(-0.0136368875227898,-0.0337401111985121,
-0.0125120210738503));
#47078=CARTESIAN_POINT('Ctrl Pts',(-0.0136714076205765,-0.033729215140356,
-0.0123583552112813));
#47079=CARTESIAN_POINT('Ctrl Pts',(-0.0136783772259481,-0.0337074000407905,
-0.0120506993559462));
#47080=CARTESIAN_POINT('Ctrl Pts',(-0.0136523764604824,-0.0336966907224385,
-0.0118996670634857));
#47081=CARTESIAN_POINT('Ctrl Pts',(-0.0135445189826161,-0.0336765999644974,
-0.0116163294009577));
#47082=CARTESIAN_POINT('Ctrl Pts',(-0.0134639062296177,-0.033667698154565,
-0.0114866694833925));
#47083=CARTESIAN_POINT('Ctrl Pts',(-0.0132547377211007,-0.0336468736678169,
-0.0112615892554586));
#47084=CARTESIAN_POINT('Ctrl Pts',(-0.0131269116311139,-0.0336357639483301,
-0.0111696323300625));
#47085=CARTESIAN_POINT('Ctrl Pts',(-0.0128482089187027,-0.0336141739931157,
-0.0110433982475888));
#47086=CARTESIAN_POINT('Ctrl Pts',(-0.0127008963514952,-0.0336038806845843,
-0.011008220391548));
#47087=CARTESIAN_POINT('Ctrl Pts',(-0.0125339405954373,-0.0335933716248387,
-0.0110009801072019));
#47088=CARTESIAN_POINT('Ctrl Pts',(-0.0125169639503397,-0.0335923161066012,
-0.0110006128129775));
#47089=CARTESIAN_POINT('Ctrl Pts',(-0.0125000000000001,-0.0335912743898723,
-0.0110006128129775));
#47090=CARTESIAN_POINT('Ctrl Pts',(-0.0124999999999996,-0.0335287743898722,
-0.0110006128129775));
#47091=CARTESIAN_POINT('Ctrl Pts',(-0.0126148986869939,-0.0335358300509642,
-0.0110006128129775));
#47092=CARTESIAN_POINT('Ctrl Pts',(-0.0127293308609662,-0.0335434541633367,
-0.011017454444084));
#47093=CARTESIAN_POINT('Ctrl Pts',(-0.012986994847461,-0.0335620348809274,
-0.0110952508003727));
#47094=CARTESIAN_POINT('Ctrl Pts',(-0.0131241327667588,-0.0335730432997486,
-0.0111682219008775));
#47095=CARTESIAN_POINT('Ctrl Pts',(-0.0133650044577329,-0.0335948077276303,
-0.0113649023707454));
#47096=CARTESIAN_POINT('Ctrl Pts',(-0.0134654911485693,-0.0336049736271007,
-0.0114876217079503));
#47097=CARTESIAN_POINT('Ctrl Pts',(-0.0136090293070465,-0.0336242176119487,
-0.0117590174263455));
#47098=CARTESIAN_POINT('Ctrl Pts',(-0.0136531133265856,-0.0336344847740661,
-0.0119038140399763));
#47099=CARTESIAN_POINT('Ctrl Pts',(-0.0136850907754152,-0.0336560467161619,
-0.0122078996444548));
#47100=CARTESIAN_POINT('Ctrl Pts',(-0.0136704101812334,-0.0336671560908242,
-0.012364573885327));
#47101=CARTESIAN_POINT('Ctrl Pts',(-0.0135820169627469,-0.0336880302264316,
-0.0126589594335283));
#47102=CARTESIAN_POINT('Ctrl Pts',(-0.0135108076846844,-0.0336969609151749,
-0.0127942518647259));
#47103=CARTESIAN_POINT('Ctrl Pts',(-0.0133207509146878,-0.0337170112452909,
-0.0130305989098306));
#47104=CARTESIAN_POINT('Ctrl Pts',(-0.0132036492230265,-0.0337277019725857,
-0.0131293130400358));
#47105=CARTESIAN_POINT('Ctrl Pts',(-0.0129347619976434,-0.0337495135035495,
-0.0132787977596712));
#47106=CARTESIAN_POINT('Ctrl Pts',(-0.0127847238389795,-0.033760425425484,
-0.0133267032210376));
#47107=CARTESIAN_POINT('Ctrl Pts',(-0.0124815104404345,-0.0337802385943466,
-0.0133603679201949));
#47108=CARTESIAN_POINT('Ctrl Pts',(-0.0123315782170086,-0.0337892093446016,
-0.0133484828980741));
#47109=CARTESIAN_POINT('Ctrl Pts',(-0.0120398348396179,-0.0338099745512868,
-0.0132680985783555));
#47110=CARTESIAN_POINT('Ctrl Pts',(-0.0119012718128719,-0.033820942856139,
-0.0131987272817984));
#47111=CARTESIAN_POINT('Ctrl Pts',(-0.0116567089731332,-0.0338426823272352,
-0.0130091439945126));
#47112=CARTESIAN_POINT('Ctrl Pts',(-0.0115537661659194,-0.0338531314367685,
-0.0128900650648286));
#47113=CARTESIAN_POINT('Ctrl Pts',(-0.0114034119906524,-0.0338719791266584,
-0.012624258248924));
#47114=CARTESIAN_POINT('Ctrl Pts',(-0.0113553126678132,-0.0338821227434151,
-0.0124812039813923));
#47115=CARTESIAN_POINT('Ctrl Pts',(-0.0113145406433663,-0.0339035466245377,
-0.0121790654350339));
#47116=CARTESIAN_POINT('Ctrl Pts',(-0.0113244949922415,-0.0339146484201904,
-0.0120224980800683));
#47117=CARTESIAN_POINT('Ctrl Pts',(-0.0114040081761379,-0.0339357434184588,
-0.0117249977310072));
#47118=CARTESIAN_POINT('Ctrl Pts',(-0.0114717055415038,-0.0339448493571179,
-0.0115867248514679));
#47119=CARTESIAN_POINT('Ctrl Pts',(-0.0116554621777097,-0.0339647148741365,
-0.0113446784505098));
#47120=CARTESIAN_POINT('Ctrl Pts',(-0.011769387434291,-0.0339753169567894,
-0.0112429628638632));
#47121=CARTESIAN_POINT('Ctrl Pts',(-0.0120346233421407,-0.0339971949315404,
-0.0110852797784763));
#47122=CARTESIAN_POINT('Ctrl Pts',(-0.0121846047606453,-0.034008263962634,
-0.0110328446552472));
#47123=CARTESIAN_POINT('Ctrl Pts',(-0.0123934552532009,-0.0340221034284428,
-0.0110042315111123));
#47124=CARTESIAN_POINT('Ctrl Pts',(-0.0124467484439296,-0.0340255043356872,
-0.0110006128129774));
#47125=CARTESIAN_POINT('Ctrl Pts',(-0.0124999999999998,-0.0340287743898722,
-0.0110006128129774));
#47126=CARTESIAN_POINT('Origin',(-0.0125,-0.0332787743898722,-0.0121758532865583));
#47127=CARTESIAN_POINT('',(-0.0124999999999998,-0.0345912743898723,-0.0110006128129774));
#47128=CARTESIAN_POINT('',(-0.0125000000423485,-0.0345287743950732,-0.0110006128129774));
#47129=CARTESIAN_POINT('',(-0.0125,-0.0332787743898722,-0.0110006128129775));
#47130=CARTESIAN_POINT('Ctrl Pts',(-0.0124999999999997,-0.0345912743898723,
-0.0110006128129774));
#47131=CARTESIAN_POINT('Ctrl Pts',(-0.0124750554773252,-0.0345897426047605,
-0.0110006128129774));
#47132=CARTESIAN_POINT('Ctrl Pts',(-0.0124500886290699,-0.0345881812931068,
-0.0110014069628304));
#47133=CARTESIAN_POINT('Ctrl Pts',(-0.012269495724329,-0.0345766828180498,
-0.0110129342348475));
#47134=CARTESIAN_POINT('Ctrl Pts',(-0.0121174170957439,-0.0345658970309991,
-0.0110537477669458));
#47135=CARTESIAN_POINT('Ctrl Pts',(-0.0118412360152098,-0.034544080492877,
-0.0111907403896408));
#47136=CARTESIAN_POINT('Ctrl Pts',(-0.0117191564965817,-0.0345332637431826,
-0.0112843872296165));
#47137=CARTESIAN_POINT('Ctrl Pts',(-0.0115190236604412,-0.0345129241353354,
-0.0115114413177684));
#47138=CARTESIAN_POINT('Ctrl Pts',(-0.0114422353637598,-0.0345041213979416,
-0.0116421012583143));
#47139=CARTESIAN_POINT('Ctrl Pts',(-0.0113398627879977,-0.0344836129238636,
-0.0119313299237687));
#47140=CARTESIAN_POINT('Ctrl Pts',(-0.0113176466556352,-0.0344725118019906,
-0.0120878877764957));
#47141=CARTESIAN_POINT('Ctrl Pts',(-0.0113355030581801,-0.0344507674845931,
-0.0123945453990058));
#47142=CARTESIAN_POINT('Ctrl Pts',(-0.0113730900707122,-0.0344403206155127,
-0.0125418763993926));
#47143=CARTESIAN_POINT('Ctrl Pts',(-0.0115035277113585,-0.0344207548638443,
-0.0128178099584733));
#47144=CARTESIAN_POINT('Ctrl Pts',(-0.0115964602246692,-0.0344112228445418,
-0.0129431204378604));
#47145=CARTESIAN_POINT('Ctrl Pts',(-0.0118256274042374,-0.0343897908260657,
-0.013150697852471));
#47146=CARTESIAN_POINT('Ctrl Pts',(-0.0119595985074006,-0.034378721487533,
-0.01323087232687));
#47147=CARTESIAN_POINT('Ctrl Pts',(-0.012245671537934,-0.034357537461157,
-0.0133328911078831));
#47148=CARTESIAN_POINT('Ctrl Pts',(-0.0123942878919688,-0.0343479318087532,
-0.0133557726528935));
#47149=CARTESIAN_POINT('Ctrl Pts',(-0.0126989942687216,-0.0343288234442705,
-0.0133445734190455));
#47150=CARTESIAN_POINT('Ctrl Pts',(-0.0128520930281185,-0.0343181215089025,
-0.0133078919067336));
#47151=CARTESIAN_POINT('Ctrl Pts',(-0.0131322163996732,-0.0342963242478649,
-0.0131782712574251));
#47152=CARTESIAN_POINT('Ctrl Pts',(-0.0132570700842285,-0.0342854447960889,
-0.0130876608532056));
#47153=CARTESIAN_POINT('Ctrl Pts',(-0.0134629554352069,-0.0342649434297038,
-0.0128660078886874));
#47154=CARTESIAN_POINT('Ctrl Pts',(-0.0135429143205125,-0.034256129396065,
-0.0127379238827873));
#47155=CARTESIAN_POINT('Ctrl Pts',(-0.013653144077261,-0.0342358355343372,
-0.0124517218707739));
#47156=CARTESIAN_POINT('Ctrl Pts',(-0.0136796361890583,-0.0342247501576865,
-0.0122953860711175));
#47157=CARTESIAN_POINT('Ctrl Pts',(-0.013669846293963,-0.0342029228794306,
-0.0119875584611037));
#47158=CARTESIAN_POINT('Ctrl Pts',(-0.013635997498135,-0.0341923834356137,
-0.0118389218897923));
#47159=CARTESIAN_POINT('Ctrl Pts',(-0.0135129416810887,-0.0341726419863371,
-0.0115605104874276));
#47160=CARTESIAN_POINT('Ctrl Pts',(-0.0134241318189287,-0.034163380193175,
-0.0114337693518147));
#47161=CARTESIAN_POINT('Ctrl Pts',(-0.0132015324683946,-0.034142142524701,
-0.0112202979153486));
#47162=CARTESIAN_POINT('Ctrl Pts',(-0.0130694805575508,-0.0341310512062501,
-0.011136179341794));
#47163=CARTESIAN_POINT('Ctrl Pts',(-0.0127893113962216,-0.0341099946665643,
-0.0110275306197938));
#47164=CARTESIAN_POINT('Ctrl Pts',(-0.01264522667166,-0.0341001924219539,
-0.0110006128129774));
#47165=CARTESIAN_POINT('Ctrl Pts',(-0.0125,-0.0340912743898723,-0.0110006128129774));
#47166=CARTESIAN_POINT('Ctrl Pts',(-0.0124999999999998,-0.0340287743898722,
-0.0110006128129774));
#47167=CARTESIAN_POINT('Ctrl Pts',(-0.0125955056067571,-0.0340346391670188,
-0.0110006128129774));
#47168=CARTESIAN_POINT('Ctrl Pts',(-0.0126908262120928,-0.0340409051371065,
-0.011012249201206));
#47169=CARTESIAN_POINT('Ctrl Pts',(-0.0129324829267262,-0.0340578775172794,
-0.011072406568164));
#47170=CARTESIAN_POINT('Ctrl Pts',(-0.0130724056305593,-0.0340687980883178,
-0.0111380764658867));
#47171=CARTESIAN_POINT('Ctrl Pts',(-0.0133213733388323,-0.0340905710059925,
-0.0113209736836162));
#47172=CARTESIAN_POINT('Ctrl Pts',(-0.013427397961506,-0.034101206621743,
-0.0114373193964856));
#47173=CARTESIAN_POINT('Ctrl Pts',(-0.0135843958313036,-0.0341201202909029,
-0.0116988657373322));
#47174=CARTESIAN_POINT('Ctrl Pts',(-0.0136361543301948,-0.0341299774445908,
-0.01184024768765));
#47175=CARTESIAN_POINT('Ctrl Pts',(-0.013684883456739,-0.0341512708602702,
-0.0121405462947768));
#47176=CARTESIAN_POINT('Ctrl Pts',(-0.0136792146875315,-0.0341623572145446,
-0.0122968958817491));
#47177=CARTESIAN_POINT('Ctrl Pts',(-0.0136078449982781,-0.034183646717213,
-0.0125971393041294));
#47178=CARTESIAN_POINT('Ctrl Pts',(-0.0135433557374113,-0.0341929738714508,
-0.0127381691020281));
#47179=CARTESIAN_POINT('Ctrl Pts',(-0.0133653109219861,-0.0342126692503355,
-0.0129853097894741));
#47180=CARTESIAN_POINT('Ctrl Pts',(-0.013254300345489,-0.0342231848416828,
-0.0130896341961224));
#47181=CARTESIAN_POINT('Ctrl Pts',(-0.0129939293247358,-0.0342449915957543,
-0.0132537346789326));
#47182=CARTESIAN_POINT('Ctrl Pts',(-0.0128457982073995,-0.0342560819201148,
-0.0133099752108118));
#47183=CARTESIAN_POINT('Ctrl Pts',(-0.0125431626361086,-0.0342764331401208,
-0.0133598168836629));
#47184=CARTESIAN_POINT('Ctrl Pts',(-0.0123920925090513,-0.0342852381394321,
-0.0133556799747317));
#47185=CARTESIAN_POINT('Ctrl Pts',(-0.0120967084097093,-0.0343056968533139,
-0.0132902464363481));
#47186=CARTESIAN_POINT('Ctrl Pts',(-0.0119554696453631,-0.0343165603444115,
-0.0132284660060567));
#47187=CARTESIAN_POINT('Ctrl Pts',(-0.0117019596409682,-0.0343383643191689,
-0.0130525602870196));
#47188=CARTESIAN_POINT('Ctrl Pts',(-0.011592818912802,-0.0343490893486699,
-0.0129390898433797));
#47189=CARTESIAN_POINT('Ctrl Pts',(-0.0114289320733949,-0.0343682679614312,
-0.0126820026092625));
#47190=CARTESIAN_POINT('Ctrl Pts',(-0.0113734465632184,-0.0343777906865557,
-0.0125422984840514));
#47191=CARTESIAN_POINT('Ctrl Pts',(-0.0113166127250521,-0.034398934582652,
-0.0122441085345134));
#47192=CARTESIAN_POINT('Ctrl Pts',(-0.0113178982285662,-0.0344099966351187,
-0.012088101673157));
#47193=CARTESIAN_POINT('Ctrl Pts',(-0.0113808354132985,-0.0344314792774952,
-0.0117851344235536));
#47194=CARTESIAN_POINT('Ctrl Pts',(-0.0114420075582455,-0.0344410932807145,
-0.0116412294678506));
#47195=CARTESIAN_POINT('Ctrl Pts',(-0.0116142017157204,-0.0344606118760316,
-0.0113889414604652));
#47196=CARTESIAN_POINT('Ctrl Pts',(-0.011722198372666,-0.0344710331859705,
-0.0112820560718705));
#47197=CARTESIAN_POINT('Ctrl Pts',(-0.0119774849513258,-0.0344927531395949,
-0.0111115973505905));
#47198=CARTESIAN_POINT('Ctrl Pts',(-0.0121236464354651,-0.0345038570820486,
-0.0110515612051203));
#47199=CARTESIAN_POINT('Ctrl Pts',(-0.0123508526918609,-0.0345193639805299,
-0.0110077099518364));
#47200=CARTESIAN_POINT('Ctrl Pts',(-0.012425419189096,-0.0345241945556681,
-0.0110006128102796));
#47201=CARTESIAN_POINT('Ctrl Pts',(-0.012500000042512,-0.0345287743924827,
-0.0110006128129774));
#47202=CARTESIAN_POINT('Origin',(-0.0125,-0.0332787743898722,-0.0121758532865583));
#47203=CARTESIAN_POINT('',(-0.0124999999999998,-0.0350912743898722,-0.0110006128129774));
#47204=CARTESIAN_POINT('',(-0.0125000000000001,-0.0350287743898722,-0.0110006128129774));
#47205=CARTESIAN_POINT('',(-0.0125,-0.0332787743898722,-0.0110006128129775));
#47206=CARTESIAN_POINT('Ctrl Pts',(-0.0124999999999996,-0.0350912743898722,
-0.0110006128129774));
#47207=CARTESIAN_POINT('Ctrl Pts',(-0.0124552876665998,-0.0350885287094876,
-0.0110006128129774));
#47208=CARTESIAN_POINT('Ctrl Pts',(-0.0124105325232473,-0.0350856899460719,
-0.011003164142657));
#47209=CARTESIAN_POINT('Ctrl Pts',(-0.0122109721925805,-0.0350726230844953,
-0.0110260764208655));
#47210=CARTESIAN_POINT('Ctrl Pts',(-0.0120611117066231,-0.0350617021504674,
-0.0110745438134338));
#47211=CARTESIAN_POINT('Ctrl Pts',(-0.0117928315208616,-0.0350398931158629,
-0.0112250095448001));
#47212=CARTESIAN_POINT('Ctrl Pts',(-0.0116761362008922,-0.0350292133877324,
-0.0113241172915062));
#47213=CARTESIAN_POINT('Ctrl Pts',(-0.0114868904033686,-0.0350091866776769,
-0.0115612027601145));
#47214=CARTESIAN_POINT('Ctrl Pts',(-0.0114161319308057,-0.0350002375159901,
-0.0116968752014844));
#47215=CARTESIAN_POINT('Ctrl Pts',(-0.0113288757678491,-0.0349793345953434,
-0.0119916667018041));
#47216=CARTESIAN_POINT('Ctrl Pts',(-0.0113148032167167,-0.0349682256427751,
-0.0121483349899323));
#47217=CARTESIAN_POINT('Ctrl Pts',(-0.011347914804051,-0.0349466804359757,
-0.0124521845784391));
#47218=CARTESIAN_POINT('Ctrl Pts',(-0.0113925179879937,-0.0349364286986426,
-0.0125967636580998));
#47219=CARTESIAN_POINT('Ctrl Pts',(-0.0115371196843806,-0.0349172114068112,
-0.0128677829279349));
#47220=CARTESIAN_POINT('Ctrl Pts',(-0.0116382332305663,-0.0349069854009331,
-0.0129902878348671));
#47221=CARTESIAN_POINT('Ctrl Pts',(-0.0118800569666037,-0.0348851947755575,
-0.0131860582348388));
#47222=CARTESIAN_POINT('Ctrl Pts',(-0.0120174377737695,-0.0348741925574974,
-0.0132584337439644));
#47223=CARTESIAN_POINT('Ctrl Pts',(-0.0123076663604168,-0.0348533088805891,
-0.0133447833022396));
#47224=CARTESIAN_POINT('Ctrl Pts',(-0.012457197589519,-0.0348442086648951,
-0.0133597213009138));
#47225=CARTESIAN_POINT('Ctrl Pts',(-0.0127608903301276,-0.0348245887360935,
-0.0133323373315443));
#47226=CARTESIAN_POINT('Ctrl Pts',(-0.0129118703237368,-0.0348137293994736,
-0.0132875463855168));
#47227=CARTESIAN_POINT('Ctrl Pts',(-0.0131840440009712,-0.0347919096621732,
-0.0131435225014095));
#47228=CARTESIAN_POINT('Ctrl Pts',(-0.0133033659481531,-0.0347811606893557,
-0.0130470111066754));
#47229=CARTESIAN_POINT('Ctrl Pts',(-0.0134978824727176,-0.0347609813752259,
-0.0128147504894661));
#47230=CARTESIAN_POINT('Ctrl Pts',(-0.0135715657997223,-0.0347521305278522,
-0.0126815283015197));
#47231=CARTESIAN_POINT('Ctrl Pts',(-0.01366618036253,-0.0347314164816825,
-0.0123894004763574));
#47232=CARTESIAN_POINT('Ctrl Pts',(-0.0136842015515831,-0.0347203076904613,
-0.0122327344636891));
#47233=CARTESIAN_POINT('Ctrl Pts',(-0.013658469194559,-0.0346986591920476,
-0.011927428165352));
#47234=CARTESIAN_POINT('Ctrl Pts',(-0.0136172510282482,-0.0346883097513367,
-0.0117814711861244));
#47235=CARTESIAN_POINT('Ctrl Pts',(-0.0134795375287987,-0.0346689211106175,
-0.0115080354025123));
#47236=CARTESIAN_POINT('Ctrl Pts',(-0.0133824475650228,-0.0346590613965485,
-0.0113841536072333));
#47237=CARTESIAN_POINT('Ctrl Pts',(-0.0131467858703251,-0.0346374426253905,
-0.0111825575193544));
#47238=CARTESIAN_POINT('Ctrl Pts',(-0.0130110166597482,-0.0346264036088737,
-0.0111063527141999));
#47239=CARTESIAN_POINT('Ctrl Pts',(-0.0127465686445372,-0.0346071066042064,
-0.0110201032108124));
#47240=CARTESIAN_POINT('Ctrl Pts',(-0.0126236004277015,-0.0345988644046192,
-0.0110006128129774));
#47241=CARTESIAN_POINT('Ctrl Pts',(-0.0124999999999997,-0.0345912743898723,
-0.0110006128129774));
#47242=CARTESIAN_POINT('Ctrl Pts',(-0.012500000042512,-0.0345287743924827,
-0.0110006128129774));
#47243=CARTESIAN_POINT('Ctrl Pts',(-0.0125751211765788,-0.034533387406676,
-0.0110006128156948));
#47244=CARTESIAN_POINT('Ctrl Pts',(-0.0126502252123126,-0.0345382546490307,
-0.0110078131349879));
#47245=CARTESIAN_POINT('Ctrl Pts',(-0.0128738424439069,-0.0345535279388742,
-0.011051291649753));
#47246=CARTESIAN_POINT('Ctrl Pts',(-0.013016290332032,-0.0345643270592042,
-0.0111091621890696));
#47247=CARTESIAN_POINT('Ctrl Pts',(-0.0132741421697673,-0.0345861459630291,
-0.0112779687180286));
#47248=CARTESIAN_POINT('Ctrl Pts',(-0.0133863167557866,-0.0345969523672073,
-0.0113884796012615));
#47249=CARTESIAN_POINT('Ctrl Pts',(-0.0135570436862805,-0.0346163907559161,
-0.0116410466310697));
#47250=CARTESIAN_POINT('Ctrl Pts',(-0.0136162397705058,-0.0346256438448179,
-0.0117791314254577));
#47251=CARTESIAN_POINT('Ctrl Pts',(-0.013681017378618,-0.0346466362775183,
-0.0120751853040379));
#47252=CARTESIAN_POINT('Ctrl Pts',(-0.0136840279483189,-0.0346576660579381,
-0.0122307370364074));
#47253=CARTESIAN_POINT('Ctrl Pts',(-0.0136294701515449,-0.0346793321314919,
-0.0125362911949342));
#47254=CARTESIAN_POINT('Ctrl Pts',(-0.0135715964158634,-0.0346892862043902,
-0.0126830698979639));
#47255=CARTESIAN_POINT('Ctrl Pts',(-0.0134051543343992,-0.0347086285387393,
-0.0129403492166821));
#47256=CARTESIAN_POINT('Ctrl Pts',(-0.0133001431436326,-0.0347189518902571,
-0.0130496425915515));
#47257=CARTESIAN_POINT('Ctrl Pts',(-0.0130499439073725,-0.0347405734590142,
-0.0132261378272708));
#47258=CARTESIAN_POINT('Ctrl Pts',(-0.0129057865875121,-0.0347516829744878,
-0.0132898024784227));
#47259=CARTESIAN_POINT('Ctrl Pts',(-0.0126058552783491,-0.0347724490275718,
-0.013356028757632));
#47260=CARTESIAN_POINT('Ctrl Pts',(-0.012453463099758,-0.0347813216172268,
-0.0133598515234103));
#47261=CARTESIAN_POINT('Ctrl Pts',(-0.0121546345135361,-0.0348014594615642,
-0.0133094343843143));
#47262=CARTESIAN_POINT('Ctrl Pts',(-0.0120111272940138,-0.0348121900505733,
-0.0132553316395669));
#47263=CARTESIAN_POINT('Ctrl Pts',(-0.0117493005129558,-0.0348340081668068,
-0.0130934321290248));
#47264=CARTESIAN_POINT('Ctrl Pts',(-0.0116342945808522,-0.0348448850404909,
-0.0129858376342885));
#47265=CARTESIAN_POINT('Ctrl Pts',(-0.0114570481241346,-0.0348645678180743,
-0.0127376695784204));
#47266=CARTESIAN_POINT('Ctrl Pts',(-0.0113942990939783,-0.0348736221129475,
-0.0126010874011101));
#47267=CARTESIAN_POINT('Ctrl Pts',(-0.0113220405410279,-0.0348944675692732,
-0.0123071063135395));
#47268=CARTESIAN_POINT('Ctrl Pts',(-0.0113149905895466,-0.0349054592775354,
-0.0121520915084571));
#47269=CARTESIAN_POINT('Ctrl Pts',(-0.0113612936472873,-0.0349271702020729,
-0.0118459048216325));
#47270=CARTESIAN_POINT('Ctrl Pts',(-0.0114150706796611,-0.0349374285204873,
-0.011697940814626));
#47271=CARTESIAN_POINT('Ctrl Pts',(-0.0115739795518052,-0.0349564432998835,
-0.0114368525347288));
#47272=CARTESIAN_POINT('Ctrl Pts',(-0.0116756081885004,-0.0349666504916691,
-0.0113249767791944));
#47273=CARTESIAN_POINT('Ctrl Pts',(-0.0119199856945809,-0.0349881465373255,
-0.0111419384868976));
#47274=CARTESIAN_POINT('Ctrl Pts',(-0.0120618120852735,-0.034999253402818,
-0.0110743112927582));
#47275=CARTESIAN_POINT('Ctrl Pts',(-0.01230684687214,-0.0350164906234034,
-0.0110125348904171));
#47276=CARTESIAN_POINT('Ctrl Pts',(-0.012403329223776,-0.035022838062379,
-0.0110006128129774));
#47277=CARTESIAN_POINT('Ctrl Pts',(-0.0125000000000002,-0.0350287743898722,
-0.0110006128129774));
#47278=CARTESIAN_POINT('Origin',(-0.0125,-0.0332787743898722,-0.0121758532865583));
#47279=CARTESIAN_POINT('',(-0.0125,-0.0355912743898722,-0.0110006128129774));
#47280=CARTESIAN_POINT('',(-0.0125000000000003,-0.0355287743898722,-0.0110006128129774));
#47281=CARTESIAN_POINT('',(-0.0125,-0.0332787743898722,-0.0110006128129775));
#47282=CARTESIAN_POINT('Ctrl Pts',(-0.0125,-0.0355912743898722,-0.0110006128129774));
#47283=CARTESIAN_POINT('Ctrl Pts',(-0.0124345292523923,-0.0355872539835591,
-0.0110006128129774));
#47284=CARTESIAN_POINT('Ctrl Pts',(-0.0123690379077626,-0.035583038398789,
-0.0110060822968235));
#47285=CARTESIAN_POINT('Ctrl Pts',(-0.0121495456404542,-0.0355682449724107,
-0.0110431705401221));
#47286=CARTESIAN_POINT('Ctrl Pts',(-0.0120017074749619,-0.0355571520648707,
-0.0110999913400475));
#47287=CARTESIAN_POINT('Ctrl Pts',(-0.0117420984906089,-0.0355353575437144,
-0.0112650666698114));
#47288=CARTESIAN_POINT('Ctrl Pts',(-0.0116315416578729,-0.0355248558389244,
-0.0113697853026487));
#47289=CARTESIAN_POINT('Ctrl Pts',(-0.0114543809551182,-0.0355051870121528,
-0.0116177083953289));
#47290=CARTESIAN_POINT('Ctrl Pts',(-0.0113903907715994,-0.035495820390194,
-0.0117591694216318));
#47291=CARTESIAN_POINT('Ctrl Pts',(-0.0113202894508321,-0.0354745012951279,
-0.0120598301822132));
#47292=CARTESIAN_POINT('Ctrl Pts',(-0.0113152836457058,-0.0354634180620672,
-0.0122161357510653));
#47293=CARTESIAN_POINT('Ctrl Pts',(-0.011365239104169,-0.0354421469389728,
-0.0125161199684137));
#47294=CARTESIAN_POINT('Ctrl Pts',(-0.0114175580229306,-0.0354323441161254,
-0.0126572463836102));
#47295=CARTESIAN_POINT('Ctrl Pts',(-0.0115755923960375,-0.035413390378229,
-0.0129181276176857));
#47296=CARTESIAN_POINT('Ctrl Pts',(-0.0116820895434152,-0.0354027408413695,
-0.0130340475493773));
#47297=CARTESIAN_POINT('Ctrl Pts',(-0.011931751210611,-0.0353809622357486,
-0.0132159032279045));
#47298=CARTESIAN_POINT('Ctrl Pts',(-0.0120718781108207,-0.0353700497578868,
-0.0132809911728404));
#47299=CARTESIAN_POINT('Ctrl Pts',(-0.0123657072097343,-0.0353494562066715,
-0.013352921241973));
#47300=CARTESIAN_POINT('Ctrl Pts',(-0.012516259401743,-0.0353406074290187,
-0.0133604437247109));
#47301=CARTESIAN_POINT('Ctrl Pts',(-0.0128199445188925,-0.0353204394393541,
-0.0133175880717269));
#47302=CARTESIAN_POINT('Ctrl Pts',(-0.0129696559249467,-0.0353093667370173,
-0.0132645817229708));
#47303=CARTESIAN_POINT('Ctrl Pts',(-0.0132341760342632,-0.0352874984708951,
-0.0131059326775182));
#47304=CARTESIAN_POINT('Ctrl Pts',(-0.0133476704264422,-0.0352769088719306,
-0.0130038229238963));
#47305=CARTESIAN_POINT('Ctrl Pts',(-0.0135305788875744,-0.0352570684653057,
-0.0127610156986414));
#47306=CARTESIAN_POINT('Ctrl Pts',(-0.0135978014977944,-0.0352479333985992,
-0.0126223366674694));
#47307=CARTESIAN_POINT('Ctrl Pts',(-0.0136761109873917,-0.0352268091623596,
-0.0123244239786432));
#47308=CARTESIAN_POINT('Ctrl Pts',(-0.0136854288183076,-0.0352157091431185,
-0.0121678816762062));
#47309=CARTESIAN_POINT('Ctrl Pts',(-0.013643476049991,-0.035194305258746,
-0.0118660251417291));
#47310=CARTESIAN_POINT('Ctrl Pts',(-0.0135948394926351,-0.0351841789224989,
-0.0117232145792489));
#47311=CARTESIAN_POINT('Ctrl Pts',(-0.0134435058323278,-0.0351653763725535,
-0.0114580443668216));
#47312=CARTESIAN_POINT('Ctrl Pts',(-0.013340116020403,-0.0351548738967728,
-0.0113393623320089));
#47313=CARTESIAN_POINT('Ctrl Pts',(-0.0130948822829875,-0.0351331275196624,
-0.011150746284128));
#47314=CARTESIAN_POINT('Ctrl Pts',(-0.0129561133062562,-0.0351221658043202,
-0.0110819175656211));
#47315=CARTESIAN_POINT('Ctrl Pts',(-0.0127074190161277,-0.0351044993361626,
-0.0110143723499798));
#47316=CARTESIAN_POINT('Ctrl Pts',(-0.0126038551037074,-0.0350976518902041,
-0.0110006128129774));
#47317=CARTESIAN_POINT('Ctrl Pts',(-0.0124999999999996,-0.0350912743898722,
-0.0110006128129774));
#47318=CARTESIAN_POINT('Ctrl Pts',(-0.0125000000000002,-0.0350287743898722,
-0.0110006128129774));
#47319=CARTESIAN_POINT('Ctrl Pts',(-0.0125546888212527,-0.0350321327031687,
-0.0110006128129774));
#47320=CARTESIAN_POINT('Ctrl Pts',(-0.012609421191665,-0.0350356290052212,
-0.0110044294629226));
#47321=CARTESIAN_POINT('Ctrl Pts',(-0.012813885449725,-0.0350492050309046,
-0.0110332092561165));
#47322=CARTESIAN_POINT('Ctrl Pts',(-0.0129584415239535,-0.0350598528762727,
-0.0110831614830011));
#47323=CARTESIAN_POINT('Ctrl Pts',(-0.0132257724025345,-0.0350817645774922,
-0.0112381672537046));
#47324=CARTESIAN_POINT('Ctrl Pts',(-0.0133447973984118,-0.0350928181986125,
-0.0113437858235582));
#47325=CARTESIAN_POINT('Ctrl Pts',(-0.0135291034215912,-0.0351128298789464,
-0.0115890033074171));
#47326=CARTESIAN_POINT('Ctrl Pts',(-0.0135952043657725,-0.0351217495110005,
-0.0117242100808198));
#47327=CARTESIAN_POINT('Ctrl Pts',(-0.0136744022935768,-0.035142454939962,
-0.01201621637848));
#47328=CARTESIAN_POINT('Ctrl Pts',(-0.0136851883990951,-0.0351534046726152,
-0.0121706392063467));
#47329=CARTESIAN_POINT('Ctrl Pts',(-0.0136465456508244,-0.0351751527339925,
-0.0124773496297772));
#47330=CARTESIAN_POINT('Ctrl Pts',(-0.0135965142476663,-0.0351857339679876,
-0.0126265755631941));
#47331=CARTESIAN_POINT('Ctrl Pts',(-0.0134443651452701,-0.0352044947311438,
-0.0128911564613117));
#47332=CARTESIAN_POINT('Ctrl Pts',(-0.0133458896582763,-0.0352145712368459,
-0.0130053181706356));
#47333=CARTESIAN_POINT('Ctrl Pts',(-0.0131068203572745,-0.0352359486738981,
-0.013194205096655));
#47334=CARTESIAN_POINT('Ctrl Pts',(-0.0129671948691386,-0.0352470451332583,
-0.0132653508528565));
#47335=CARTESIAN_POINT('Ctrl Pts',(-0.0126704764749306,-0.0352682204812501,
-0.0133486865425982));
#47336=CARTESIAN_POINT('Ctrl Pts',(-0.0125165627929197,-0.0352774099212503,
-0.013360892051278));
#47337=CARTESIAN_POINT('Ctrl Pts',(-0.0122144216837957,-0.0352972060465856,
-0.0133258508181941));
#47338=CARTESIAN_POINT('Ctrl Pts',(-0.0120690292452226,-0.0353077733883185,
-0.0132796178839744));
#47339=CARTESIAN_POINT('Ctrl Pts',(-0.0117985458588359,-0.0353296238447704,
-0.0131317998728765));
#47340=CARTESIAN_POINT('Ctrl Pts',(-0.0116771593965247,-0.0353407025688426,
-0.0130295634347428));
#47341=CARTESIAN_POINT('Ctrl Pts',(-0.0114864993883782,-0.0353609273379629,
-0.0127893410420865));
#47342=CARTESIAN_POINT('Ctrl Pts',(-0.0114167578880609,-0.0353697579334339,
-0.012655583483048));
#47343=CARTESIAN_POINT('Ctrl Pts',(-0.0113301579872456,-0.0353903101380483,
-0.0123657380908379));
#47344=CARTESIAN_POINT('Ctrl Pts',(-0.0113154036292189,-0.0354012080560016,
-0.0122120459997603));
#47345=CARTESIAN_POINT('Ctrl Pts',(-0.011345879036472,-0.0354229957397928,
-0.011904776785957));
#47346=CARTESIAN_POINT('Ctrl Pts',(-0.0113919595530775,-0.0354336692035811,
-0.0117542501463094));
#47347=CARTESIAN_POINT('Ctrl Pts',(-0.011536956117191,-0.0354526927734774,
-0.0114859629147793));
#47348=CARTESIAN_POINT('Ctrl Pts',(-0.0116321417068633,-0.0354624040789343,
-0.0113694639712957));
#47349=CARTESIAN_POINT('Ctrl Pts',(-0.0118654117781541,-0.0354836360779248,
-0.0111746346774902));
#47350=CARTESIAN_POINT('Ctrl Pts',(-0.0120026293927432,-0.0354947134002586,
-0.0110998581365557));
#47351=CARTESIAN_POINT('Ctrl Pts',(-0.0122637927405005,-0.0355136358715802,
-0.0110184834241725));
#47352=CARTESIAN_POINT('Ctrl Pts',(-0.0123816436139273,-0.035521506399523,
-0.0110006128129773));
#47353=CARTESIAN_POINT('Ctrl Pts',(-0.0125000000000005,-0.0355287743898722,
-0.0110006128129774));
#47354=CARTESIAN_POINT('Origin',(-0.0125,-0.0332787743898722,-0.0121758532865583));
#47355=CARTESIAN_POINT('',(-0.0125,-0.0360912743898722,-0.0110006128129774));
#47356=CARTESIAN_POINT('',(-0.0125000000000001,-0.0360287743898721,-0.0110006128129774));
#47357=CARTESIAN_POINT('',(-0.0125,-0.0332787743898722,-0.0110006128129775));
#47358=CARTESIAN_POINT('Ctrl Pts',(-0.0125,-0.0360912743898722,-0.0110006128129774));
#47359=CARTESIAN_POINT('Ctrl Pts',(-0.012413435300456,-0.0360859586530392,
-0.0110006128129774));
#47360=CARTESIAN_POINT('Ctrl Pts',(-0.0123269621105405,-0.036080309589048,
-0.0110101730619216));
#47361=CARTESIAN_POINT('Ctrl Pts',(-0.0120899200069141,-0.0360638632442838,
-0.0110634859351337));
#47362=CARTESIAN_POINT('Ctrl Pts',(-0.0119460639646851,-0.0360527535455263,
-0.0111276775841142));
#47363=CARTESIAN_POINT('Ctrl Pts',(-0.0116966226736852,-0.0360311475618236,
-0.011305046031054));
#47364=CARTESIAN_POINT('Ctrl Pts',(-0.0115920538498495,-0.0360208390958381,
-0.0114146857500023));
#47365=CARTESIAN_POINT('Ctrl Pts',(-0.0114264611124559,-0.0360015229937221,
-0.0116726962754399));
#47366=CARTESIAN_POINT('Ctrl Pts',(-0.01136907791787,-0.0359915139244068,
-0.0118199030163285));
#47367=CARTESIAN_POINT('Ctrl Pts',(-0.0113157648081405,-0.0359698213362853,
-0.0121258311067729));
#47368=CARTESIAN_POINT('Ctrl Pts',(-0.0113194081891567,-0.0359587970230021,
-0.0122813057367389));
#47369=CARTESIAN_POINT('Ctrl Pts',(-0.011385356716575,-0.0359378273196457,
-0.0125770390659802));
#47370=CARTESIAN_POINT('Ctrl Pts',(-0.0114451049974313,-0.0359286089360712,
-0.012714887258803));
#47371=CARTESIAN_POINT('Ctrl Pts',(-0.0116168474225842,-0.035909132270421,
-0.0129667750309259));
#47372=CARTESIAN_POINT('Ctrl Pts',(-0.0117294670069977,-0.0358983144293304,
-0.0130768377412685));
#47373=CARTESIAN_POINT('Ctrl Pts',(-0.0119879486539683,-0.0358764946783662,
-0.0132445773028502));
#47374=CARTESIAN_POINT('Ctrl Pts',(-0.0121305675837105,-0.0358657057712151,
-0.013301863518808));
#47375=CARTESIAN_POINT('Ctrl Pts',(-0.0124279931249051,-0.0358454335983883,
-0.0133584996418362));
#47376=CARTESIAN_POINT('Ctrl Pts',(-0.0125798203026902,-0.0358366175954246,
-0.0133579981003807));
#47377=CARTESIAN_POINT('Ctrl Pts',(-0.0128809190574449,-0.0358160218599593,
-0.0132985978360654));
#47378=CARTESIAN_POINT('Ctrl Pts',(-0.013026776606966,-0.0358049165633889,
-0.0132379970664895));
#47379=CARTESIAN_POINT('Ctrl Pts',(-0.0132812863836961,-0.0357832109116246,
-0.013066596279796));
#47380=CARTESIAN_POINT('Ctrl Pts',(-0.0133888252941528,-0.0357728043328982,
-0.0129593335562388));
#47381=CARTESIAN_POINT('Ctrl Pts',(-0.0135601350121641,-0.0357533126813555,
-0.0127062736247038));
#47382=CARTESIAN_POINT('Ctrl Pts',(-0.013620802551971,-0.0357436500957637,
-0.0125619297372353));
#47383=CARTESIAN_POINT('Ctrl Pts',(-0.0136824570305482,-0.0357221388215468,
-0.01225855869606));
#47384=CARTESIAN_POINT('Ctrl Pts',(-0.0136830809345521,-0.0357110811902516,
-0.0121026141859789));
#47385=CARTESIAN_POINT('Ctrl Pts',(-0.0136250240899294,-0.035689960300378,
-0.0118047486905688));
#47386=CARTESIAN_POINT('Ctrl Pts',(-0.0135689711989981,-0.0356804829095764,
-0.0116652954951538));
#47387=CARTESIAN_POINT('Ctrl Pts',(-0.0134040369024801,-0.0356612642993465,
-0.0114088943505184));
#47388=CARTESIAN_POINT('Ctrl Pts',(-0.0132944275724384,-0.0356505263238068,
-0.0112958703961299));
#47389=CARTESIAN_POINT('Ctrl Pts',(-0.0130402416050823,-0.0356287190275158,
-0.0111210417928692));
#47390=CARTESIAN_POINT('Ctrl Pts',(-0.0128988113017588,-0.035617864895353,
-0.0110598570937938));
#47391=CARTESIAN_POINT('Ctrl Pts',(-0.0126674192887738,-0.0356018724580381,
-0.0110095607862607));
#47392=CARTESIAN_POINT('Ctrl Pts',(-0.0125837461649245,-0.0355964170470507,
-0.0110006128129774));
#47393=CARTESIAN_POINT('Ctrl Pts',(-0.0125,-0.0355912743898722,-0.0110006128129774));
#47394=CARTESIAN_POINT('Ctrl Pts',(-0.0125000000000005,-0.0355287743898722,
-0.0110006128129774));
#47395=CARTESIAN_POINT('Ctrl Pts',(-0.0125352607803295,-0.0355309396723689,
-0.0110006128129774));
#47396=CARTESIAN_POINT('Ctrl Pts',(-0.0125705595312421,-0.0355331635441847,
-0.0110021996029348));
#47397=CARTESIAN_POINT('Ctrl Pts',(-0.0127559944899348,-0.0355451448907968,
-0.0110189599561776));
#47398=CARTESIAN_POINT('Ctrl Pts',(-0.0129021555048979,-0.0355556220749168,
-0.0110613187120238));
#47399=CARTESIAN_POINT('Ctrl Pts',(-0.0131757139460477,-0.0355773945099593,
-0.0112016099180018));
#47400=CARTESIAN_POINT('Ctrl Pts',(-0.0132994550792732,-0.0355884914708227,
-0.0113002823292377));
#47401=CARTESIAN_POINT('Ctrl Pts',(-0.0134966602349332,-0.0356089319691525,
-0.0115352530026169));
#47402=CARTESIAN_POINT('Ctrl Pts',(-0.0135701985822092,-0.0356177315824229,
-0.0116675456934071));
#47403=CARTESIAN_POINT('Ctrl Pts',(-0.013664364715511,-0.0356381230742689,
-0.0119551245718167));
#47404=CARTESIAN_POINT('Ctrl Pts',(-0.0136831514017129,-0.0356489605700093,
-0.0121079645353335));
#47405=CARTESIAN_POINT('Ctrl Pts',(-0.0136610422585882,-0.0356707727365856,
-0.0124155790270557));
#47406=CARTESIAN_POINT('Ctrl Pts',(-0.013619044184284,-0.0356815327234571,
-0.0125673258918548));
#47407=CARTESIAN_POINT('Ctrl Pts',(-0.0134814021934161,-0.0357008204286667,
-0.012839338193513));
#47408=CARTESIAN_POINT('Ctrl Pts',(-0.0133895245057508,-0.035710222753393,
-0.0129582436133824));
#47409=CARTESIAN_POINT('Ctrl Pts',(-0.0131621388582059,-0.0357313036319399,
-0.0131590025594084));
#47410=CARTESIAN_POINT('Ctrl Pts',(-0.0130274454060454,-0.0357423531566018,
-0.013237367023135));
#47411=CARTESIAN_POINT('Ctrl Pts',(-0.012734402148394,-0.0357639135612769,
-0.0133379290568871));
#47412=CARTESIAN_POINT('Ctrl Pts',(-0.0125788408017119,-0.035773663317448,
-0.0133586992261027));
#47413=CARTESIAN_POINT('Ctrl Pts',(-0.0122736417786934,-0.0357931082597812,
-0.0133388598427143));
#47414=CARTESIAN_POINT('Ctrl Pts',(-0.0121268166857713,-0.0358034890875824,
-0.0133003691079313));
#47415=CARTESIAN_POINT('Ctrl Pts',(-0.0118503981711957,-0.0358251693033963,
-0.0131676328089166));
#47416=CARTESIAN_POINT('Ctrl Pts',(-0.0117244118494424,-0.0358362765115161,
-0.013072560146511));
#47417=CARTESIAN_POINT('Ctrl Pts',(-0.011520737759579,-0.0358569263453031,
-0.0128428895278003));
#47418=CARTESIAN_POINT('Ctrl Pts',(-0.0114433966050415,-0.0358657557902617,
-0.0127120252506927));
#47419=CARTESIAN_POINT('Ctrl Pts',(-0.0113418062985382,-0.0358859857536244,
-0.0124267243900175));
#47420=CARTESIAN_POINT('Ctrl Pts',(-0.0113190928250837,-0.0358967567230716,
-0.0122748226392094));
#47421=CARTESIAN_POINT('Ctrl Pts',(-0.0113329888046075,-0.0359185770962935,
-0.0119670924101008));
#47422=CARTESIAN_POINT('Ctrl Pts',(-0.0113709445238759,-0.035929414185463,
-0.0118142581804075));
#47423=CARTESIAN_POINT('Ctrl Pts',(-0.0115013278036741,-0.0359489564107254,
-0.0115386564115406));
#47424=CARTESIAN_POINT('Ctrl Pts',(-0.0115900090416198,-0.0359581184087839,
-0.0114173686868488));
#47425=CARTESIAN_POINT('Ctrl Pts',(-0.011811665809368,-0.0359790489329139,
-0.0112109278922474));
#47426=CARTESIAN_POINT('Ctrl Pts',(-0.011943827653377,-0.0359900634554343,
-0.0111291658169776));
#47427=CARTESIAN_POINT('Ctrl Pts',(-0.0122199143932926,-0.0360106814687695,
-0.0110258151076541));
#47428=CARTESIAN_POINT('Ctrl Pts',(-0.0123594608525394,-0.0360201442077475,
-0.0110006128129774));
#47429=CARTESIAN_POINT('Ctrl Pts',(-0.0125000000000001,-0.0360287743898721,
-0.0110006128129774));
#47430=CARTESIAN_POINT('Origin',(-0.0125,-0.0332787743898722,-0.0121758532865583));
#47431=CARTESIAN_POINT('',(-0.0125000000000002,-0.0365912743898722,-0.0110006128129774));
#47432=CARTESIAN_POINT('',(-0.0125,-0.0365287743898721,-0.0110006128129774));
#47433=CARTESIAN_POINT('',(-0.0125,-0.0332787743898722,-0.0110006128129775));
#47434=CARTESIAN_POINT('Ctrl Pts',(-0.0125000000000005,-0.0365912743898722,
-0.0110006128129774));
#47435=CARTESIAN_POINT('Ctrl Pts',(-0.0123910159324724,-0.0365845819318031,
-0.0110006128129773));
#47436=CARTESIAN_POINT('Ctrl Pts',(-0.0122823814488855,-0.036577373740337,
-0.0110157649684074));
#47437=CARTESIAN_POINT('Ctrl Pts',(-0.0120280106007402,-0.0365591770328985,
-0.0110884339050792));
#47438=CARTESIAN_POINT('Ctrl Pts',(-0.0118887595288113,-0.0365480830408749,
-0.0111601585760449));
#47439=CARTESIAN_POINT('Ctrl Pts',(-0.0116506050560141,-0.0365267283069574,
-0.0113499896715688));
#47440=CARTESIAN_POINT('Ctrl Pts',(-0.0115526507348646,-0.036516713373673,
-0.011464518064052));
#47441=CARTESIAN_POINT('Ctrl Pts',(-0.0114016238544625,-0.0364979109941513,
-0.0117296858730143));
#47442=CARTESIAN_POINT('Ctrl Pts',(-0.0113522108068163,-0.0364873147643931,
-0.0118791232899648));
#47443=CARTESIAN_POINT('Ctrl Pts',(-0.0113148510144864,-0.0364655594486451,
-0.0121859360209553));
#47444=CARTESIAN_POINT('Ctrl Pts',(-0.0113262625624588,-0.0364546173849002,
-0.0123402506950854));
#47445=CARTESIAN_POINT('Ctrl Pts',(-0.011406624700875,-0.036433935792472,
-0.0126319208288421));
#47446=CARTESIAN_POINT('Ctrl Pts',(-0.0114732936437026,-0.0364250339442455,
-0.0127668984933356));
#47447=CARTESIAN_POINT('Ctrl Pts',(-0.0116585957038017,-0.0364049886306321,
-0.0130113394432357));
#47448=CARTESIAN_POINT('Ctrl Pts',(-0.0117779956413319,-0.0363939305998197,
-0.0131164329738666));
#47449=CARTESIAN_POINT('Ctrl Pts',(-0.0120458313213491,-0.0363720275650022,
-0.013270319960279));
#47450=CARTESIAN_POINT('Ctrl Pts',(-0.012190524267742,-0.0363613918846556,
-0.0133196919938076));
#47451=CARTESIAN_POINT('Ctrl Pts',(-0.0124913697293818,-0.0363414577344296,
-0.0133608704526666));
#47452=CARTESIAN_POINT('Ctrl Pts',(-0.0126446562435927,-0.0363324250092816,
-0.013352042118004));
#47453=CARTESIAN_POINT('Ctrl Pts',(-0.0129427148659104,-0.0363114108653244,
-0.0132755746555834));
#47454=CARTESIAN_POINT('Ctrl Pts',(-0.0130842049671664,-0.0363003051179879,
-0.0132073965295047));
#47455=CARTESIAN_POINT('Ctrl Pts',(-0.0133277502173527,-0.0362788280763752,
-0.0130234527514248));
#47456=CARTESIAN_POINT('Ctrl Pts',(-0.0134288980729769,-0.0362686378228613,
-0.0129112220156681));
#47457=CARTESIAN_POINT('Ctrl Pts',(-0.0135867608199831,-0.0362496677210636,
-0.0126495819600103));
#47458=CARTESIAN_POINT('Ctrl Pts',(-0.0136399664581206,-0.036239359446599,
-0.0125014192025588));
#47459=CARTESIAN_POINT('Ctrl Pts',(-0.0136850836135262,-0.0362176404152308,
-0.0121951181860278));
#47460=CARTESIAN_POINT('Ctrl Pts',(-0.0136774522781934,-0.0362066548093585,
-0.0120401894422534));
#47461=CARTESIAN_POINT('Ctrl Pts',(-0.0136041153929361,-0.0361858308806997,
-0.0117465119569074));
#47462=CARTESIAN_POINT('Ctrl Pts',(-0.0135408491767724,-0.0361768006977145,
-0.0116101446405585));
#47463=CARTESIAN_POINT('Ctrl Pts',(-0.0133626568531267,-0.036157082734181,
-0.0113626224274056));
#47464=CARTESIAN_POINT('Ctrl Pts',(-0.013247245286305,-0.036146196223676,
-0.0112554586986463));
#47465=CARTESIAN_POINT('Ctrl Pts',(-0.0129848554626663,-0.0361243794529055,
-0.0110945723562825));
#47466=CARTESIAN_POINT('Ctrl Pts',(-0.0128412022424354,-0.0361136593901614,
-0.011041019393603));
#47467=CARTESIAN_POINT('Ctrl Pts',(-0.012627932464109,-0.0360993154528448,
-0.0110058316689456));
#47468=CARTESIAN_POINT('Ctrl Pts',(-0.0125639527294939,-0.0360952015782241,
-0.0110006128129774));
#47469=CARTESIAN_POINT('Ctrl Pts',(-0.0125,-0.0360912743898722,-0.0110006128129774));
#47470=CARTESIAN_POINT('Ctrl Pts',(-0.0125000000000001,-0.0360287743898721,
-0.0110006128129774));
#47471=CARTESIAN_POINT('Ctrl Pts',(-0.0125159710528335,-0.0360297551350749,
-0.0110006128129774));
#47472=CARTESIAN_POINT('Ctrl Pts',(-0.0125319535331271,-0.0360307481242455,
-0.0110009383705918));
#47473=CARTESIAN_POINT('Ctrl Pts',(-0.0126978941423195,-0.0360411783251345,
-0.0110077126660084));
#47474=CARTESIAN_POINT('Ctrl Pts',(-0.0128452591868545,-0.0360514610293382,
-0.011042500525408));
#47475=CARTESIAN_POINT('Ctrl Pts',(-0.013124220810136,-0.0360730396778832,
-0.0111679672477668));
#47476=CARTESIAN_POINT('Ctrl Pts',(-0.0132522584585505,-0.036084149314727,
-0.011259555412206));
#47477=CARTESIAN_POINT('Ctrl Pts',(-0.0134620710591082,-0.0361049940698633,
-0.0114840917255256));
#47478=CARTESIAN_POINT('Ctrl Pts',(-0.0135430702704042,-0.0361139072157517,
-0.0116136110874333));
#47479=CARTESIAN_POINT('Ctrl Pts',(-0.0136516603585244,-0.036133981516931,
-0.011896716662131));
#47480=CARTESIAN_POINT('Ctrl Pts',(-0.0136780436136455,-0.0361446833036546,
-0.0120476427368969));
#47481=CARTESIAN_POINT('Ctrl Pts',(-0.0136718829591347,-0.036166497058621,
-0.0123552796295048));
#47482=CARTESIAN_POINT('Ctrl Pts',(-0.0136377657036639,-0.0361773996416091,
-0.0125090375110348));
#47483=CARTESIAN_POINT('Ctrl Pts',(-0.0135142640645741,-0.0361971773939341,
-0.0127879608911405));
#47484=CARTESIAN_POINT('Ctrl Pts',(-0.0134285562951811,-0.0362061692572171,
-0.0129115166694147));
#47485=CARTESIAN_POINT('Ctrl Pts',(-0.0132122586389499,-0.0362269563897444,
-0.0131231952466817));
#47486=CARTESIAN_POINT('Ctrl Pts',(-0.0130825270295917,-0.0362379312655106,
-0.0132080483445592));
#47487=CARTESIAN_POINT('Ctrl Pts',(-0.0127955530036067,-0.0362596633872245,
-0.0133239660074586));
#47488=CARTESIAN_POINT('Ctrl Pts',(-0.0126408357058475,-0.036270059136913,
-0.0133529795944559));
#47489=CARTESIAN_POINT('Ctrl Pts',(-0.0123354049479832,-0.0362889526234046,
-0.0133490958249835));
#47490=CARTESIAN_POINT('Ctrl Pts',(-0.0121875277880686,-0.0362991137265824,
-0.0133186248261753));
#47491=CARTESIAN_POINT('Ctrl Pts',(-0.0119058402015021,-0.0363205576805671,
-0.0132016787746938));
#47492=CARTESIAN_POINT('Ctrl Pts',(-0.0117755311350052,-0.0363316611044815,
-0.0131142000622447));
#47493=CARTESIAN_POINT('Ctrl Pts',(-0.0115586245092616,-0.0363527261250893,
-0.0128957382034486));
#47494=CARTESIAN_POINT('Ctrl Pts',(-0.0114733255896075,-0.0363618036710384,
-0.0127677615363021));
#47495=CARTESIAN_POINT('Ctrl Pts',(-0.011356692714163,-0.0363816947711399,
-0.0124872396254632));
#47496=CARTESIAN_POINT('Ctrl Pts',(-0.01132613730169,-0.036392309467934,
-0.0123375417700171));
#47497=CARTESIAN_POINT('Ctrl Pts',(-0.0113234200773491,-0.0364141970386679,
-0.0120288638620781));
#47498=CARTESIAN_POINT('Ctrl Pts',(-0.0113536446109233,-0.0364252621359081,
-0.011872814060629));
#47499=CARTESIAN_POINT('Ctrl Pts',(-0.0114706989202091,-0.0364453642075344,
-0.011589316842492));
#47500=CARTESIAN_POINT('Ctrl Pts',(-0.0115534420207808,-0.0364542391830359,
-0.0114634493033982));
#47501=CARTESIAN_POINT('Ctrl Pts',(-0.0117643758445707,-0.0364748802581914,
-0.0112465999566501));
#47502=CARTESIAN_POINT('Ctrl Pts',(-0.0118916190719469,-0.0364858089497747,
-0.0111587395152585));
#47503=CARTESIAN_POINT('Ctrl Pts',(-0.0121750606586413,-0.0365075756620527,
-0.011035727834487));
#47504=CARTESIAN_POINT('Ctrl Pts',(-0.0123289643669752,-0.0365181968274219,
-0.0110027187147509));
#47505=CARTESIAN_POINT('Ctrl Pts',(-0.0124899082346748,-0.0365281535261902,
-0.0110006453017553));
#47506=CARTESIAN_POINT('Ctrl Pts',(-0.0124949547290055,-0.0365284645715166,
-0.0110006128129774));
#47507=CARTESIAN_POINT('Ctrl Pts',(-0.0125,-0.0365287743898721,-0.0110006128129774));
#47508=CARTESIAN_POINT('Origin',(-0.0125,-0.0332787743898722,-0.0121758532865583));
#47509=CARTESIAN_POINT('',(-0.0125000000000002,-0.0370912743898722,-0.0110006128129773));
#47510=CARTESIAN_POINT('',(-0.0124999999999998,-0.0370287743898721,-0.0110006128129773));
#47511=CARTESIAN_POINT('',(-0.0125,-0.0332787743898722,-0.0110006128129775));
#47512=CARTESIAN_POINT('Ctrl Pts',(-0.0125000000000003,-0.0370912743898722,
-0.0110006128129773));
#47513=CARTESIAN_POINT('Ctrl Pts',(-0.0123685975923388,-0.0370832052736848,
-0.0110006128129773));
#47514=CARTESIAN_POINT('Ctrl Pts',(-0.0122379669078175,-0.0370744025225916,
-0.0110226422150859));
#47515=CARTESIAN_POINT('Ctrl Pts',(-0.0119678246142031,-0.0370544785569455,
-0.0111167128569917));
#47516=CARTESIAN_POINT('Ctrl Pts',(-0.011833539781003,-0.0370434342199873,
-0.0111956387463349));
#47517=CARTESIAN_POINT('Ctrl Pts',(-0.0116070898289398,-0.037022377685569,
-0.0113973317195526));
#47518=CARTESIAN_POINT('Ctrl Pts',(-0.0115157356944448,-0.0370130187127627,
-0.0115166234445081));
#47519=CARTESIAN_POINT('Ctrl Pts',(-0.0113792725155753,-0.0369936892534286,
-0.0117892245998102));
#47520=CARTESIAN_POINT('Ctrl Pts',(-0.0113379302073818,-0.0369829161845667,
-0.0119411559584241));
#47521=CARTESIAN_POINT('Ctrl Pts',(-0.0113171581777985,-0.0369611016134194,
-0.0122488043615369));
#47522=CARTESIAN_POINT('Ctrl Pts',(-0.011336586286407,-0.0369502744617805,
-0.0124014984433715));
#47523=CARTESIAN_POINT('Ctrl Pts',(-0.0114319609518788,-0.036929909022047,
-0.0126887099118166));
#47524=CARTESIAN_POINT('Ctrl Pts',(-0.0115061132334518,-0.0369211086252034,
-0.0128207699478459));
#47525=CARTESIAN_POINT('Ctrl Pts',(-0.0117043682898292,-0.0369006338935512,
-0.0130548877171049));
#47526=CARTESIAN_POINT('Ctrl Pts',(-0.0118284795125062,-0.0368895347393193,
-0.0131529809802588));
#47527=CARTESIAN_POINT('Ctrl Pts',(-0.0121025144857545,-0.0368677762466659,
-0.0132920535525929));
#47528=CARTESIAN_POINT('Ctrl Pts',(-0.0122487898210647,-0.0368573142119794,
-0.0133337869983317));
#47529=CARTESIAN_POINT('Ctrl Pts',(-0.0125527314161703,-0.036837720222863,
-0.0133600082902373));
#47530=CARTESIAN_POINT('Ctrl Pts',(-0.0127075865527121,-0.0368282354164281,
-0.0133428699125894));
#47531=CARTESIAN_POINT('Ctrl Pts',(-0.0130022365098488,-0.0368068340239882,
-0.0132495758267264));
#47532=CARTESIAN_POINT('Ctrl Pts',(-0.0131390542732378,-0.0367957606001123,
-0.0131742166822104));
#47533=CARTESIAN_POINT('Ctrl Pts',(-0.0133713796489952,-0.0367745526274465,
-0.0129784288087641));
#47534=CARTESIAN_POINT('Ctrl Pts',(-0.0134660322655738,-0.0367648951321246,
-0.0128615460563626));
#47535=CARTESIAN_POINT('Ctrl Pts',(-0.0136098548297126,-0.0367458289813388,
-0.0125926583114163));
#47536=CARTESIAN_POINT('Ctrl Pts',(-0.0136552848518729,-0.0367351411395208,
-0.01244192890006));
#47537=CARTESIAN_POINT('Ctrl Pts',(-0.0136844222710554,-0.0367133484465393,
-0.0121345890422173));
#47538=CARTESIAN_POINT('Ctrl Pts',(-0.013669020831319,-0.0367024596930923,
-0.0119810261971247));
#47539=CARTESIAN_POINT('Ctrl Pts',(-0.0135812101027114,-0.0366819329301478,
-0.011691539605877));
#47540=CARTESIAN_POINT('Ctrl Pts',(-0.0135108662789414,-0.0366731114162018,
-0.0115580175121104));
#47541=CARTESIAN_POINT('Ctrl Pts',(-0.0133191621693466,-0.0366528519710482,
-0.0113186254919463));
#47542=CARTESIAN_POINT('Ctrl Pts',(-0.0131973946833203,-0.0366417698145867,
-0.0112169521930585));
#47543=CARTESIAN_POINT('Ctrl Pts',(-0.012926408855032,-0.0366199307819255,
-0.0110703266536913));
#47544=CARTESIAN_POINT('Ctrl Pts',(-0.0127808874148052,-0.0366093773287217,
-0.0110247088935657));
#47545=CARTESIAN_POINT('Ctrl Pts',(-0.012587214336645,-0.0365967159688182,
-0.0110030370823802));
#47546=CARTESIAN_POINT('Ctrl Pts',(-0.0125435845119462,-0.0365939508133649,
-0.0110006128129774));
#47547=CARTESIAN_POINT('Ctrl Pts',(-0.0125000000000005,-0.0365912743898722,
-0.0110006128129774));
#47548=CARTESIAN_POINT('Ctrl Pts',(-0.0125,-0.0365287743898721,-0.0110006128129774));
#47549=CARTESIAN_POINT('Ctrl Pts',(-0.012644057324453,-0.0365376206150619,
-0.0110006128129774));
#47550=CARTESIAN_POINT('Ctrl Pts',(-0.0127870035996141,-0.0365473376160089,
-0.0110270981087197));
#47551=CARTESIAN_POINT('Ctrl Pts',(-0.0130663655501122,-0.0365682998844921,
-0.0111344859689061));
#47552=CARTESIAN_POINT('Ctrl Pts',(-0.0131986298923942,-0.0365793892413662,
-0.0112181812726274));
#47553=CARTESIAN_POINT('Ctrl Pts',(-0.0134219398439058,-0.0366006481927421,
-0.0114310222127636));
#47554=CARTESIAN_POINT('Ctrl Pts',(-0.0135111919474361,-0.0366099362468724,
-0.0115576089672795));
#47555=CARTESIAN_POINT('Ctrl Pts',(-0.013635047801415,-0.0366296588464219,
-0.0118357545340962));
#47556=CARTESIAN_POINT('Ctrl Pts',(-0.0136693042393584,-0.0366401885685552,
-0.0119842540016153));
#47557=CARTESIAN_POINT('Ctrl Pts',(-0.0136799717532264,-0.0366620075578438,
-0.0122919647132708));
#47558=CARTESIAN_POINT('Ctrl Pts',(-0.0136539438670768,-0.0366730950308132,
-0.0124483300770714));
#47559=CARTESIAN_POINT('Ctrl Pts',(-0.0135445649441898,-0.036693412455111,
-0.0127348643893149));
#47560=CARTESIAN_POINT('Ctrl Pts',(-0.0134649510895904,-0.0367022222555921,
-0.0128632260770478));
#47561=CARTESIAN_POINT('Ctrl Pts',(-0.013259691741225,-0.0367227061503151,
-0.0130854705081921));
#47562=CARTESIAN_POINT('Ctrl Pts',(-0.0131351373811488,-0.0367335791151055,
-0.0131764163871841));
#47563=CARTESIAN_POINT('Ctrl Pts',(-0.0128554348450942,-0.0367553792705709,
-0.0133068475845299));
#47564=CARTESIAN_POINT('Ctrl Pts',(-0.012702441844019,-0.0367660907526982,
-0.0133439815493386));
#47565=CARTESIAN_POINT('Ctrl Pts',(-0.0123977835902895,-0.0367852279905299,
-0.0133560785297924));
#47566=CARTESIAN_POINT('Ctrl Pts',(-0.0122491209316249,-0.0367947990505451,
-0.0133336411379627));
#47567=CARTESIAN_POINT('Ctrl Pts',(-0.0119628073437893,-0.0368159666251517,
-0.0132325030492665));
#47568=CARTESIAN_POINT('Ctrl Pts',(-0.0118286330905472,-0.0368270330427736,
-0.0131527628276649));
#47569=CARTESIAN_POINT('Ctrl Pts',(-0.0115987499446077,-0.0368484859204106,
-0.012945837154466));
#47570=CARTESIAN_POINT('Ctrl Pts',(-0.0115053631408727,-0.0368580511205173,
-0.012820683327321));
#47571=CARTESIAN_POINT('Ctrl Pts',(-0.0113741223718986,-0.0368775975153528,
-0.0125450227554419));
#47572=CARTESIAN_POINT('Ctrl Pts',(-0.0113361318600384,-0.0368880339276796,
-0.0123978392254569));
#47573=CARTESIAN_POINT('Ctrl Pts',(-0.0113174022638658,-0.0369097683479152,
-0.0120913211814888));
#47574=CARTESIAN_POINT('Ctrl Pts',(-0.0113391542897758,-0.0369208706975362,
-0.0119347460139715));
#47575=CARTESIAN_POINT('Ctrl Pts',(-0.0114406711066737,-0.0369414021390191,
-0.0116451934418326));
#47576=CARTESIAN_POINT('Ctrl Pts',(-0.0115171160639166,-0.0369502073678009,
-0.0115142513591822));
#47577=CARTESIAN_POINT('Ctrl Pts',(-0.0117166261953091,-0.0369705293043836,
-0.0112866171464137));
#47578=CARTESIAN_POINT('Ctrl Pts',(-0.0118384023485465,-0.0369813388560223,
-0.0111926478888798));
#47579=CARTESIAN_POINT('Ctrl Pts',(-0.0121141467720003,-0.037003156502872,
-0.0110548676814199));
#47580=CARTESIAN_POINT('Ctrl Pts',(-0.0122661085524211,-0.0370139508462579,
-0.0110136104243289));
#47581=CARTESIAN_POINT('Ctrl Pts',(-0.0124478103935037,-0.0370255387636812,
-0.0110014810954639));
#47582=CARTESIAN_POINT('Ctrl Pts',(-0.012473917137073,-0.0370271727019334,
-0.0110006128129773));
#47583=CARTESIAN_POINT('Ctrl Pts',(-0.0124999999999997,-0.0370287743898721,
-0.0110006128129773));
#47584=CARTESIAN_POINT('Origin',(-0.0125,-0.0332787743898722,-0.0121758532865583));
#47585=CARTESIAN_POINT('',(-0.0125,-0.0375912743898721,-0.0110006128129773));
#47586=CARTESIAN_POINT('',(-0.0124999999999998,-0.037528774389872,-0.0110006128129773));
#47587=CARTESIAN_POINT('',(-0.0125,-0.0332787743898722,-0.0110006128129775));
#47588=CARTESIAN_POINT('Ctrl Pts',(-0.0125,-0.0375912743898721,-0.0110006128129773));
#47589=CARTESIAN_POINT('Ctrl Pts',(-0.0124966408622287,-0.0375910681130356,
-0.0110006128129773));
#47590=CARTESIAN_POINT('Ctrl Pts',(-0.0124932811404291,-0.0375908612897337,
-0.0110006272148874));
#47591=CARTESIAN_POINT('Ctrl Pts',(-0.0123403235283202,-0.0375814220089463,
-0.0110019390550596));
#47592=CARTESIAN_POINT('Ctrl Pts',(-0.0121923815235324,-0.0375712794821269,
-0.0110317737787349));
#47593=CARTESIAN_POINT('Ctrl Pts',(-0.0119103137976082,-0.0375498568575994,
-0.0111474597957408));
#47594=CARTESIAN_POINT('Ctrl Pts',(-0.0117796808171522,-0.037538755169121,
-0.0112343285234444));
#47595=CARTESIAN_POINT('Ctrl Pts',(-0.0115617337990316,-0.0375176583154644,
-0.0114518862454815));
#47596=CARTESIAN_POINT('Ctrl Pts',(-0.0114757973806388,-0.0375085505706955,
-0.0115796371412965));
#47597=CARTESIAN_POINT('Ctrl Pts',(-0.0113579887363392,-0.0374886866424524,
-0.011859775850523));
#47598=CARTESIAN_POINT('Ctrl Pts',(-0.011326827768129,-0.0374780853466678,
-0.0120092847130642));
#47599=CARTESIAN_POINT('Ctrl Pts',(-0.0113228124329801,-0.0374562079777241,
-0.0123178187463206));
#47600=CARTESIAN_POINT('Ctrl Pts',(-0.0113523530815602,-0.0374451387087904,
-0.0124739273806864));
#47601=CARTESIAN_POINT('Ctrl Pts',(-0.0114681589190712,-0.0374250011824154,
-0.012757924613091));
#47602=CARTESIAN_POINT('Ctrl Pts',(-0.0115503903526256,-0.037416140972307,
-0.0128841962096427));
#47603=CARTESIAN_POINT('Ctrl Pts',(-0.0117603969781781,-0.0373955253953266,
-0.0131019323151485));
#47604=CARTESIAN_POINT('Ctrl Pts',(-0.0118872046835685,-0.0373846053327843,
-0.0131903037139901));
#47605=CARTESIAN_POINT('Ctrl Pts',(-0.0121700470964044,-0.0373628320434691,
-0.0133145387047329));
#47606=CARTESIAN_POINT('Ctrl Pts',(-0.012323809423536,-0.0373521955392449,
-0.0133482253481312));
#47607=CARTESIAN_POINT('Ctrl Pts',(-0.0126288105206927,-0.0373332793246859,
-0.0133534943744511));
#47608=CARTESIAN_POINT('Ctrl Pts',(-0.0127771338405923,-0.0373234256615799,
-0.0133276665041483));
#47609=CARTESIAN_POINT('Ctrl Pts',(-0.013060582622869,-0.0373022087885629,
-0.0132201759269938));
#47610=CARTESIAN_POINT('Ctrl Pts',(-0.0131923450799375,-0.0372912003904165,
-0.0131378948349357));
#47611=CARTESIAN_POINT('Ctrl Pts',(-0.013413112214115,-0.0372702934898366,
-0.0129305794702442));
#47612=CARTESIAN_POINT('Ctrl Pts',(-0.0135012988579798,-0.0372611634086988,
-0.0128089179874886));
#47613=CARTESIAN_POINT('Ctrl Pts',(-0.0136305459609977,-0.0372415819072085,
-0.0125327623104696));
#47614=CARTESIAN_POINT('Ctrl Pts',(-0.0136678681958573,-0.0372307334953414,
-0.0123797683980664));
#47615=CARTESIAN_POINT('Ctrl Pts',(-0.0136804833451595,-0.0372089132558917,
-0.0120720400555337));
#47616=CARTESIAN_POINT('Ctrl Pts',(-0.0136571603139226,-0.037198153304402,
-0.0119202936897192));
#47617=CARTESIAN_POINT('Ctrl Pts',(-0.0135544116682296,-0.0371779488572334,
-0.011635352681013));
#47618=CARTESIAN_POINT('Ctrl Pts',(-0.0134764704145116,-0.0371691093436274,
-0.0115047113528514));
#47619=CARTESIAN_POINT('Ctrl Pts',(-0.0132717829635454,-0.0371484270651985,
-0.0112758808009031));
#47620=CARTESIAN_POINT('Ctrl Pts',(-0.0131454526554889,-0.0371373189630884,
-0.0111813787245666));
#47621=CARTESIAN_POINT('Ctrl Pts',(-0.0128686027709003,-0.0371156545638149,
-0.0110498356980546));
#47622=CARTESIAN_POINT('Ctrl Pts',(-0.0127216824450164,-0.0371052894822773,
-0.0110119540471123));
#47623=CARTESIAN_POINT('Ctrl Pts',(-0.0125477199530562,-0.0370942304977055,
-0.0110013387314271));
#47624=CARTESIAN_POINT('Ctrl Pts',(-0.0125238488275897,-0.0370927388908975,
-0.0110006128129773));
#47625=CARTESIAN_POINT('Ctrl Pts',(-0.0125000000000003,-0.0370912743898722,
-0.0110006128129773));
#47626=CARTESIAN_POINT('Ctrl Pts',(-0.0124999999999997,-0.0370287743898721,
-0.0110006128129773));
#47627=CARTESIAN_POINT('Ctrl Pts',(-0.0126224476628745,-0.0370362936160126,
-0.0110006128129773));
#47628=CARTESIAN_POINT('Ctrl Pts',(-0.0127442864279888,-0.037044453621814,
-0.0110197411394502));
#47629=CARTESIAN_POINT('Ctrl Pts',(-0.0130078504536451,-0.0370636559755463,
-0.0111048520550244));
#47630=CARTESIAN_POINT('Ctrl Pts',(-0.0131438051915405,-0.0370746912530215,
-0.0111806300548851));
#47631=CARTESIAN_POINT('Ctrl Pts',(-0.013380158569642,-0.0370963295804707,
-0.0113815797122461));
#47632=CARTESIAN_POINT('Ctrl Pts',(-0.0134776962594941,-0.0371062277278314,
-0.0115053081471911));
#47633=CARTESIAN_POINT('Ctrl Pts',(-0.0136161835651565,-0.0371255972993,
-0.0117784749993407));
#47634=CARTESIAN_POINT('Ctrl Pts',(-0.0136577846176067,-0.0371359360257146,
-0.0119242808760732));
#47635=CARTESIAN_POINT('Ctrl Pts',(-0.0136843498331268,-0.0371575735251978,
-0.0122294320577491));
#47636=CARTESIAN_POINT('Ctrl Pts',(-0.0136667734166237,-0.0371686826771268,
-0.0123861031574389));
#47637=CARTESIAN_POINT('Ctrl Pts',(-0.0135729847832567,-0.0371894182276145,
-0.0126785342555404));
#47638=CARTESIAN_POINT('Ctrl Pts',(-0.0134996307059135,-0.037198277582668,
-0.0128120303918967));
#47639=CARTESIAN_POINT('Ctrl Pts',(-0.0133057084576302,-0.037218439798747,
-0.0130448380621064));
#47640=CARTESIAN_POINT('Ctrl Pts',(-0.0131866808977871,-0.0372291812321277,
-0.0131416466950343));
#47641=CARTESIAN_POINT('Ctrl Pts',(-0.0129149399853398,-0.0372510004198648,
-0.0132864046488839));
#47642=CARTESIAN_POINT('Ctrl Pts',(-0.0127640820083308,-0.0372618670604148,
-0.0133316129468484));
#47643=CARTESIAN_POINT('Ctrl Pts',(-0.0124604504641844,-0.0372815129854695,
-0.0133598361559728));
#47644=CARTESIAN_POINT('Ctrl Pts',(-0.0123108671398517,-0.0372905937650852,
-0.0133453068884122));
#47645=CARTESIAN_POINT('Ctrl Pts',(-0.012019245236608,-0.0373115470184224,
-0.0132594081683051));
#47646=CARTESIAN_POINT('Ctrl Pts',(-0.0118806865943221,-0.0373226359432046,
-0.0131866270995324));
#47647=CARTESIAN_POINT('Ctrl Pts',(-0.0116442109327482,-0.0373439487779304,
-0.012995070016698));
#47648=CARTESIAN_POINT('Ctrl Pts',(-0.0115472108189611,-0.037353854567675,
-0.0128798668323187));
#47649=CARTESIAN_POINT('Ctrl Pts',(-0.0113982492115195,-0.0373727331647398,
-0.0126136241360601));
#47650=CARTESIAN_POINT('Ctrl Pts',(-0.0113499757176555,-0.0373833564818653,
-0.0124638047090652));
#47651=CARTESIAN_POINT('Ctrl Pts',(-0.0113149756787381,-0.0374051241371581,
-0.0121568179548843));
#47652=CARTESIAN_POINT('Ctrl Pts',(-0.011327535565838,-0.0374160516372124,
-0.0120027086708183));
#47653=CARTESIAN_POINT('Ctrl Pts',(-0.0114100374733141,-0.0374366891624931,
-0.011711660011005));
#47654=CARTESIAN_POINT('Ctrl Pts',(-0.011477754783642,-0.037445561983475,
-0.0115771022701026));
#47655=CARTESIAN_POINT('Ctrl Pts',(-0.0116648908044211,-0.0374656690033175,
-0.011334097361487));
#47656=CARTESIAN_POINT('Ctrl Pts',(-0.0117849765197717,-0.0374767346940491,
-0.0112299755789547));
#47657=CARTESIAN_POINT('Ctrl Pts',(-0.0120537314192286,-0.0374986208661648,
-0.011078156352826));
#47658=CARTESIAN_POINT('Ctrl Pts',(-0.0121986708078293,-0.0375092337062857,
-0.0110298553959062));
#47659=CARTESIAN_POINT('Ctrl Pts',(-0.0123990475439641,-0.0375224599652766,
-0.0110038612464219));
#47660=CARTESIAN_POINT('Ctrl Pts',(-0.0124495468686633,-0.0375256761804403,
-0.0110006128129773));
#47661=CARTESIAN_POINT('Ctrl Pts',(-0.0124999999999997,-0.037528774389872,
-0.0110006128129773));
#47662=CARTESIAN_POINT('Origin',(-0.0125,-0.0332787743898722,-0.0121758532865583));
#47663=CARTESIAN_POINT('',(-0.0124999999999998,-0.0380912743898721,-0.0110006128129773));
#47664=CARTESIAN_POINT('',(-0.0125,-0.0380287743898721,-0.0110006128129773));
#47665=CARTESIAN_POINT('',(-0.0125,-0.0332787743898722,-0.0110006128129775));
#47666=CARTESIAN_POINT('Ctrl Pts',(-0.0124999999999997,-0.0380912743898721,
-0.0110006128129773));
#47667=CARTESIAN_POINT('Ctrl Pts',(-0.0124762424888991,-0.0380898154963799,
-0.0110006128129773));
#47668=CARTESIAN_POINT('Ctrl Pts',(-0.0124524628126795,-0.0380883297019628,
-0.0110013331832036));
#47669=CARTESIAN_POINT('Ctrl Pts',(-0.0122785928628455,-0.0380772780454556,
-0.011011902092839));
#47670=CARTESIAN_POINT('Ctrl Pts',(-0.0121316670101472,-0.0380669138956383,
-0.0110497478911719));
#47671=CARTESIAN_POINT('Ctrl Pts',(-0.0118547918942762,-0.0380452504383218,
-0.0111812206471982));
#47672=CARTESIAN_POINT('Ctrl Pts',(-0.0117284414188247,-0.0380341422896691,
-0.0112756891053517));
#47673=CARTESIAN_POINT('Ctrl Pts',(-0.0115236943642097,-0.0380134581061522,
-0.0115044701552302));
#47674=CARTESIAN_POINT('Ctrl Pts',(-0.0114457177685337,-0.0380046179541512,
-0.0116350983828561));
#47675=CARTESIAN_POINT('Ctrl Pts',(-0.0113429010274434,-0.0379844150100093,
-0.0119200181945472));
#47676=CARTESIAN_POINT('Ctrl Pts',(-0.0113195421890426,-0.0379736557115737,
-0.0120717553504145));
#47677=CARTESIAN_POINT('Ctrl Pts',(-0.0113320820491274,-0.0379518354918623,
-0.0123794834145812));
#47678=CARTESIAN_POINT('Ctrl Pts',(-0.0113693670208866,-0.0379409864203264,
-0.0125324866302184));
#47679=CARTESIAN_POINT('Ctrl Pts',(-0.0114985472991291,-0.0379214026135655,
-0.0128086748182053));
#47680=CARTESIAN_POINT('Ctrl Pts',(-0.0115867048996421,-0.0379122743621264,
-0.0129303582918763));
#47681=CARTESIAN_POINT('Ctrl Pts',(-0.0118074197690923,-0.0378913688516608,
-0.013137724972483));
#47682=CARTESIAN_POINT('Ctrl Pts',(-0.0119391587116199,-0.0378803608189864,
-0.0132200364834926));
#47683=CARTESIAN_POINT('Ctrl Pts',(-0.0122299052169146,-0.037858594732115,
-0.0133303780340251));
#47684=CARTESIAN_POINT('Ctrl Pts',(-0.0123864346840221,-0.0378484250732582,
-0.013356083403582));
#47685=CARTESIAN_POINT('Ctrl Pts',(-0.0126932523815696,-0.0378291827723794,
-0.0133447633052546));
#47686=CARTESIAN_POINT('Ctrl Pts',(-0.0128406964987416,-0.0378189165812173,
-0.0133105781667553));
#47687=CARTESIAN_POINT('Ctrl Pts',(-0.0131200541284824,-0.0377973556880612,
-0.0131862981521401));
#47688=CARTESIAN_POINT('Ctrl Pts',(-0.013248416655367,-0.0377862463352569,
-0.0130952807052713));
#47689=CARTESIAN_POINT('Ctrl Pts',(-0.0134592235887506,-0.0377653703768205,
-0.0128715865137773));
#47690=CARTESIAN_POINT('Ctrl Pts',(-0.0135408206552691,-0.0377564385561343,
-0.0127422839319029));
#47691=CARTESIAN_POINT('Ctrl Pts',(-0.0136505409160875,-0.037736389717793,
-0.0124595374567003));
#47692=CARTESIAN_POINT('Ctrl Pts',(-0.0136775134542161,-0.0377256996822031,
-0.0123087771068284));
#47693=CARTESIAN_POINT('Ctrl Pts',(-0.0136726003590957,-0.0377038882999825,
-0.0120011736767842));
#47694=CARTESIAN_POINT('Ctrl Pts',(-0.013639105015219,-0.0376929758033051,
-0.0118472759836266));
#47695=CARTESIAN_POINT('Ctrl Pts',(-0.0135167180201757,-0.0376731604377815,
-0.0115678221488813));
#47696=CARTESIAN_POINT('Ctrl Pts',(-0.0134314870394243,-0.0376641909579558,
-0.0114438979822576));
#47697=CARTESIAN_POINT('Ctrl Pts',(-0.0132160508428487,-0.0376434271143786,
-0.0112313841959012));
#47698=CARTESIAN_POINT('Ctrl Pts',(-0.0130867152099326,-0.0376324592223532,
-0.0111460422285071));
#47699=CARTESIAN_POINT('Ctrl Pts',(-0.0128033956951292,-0.0376109556656038,
-0.0110302416176938));
#47700=CARTESIAN_POINT('Ctrl Pts',(-0.0126523623669168,-0.0376006306084005,
-0.0110006128129773));
#47701=CARTESIAN_POINT('Ctrl Pts',(-0.0125,-0.0375912743898721,-0.0110006128129773));
#47702=CARTESIAN_POINT('Ctrl Pts',(-0.0124999999999997,-0.037528774389872,
-0.0110006128129773));
#47703=CARTESIAN_POINT('Ctrl Pts',(-0.0126013419560833,-0.0375349975636544,
-0.0110006128129773));
#47704=CARTESIAN_POINT('Ctrl Pts',(-0.012702440074249,-0.0375416702731698,
-0.0110137146547475));
#47705=CARTESIAN_POINT('Ctrl Pts',(-0.0129510701067612,-0.0375592721463527,
-0.0110795492167575));
#47706=CARTESIAN_POINT('Ctrl Pts',(-0.0130919325839813,-0.0375703753413148,
-0.0111487424278653));
#47707=CARTESIAN_POINT('Ctrl Pts',(-0.0133339294243193,-0.0375918163492662,
-0.0113343517732612));
#47708=CARTESIAN_POINT('Ctrl Pts',(-0.0134341845631314,-0.0376019748769485,
-0.0114472338883389));
#47709=CARTESIAN_POINT('Ctrl Pts',(-0.0135901067471434,-0.0376208616106867,
-0.0117098836372724));
#47710=CARTESIAN_POINT('Ctrl Pts',(-0.0136422534676913,-0.0376312651783639,
-0.0118584084498437));
#47711=CARTESIAN_POINT('Ctrl Pts',(-0.0136851759337633,-0.0376529984057797,
-0.0121649096716104));
#47712=CARTESIAN_POINT('Ctrl Pts',(-0.0136764702810102,-0.0376639723199725,
-0.0123196735289665));
#47713=CARTESIAN_POINT('Ctrl Pts',(-0.013601139433123,-0.0376847562163576,
-0.0126127864437316));
#47714=CARTESIAN_POINT('Ctrl Pts',(-0.013536913370896,-0.0376937448829899,
-0.0127487575711001));
#47715=CARTESIAN_POINT('Ctrl Pts',(-0.0133569680278647,-0.0377135278724449,
-0.0129950775718869));
#47716=CARTESIAN_POINT('Ctrl Pts',(-0.0132408082311493,-0.0377244318449745,
-0.013101437858328));
#47717=CARTESIAN_POINT('Ctrl Pts',(-0.0129773842082659,-0.0377462452916852,
-0.0132604391573848));
#47718=CARTESIAN_POINT('Ctrl Pts',(-0.012833465607223,-0.0377569454540161,
-0.0133129711605081));
#47719=CARTESIAN_POINT('Ctrl Pts',(-0.0125339585442544,-0.0377770162200712,
-0.0133603211487119));
#47720=CARTESIAN_POINT('Ctrl Pts',(-0.0123812764837934,-0.0377859318764176,
-0.0133548464932053));
#47721=CARTESIAN_POINT('Ctrl Pts',(-0.0120819481442601,-0.0378067809750571,
-0.0132852334760115));
#47722=CARTESIAN_POINT('Ctrl Pts',(-0.0119386576122462,-0.0378178905837921,
-0.0132200648737588));
#47723=CARTESIAN_POINT('Ctrl Pts',(-0.01169063449608,-0.0378394667862012,
-0.0130410800803158));
#47724=CARTESIAN_POINT('Ctrl Pts',(-0.0115868917499629,-0.0378497472054623,
-0.012930800632283));
#47725=CARTESIAN_POINT('Ctrl Pts',(-0.0114228833421882,-0.0378690142336669,
-0.0126714301349768));
#47726=CARTESIAN_POINT('Ctrl Pts',(-0.0113664177539262,-0.0378791291329928,
-0.0125234225269568));
#47727=CARTESIAN_POINT('Ctrl Pts',(-0.0113154314733675,-0.0379008707744343,
-0.0122168026431469));
#47728=CARTESIAN_POINT('Ctrl Pts',(-0.0113202540238054,-0.0379118844087942,
-0.0120614786168155));
#47729=CARTESIAN_POINT('Ctrl Pts',(-0.0113883853282242,-0.0379328114671998,
-0.011766346704439));
#47730=CARTESIAN_POINT('Ctrl Pts',(-0.0114491667925139,-0.0379419686853233,
-0.0116289381630961));
#47731=CARTESIAN_POINT('Ctrl Pts',(-0.0116228071807605,-0.0379615166845352,
-0.0113783257413523));
#47732=CARTESIAN_POINT('Ctrl Pts',(-0.0117362545785923,-0.0379723554481044,
-0.0112691067112621));
#47733=CARTESIAN_POINT('Ctrl Pts',(-0.0119959028700665,-0.0379941758255843,
-0.0111033701658758));
#47734=CARTESIAN_POINT('Ctrl Pts',(-0.0121388355308802,-0.0380049451881162,
-0.011047178619133));
#47735=CARTESIAN_POINT('Ctrl Pts',(-0.0123584576527009,-0.0380198560395445,
-0.0110070032263349));
#47736=CARTESIAN_POINT('Ctrl Pts',(-0.0124292306108147,-0.0380244286063054,
-0.0110006128129773));
#47737=CARTESIAN_POINT('Ctrl Pts',(-0.0125,-0.0380287743898721,-0.0110006128129773));
#47738=CARTESIAN_POINT('Origin',(-0.0125,-0.0332787743898722,-0.0121758532865583));
#47739=CARTESIAN_POINT('',(-0.0124999999999998,-0.0385912743898722,-0.0110006128129773));
#47740=CARTESIAN_POINT('',(-0.0125000000000001,-0.0385287743898722,-0.0110006128129773));
#47741=CARTESIAN_POINT('',(-0.0125,-0.0332787743898722,-0.0110006128129775));
#47742=CARTESIAN_POINT('Ctrl Pts',(-0.0124999999999995,-0.0385912743898722,
-0.0110006128129773));
#47743=CARTESIAN_POINT('Ctrl Pts',(-0.0124565087484192,-0.0385886036932816,
-0.0110006128129773));
#47744=CARTESIAN_POINT('Ctrl Pts',(-0.0124129722332789,-0.038585844635133,
-0.0110030267200982));
#47745=CARTESIAN_POINT('Ctrl Pts',(-0.0122193907855129,-0.0385731909235403,
-0.0110246415132767));
#47746=CARTESIAN_POINT('Ctrl Pts',(-0.0120738617796335,-0.0385626382988648,
-0.0110702228000275));
#47747=CARTESIAN_POINT('Ctrl Pts',(-0.0118028463302189,-0.0385407999549928,
-0.0112167776062675));
#47748=CARTESIAN_POINT('Ctrl Pts',(-0.0116810563382989,-0.0385297176014095,
-0.0113184174837754));
#47749=CARTESIAN_POINT('Ctrl Pts',(-0.0114892903831182,-0.038509456105351,
-0.0115577602315995));
#47750=CARTESIAN_POINT('Ctrl Pts',(-0.011418910843281,-0.0385006350800992,
-0.0116912684002995));
#47751=CARTESIAN_POINT('Ctrl Pts',(-0.0113310284402633,-0.0384801098264777,
-0.0119807337057369));
#47752=CARTESIAN_POINT('Ctrl Pts',(-0.011315588716793,-0.0384692216215687,
-0.012134288814862));
#47753=CARTESIAN_POINT('Ctrl Pts',(-0.0113446469210865,-0.0384474286450853,
-0.0124416326708999));
#47754=CARTESIAN_POINT('Ctrl Pts',(-0.0113900384024102,-0.0384367399584771,
-0.0125923739962358));
#47755=CARTESIAN_POINT('Ctrl Pts',(-0.0115337914369434,-0.0384176712908055,
-0.012861297236537));
#47756=CARTESIAN_POINT('Ctrl Pts',(-0.0116284125486714,-0.0384080169285458,
-0.0129782027228725));
#47757=CARTESIAN_POINT('Ctrl Pts',(-0.0118606820391104,-0.0383868103800675,
-0.013174047222225));
#47758=CARTESIAN_POINT('Ctrl Pts',(-0.0119974760830762,-0.0383757371936117,
-0.0132494407533667));
#47759=CARTESIAN_POINT('Ctrl Pts',(-0.012292108301633,-0.0383543339708812,
-0.0133428171881113));
#47760=CARTESIAN_POINT('Ctrl Pts',(-0.0124469713593605,-0.0383448463927707,
-0.013359996557367));
#47761=CARTESIAN_POINT('Ctrl Pts',(-0.0127509274661702,-0.0383252540851647,
-0.0133338478287654));
#47762=CARTESIAN_POINT('Ctrl Pts',(-0.0128972094706624,-0.0383147929505996,
-0.0132921513230074));
#47763=CARTESIAN_POINT('Ctrl Pts',(-0.0131712724234851,-0.0382930352932722,
-0.0131531507737321));
#47764=CARTESIAN_POINT('Ctrl Pts',(-0.013295405422814,-0.0382819360159618,
-0.0130550917573229));
#47765=CARTESIAN_POINT('Ctrl Pts',(-0.0134937224473557,-0.0382614592670485,
-0.0128210244216694));
#47766=CARTESIAN_POINT('Ctrl Pts',(-0.0135679110095299,-0.0382526587741834,
-0.0126889780991429));
#47767=CARTESIAN_POINT('Ctrl Pts',(-0.0136633569632183,-0.0382322948744837,
-0.0124017883496194));
#47768=CARTESIAN_POINT('Ctrl Pts',(-0.0136828228830148,-0.0382214683389497,
-0.0122491029566404));
#47769=CARTESIAN_POINT('Ctrl Pts',(-0.013662129729114,-0.0381996536389373,
-0.0119414527361572));
#47770=CARTESIAN_POINT('Ctrl Pts',(-0.0136208261326266,-0.038188879804804,
-0.0117895105850076));
#47771=CARTESIAN_POINT('Ctrl Pts',(-0.013484432524159,-0.0381695478863152,
-0.0115168747485271));
#47772=CARTESIAN_POINT('Ctrl Pts',(-0.0133931092330342,-0.0381601914192525,
-0.0113975602185732));
#47773=CARTESIAN_POINT('Ctrl Pts',(-0.0131667144387111,-0.0381391363225177,
-0.0111958122603209));
#47774=CARTESIAN_POINT('Ctrl Pts',(-0.0130324537532802,-0.0381280922978589,
-0.0111168533544608));
#47775=CARTESIAN_POINT('Ctrl Pts',(-0.0127622413096364,-0.0381081602964126,
-0.0110226775600301));
#47776=CARTESIAN_POINT('Ctrl Pts',(-0.0126315077083065,-0.0380993499723272,
-0.0110006128129773));
#47777=CARTESIAN_POINT('Ctrl Pts',(-0.0124999999999997,-0.0380912743898721,
-0.0110006128129773));
#47778=CARTESIAN_POINT('Ctrl Pts',(-0.0125,-0.0380287743898721,-0.0110006128129773));
#47779=CARTESIAN_POINT('Ctrl Pts',(-0.0125792245739267,-0.0380336393866655,
-0.0110006128129773));
#47780=CARTESIAN_POINT('Ctrl Pts',(-0.0126584094591171,-0.0380387858650269,
-0.0110086209606377));
#47781=CARTESIAN_POINT('Ctrl Pts',(-0.0128894712097824,-0.0380546568427985,
-0.0110560634391791));
#47782=CARTESIAN_POINT('Ctrl Pts',(-0.0130347525988559,-0.0380657641942526,
-0.0111177201075049));
#47783=CARTESIAN_POINT('Ctrl Pts',(-0.0132877951446664,-0.0380874421122772,
-0.0112908799611763));
#47784=CARTESIAN_POINT('Ctrl Pts',(-0.0133944713437147,-0.0380978206403427,
-0.0113988457541976));
#47785=CARTESIAN_POINT('Ctrl Pts',(-0.0135641167653714,-0.0381172614344754,
-0.0116533538590951));
#47786=CARTESIAN_POINT('Ctrl Pts',(-0.0136238323153567,-0.0381270191111541,
-0.0117985266493816));
#47787=CARTESIAN_POINT('Ctrl Pts',(-0.0136830674183474,-0.0381485838480861,
-0.0121026516691176));
#47788=CARTESIAN_POINT('Ctrl Pts',(-0.0136824472934211,-0.038159632625784,
-0.012258471317927));
#47789=CARTESIAN_POINT('Ctrl Pts',(-0.0136220906017364,-0.0381807099432772,
-0.012555722317037));
#47790=CARTESIAN_POINT('Ctrl Pts',(-0.0135649670083539,-0.0381901058174151,
-0.0126947052449274));
#47791=CARTESIAN_POINT('Ctrl Pts',(-0.0133980574140238,-0.0382093996438471,
-0.0129498066043904));
#47792=CARTESIAN_POINT('Ctrl Pts',(-0.013287568282305,-0.0382201615589701,
-0.0130619819319864));
#47793=CARTESIAN_POINT('Ctrl Pts',(-0.0130321183860904,-0.0382419741035772,
-0.0132347693790506));
#47794=CARTESIAN_POINT('Ctrl Pts',(-0.0128903331222531,-0.0382528100966197,
-0.0132948276405998));
#47795=CARTESIAN_POINT('Ctrl Pts',(-0.0125941574734224,-0.038273197780509,
-0.0133568867193244));
#47796=CARTESIAN_POINT('Ctrl Pts',(-0.012442804108133,-0.0382819974089869,
-0.0133592522105797));
#47797=CARTESIAN_POINT('Ctrl Pts',(-0.0121407420705348,-0.0383024429238496,
-0.0133057574890605));
#47798=CARTESIAN_POINT('Ctrl Pts',(-0.0119934648327149,-0.038313540218447,
-0.0132478413935696));
#47799=CARTESIAN_POINT('Ctrl Pts',(-0.0117353091325814,-0.0383353106378249,
-0.0130809287109513));
#47800=CARTESIAN_POINT('Ctrl Pts',(-0.0116256156192813,-0.0383457856167584,
-0.0129754685883863));
#47801=CARTESIAN_POINT('Ctrl Pts',(-0.0114501336999095,-0.0383654038662279,
-0.0127260643294132));
#47802=CARTESIAN_POINT('Ctrl Pts',(-0.0113870932397963,-0.0383748492484878,
-0.0125837812488675));
#47803=CARTESIAN_POINT('Ctrl Pts',(-0.01131940612733,-0.0383962241418599,
-0.0122823335711542));
#47804=CARTESIAN_POINT('Ctrl Pts',(-0.0113156586839864,-0.0384073009082556,
-0.0121261192009379));
#47805=CARTESIAN_POINT('Ctrl Pts',(-0.0113679411761218,-0.0384285294031837,
-0.0118267361637458));
#47806=CARTESIAN_POINT('Ctrl Pts',(-0.011421326884658,-0.0384382327481969,
-0.0116860930166371));
#47807=CARTESIAN_POINT('Ctrl Pts',(-0.0115813338519879,-0.0384572625424429,
-0.0114264831879714));
#47808=CARTESIAN_POINT('Ctrl Pts',(-0.0116887267330117,-0.0384679381180455,
-0.0113113802696304));
#47809=CARTESIAN_POINT('Ctrl Pts',(-0.0119396988863677,-0.038489726559083,
-0.0111315170042053));
#47810=CARTESIAN_POINT('Ctrl Pts',(-0.0120802083836475,-0.0385006231509987,
-0.0110675398121957));
#47811=CARTESIAN_POINT('Ctrl Pts',(-0.0123180275050788,-0.0385172248734522,
-0.0110111902257223));
#47812=CARTESIAN_POINT('Ctrl Pts',(-0.0124089449706238,-0.0385231829123296,
-0.0110006128129773));
#47813=CARTESIAN_POINT('Ctrl Pts',(-0.0125000000000001,-0.0385287743898722,
-0.0110006128129773));
#47814=CARTESIAN_POINT('Origin',(-0.0125,-0.0332787743898722,-0.0121758532865583));
#47815=CARTESIAN_POINT('',(-0.0125,-0.0390912743898723,-0.0110006128129773));
#47816=CARTESIAN_POINT('',(-0.0125000000000002,-0.0390287743898722,-0.0110006128129773));
#47817=CARTESIAN_POINT('',(-0.0125,-0.0332787743898722,-0.0110006128129775));
#47818=CARTESIAN_POINT('Ctrl Pts',(-0.0124999999999999,-0.0390912743898723,
-0.0110006128129773));
#47819=CARTESIAN_POINT('Ctrl Pts',(-0.0124361318042558,-0.0390873523925412,
-0.0110006128129773));
#47820=CARTESIAN_POINT('Ctrl Pts',(-0.0123722363768311,-0.0390832441837451,
-0.0110058178843355));
#47821=CARTESIAN_POINT('Ctrl Pts',(-0.01215904607225,-0.0390689072685523,
-0.0110409451971411));
#47822=CARTESIAN_POINT('Ctrl Pts',(-0.0120153842146561,-0.0390581878376882,
-0.0110944653768048));
#47823=CARTESIAN_POINT('Ctrl Pts',(-0.0117529609530406,-0.0390363711569898,
-0.0112552912623418));
#47824=CARTESIAN_POINT('Ctrl Pts',(-0.0116375252587077,-0.0390254840770212,
-0.0113624292631865));
#47825=CARTESIAN_POINT('Ctrl Pts',(-0.0114592765757163,-0.0390057640191463,
-0.0116099129316036));
#47826=CARTESIAN_POINT('Ctrl Pts',(-0.0113959795277,-0.0389967352350057,
-0.0117462674698344));
#47827=CARTESIAN_POINT('Ctrl Pts',(-0.0113225784449348,-0.0389759125906752,
-0.0120399268424449));
#47828=CARTESIAN_POINT('Ctrl Pts',(-0.0113149125058534,-0.0389649273529849,
-0.0121948503937928));
#47829=CARTESIAN_POINT('Ctrl Pts',(-0.0113599590372235,-0.0389432078485187,
-0.0125011580823699));
#47830=CARTESIAN_POINT('Ctrl Pts',(-0.0114131306293705,-0.0389328965650288,
-0.0126493326067472));
#47831=CARTESIAN_POINT('Ctrl Pts',(-0.0115709310215612,-0.0389139291321524,
-0.0129110053851285));
#47832=CARTESIAN_POINT('Ctrl Pts',(-0.0116720502096819,-0.0389037398919044,
-0.0130232571945109));
#47833=CARTESIAN_POINT('Ctrl Pts',(-0.0119155457982235,-0.0388822639923835,
-0.0132072547755021));
#47834=CARTESIAN_POINT('Ctrl Pts',(-0.01205701580927,-0.0388711583174186,
-0.0132754656575466));
#47835=CARTESIAN_POINT('Ctrl Pts',(-0.0123550601297221,-0.0388501423856107,
-0.0133520083192323));
#47836=CARTESIAN_POINT('Ctrl Pts',(-0.012508353399461,-0.0388411081565501,
-0.0133608735333428));
#47837=CARTESIAN_POINT('Ctrl Pts',(-0.0128092132906521,-0.0388211755114125,
-0.0133197625193752));
#47838=CARTESIAN_POINT('Ctrl Pts',(-0.0129539143058282,-0.0388105405594625,
-0.0132704250063773));
#47839=CARTESIAN_POINT('Ctrl Pts',(-0.0132217798683727,-0.0387886380506598,
-0.0131166046146733));
#47840=CARTESIAN_POINT('Ctrl Pts',(-0.0133412020375297,-0.0387775797632527,
-0.0130115423529003));
#47841=CARTESIAN_POINT('Ctrl Pts',(-0.0135265633021201,-0.0387575324531254,
-0.0127671476349733));
#47842=CARTESIAN_POINT('Ctrl Pts',(-0.0135932660368702,-0.0387486316172506,
-0.0126321835652931));
#47843=CARTESIAN_POINT('Ctrl Pts',(-0.0136736973294375,-0.0387279514438123,
-0.0123405334433879));
#47844=CARTESIAN_POINT('Ctrl Pts',(-0.0136851460146902,-0.038717009841257,
-0.0121862252733616));
#47845=CARTESIAN_POINT('Ctrl Pts',(-0.0136478624518023,-0.0386952541065763,
-0.0118794066342107));
#47846=CARTESIAN_POINT('Ctrl Pts',(-0.0135984861716224,-0.0386846569917755,
-0.0117299567356054));
#47847=CARTESIAN_POINT('Ctrl Pts',(-0.0134475259835041,-0.0386658521435036,
-0.0114647541101418));
#47848=CARTESIAN_POINT('Ctrl Pts',(-0.0133496025749925,-0.0386558408190745,
-0.0113502039268433));
#47849=CARTESIAN_POINT('Ctrl Pts',(-0.0131115024117913,-0.0386344874358246,
-0.0111603168609624));
#47850=CARTESIAN_POINT('Ctrl Pts',(-0.0129722736321817,-0.0386233935968088,
-0.01108855789427));
#47851=CARTESIAN_POINT('Ctrl Pts',(-0.012717825645211,-0.0386051887856272,
-0.0110157939936399));
#47852=CARTESIAN_POINT('Ctrl Pts',(-0.0126090884023289,-0.0385979732548987,
-0.0110006128129773));
#47853=CARTESIAN_POINT('Ctrl Pts',(-0.0124999999999995,-0.0385912743898722,
-0.0110006128129773));
#47854=CARTESIAN_POINT('Ctrl Pts',(-0.0125000000000001,-0.0385287743898722,
-0.0110006128129773));
#47855=CARTESIAN_POINT('Ctrl Pts',(-0.0125578492220588,-0.0385323267760305,
-0.0110006128129773));
#47856=CARTESIAN_POINT('Ctrl Pts',(-0.0126157352120663,-0.038536032821848,
-0.0110048832182397));
#47857=CARTESIAN_POINT('Ctrl Pts',(-0.0128286273097136,-0.0385502306554375,
-0.0110366041367009));
#47858=CARTESIAN_POINT('Ctrl Pts',(-0.0129778167006288,-0.0385613098926756,
-0.0110906989641319));
#47859=CARTESIAN_POINT('Ctrl Pts',(-0.0132409588145226,-0.0385831587061255,
-0.0112511860900441));
#47860=CARTESIAN_POINT('Ctrl Pts',(-0.0133536257320299,-0.0385937240327688,
-0.0113540444522945));
#47861=CARTESIAN_POINT('Ctrl Pts',(-0.0135349091409325,-0.0386135161787347,
-0.0115983051214637));
#47862=CARTESIAN_POINT('Ctrl Pts',(-0.0136012206378563,-0.0386227106913121,
-0.0117377654968751));
#47863=CARTESIAN_POINT('Ctrl Pts',(-0.013677218490762,-0.0386438906044774,
-0.0120364633910202));
#47864=CARTESIAN_POINT('Ctrl Pts',(-0.0136853168434272,-0.038654986717369,
-0.0121929506026564));
#47865=CARTESIAN_POINT('Ctrl Pts',(-0.0136410847413676,-0.0386763608530617,
-0.0124943875949039));
#47866=CARTESIAN_POINT('Ctrl Pts',(-0.0135913713404146,-0.0386864282979431,
-0.0126367116161759));
#47867=CARTESIAN_POINT('Ctrl Pts',(-0.0134381563641025,-0.0387051951268156,
-0.012900668377162));
#47868=CARTESIAN_POINT('Ctrl Pts',(-0.0133338668335931,-0.0387157785554355,
-0.0130185473795422));
#47869=CARTESIAN_POINT('Ctrl Pts',(-0.0130874626240551,-0.0387375276967032,
-0.0132052140754249));
#47870=CARTESIAN_POINT('Ctrl Pts',(-0.012948303434786,-0.0387484763239597,
-0.0132729977664375));
#47871=CARTESIAN_POINT('Ctrl Pts',(-0.0126557771581247,-0.0387691782884885,
-0.0133502422710352));
#47872=CARTESIAN_POINT('Ctrl Pts',(-0.0125056218009486,-0.0387780952443826,
-0.01336051233767));
#47873=CARTESIAN_POINT('Ctrl Pts',(-0.0122011294815262,-0.0387981118242208,
-0.0133233254309806));
#47874=CARTESIAN_POINT('Ctrl Pts',(-0.0120501873479036,-0.0388091660979174,
-0.0132729705589158));
#47875=CARTESIAN_POINT('Ctrl Pts',(-0.0117823869548519,-0.0388310765594811,
-0.0131188129765792));
#47876=CARTESIAN_POINT('Ctrl Pts',(-0.0116669120554339,-0.03884172264508,
-0.0130185403130255));
#47877=CARTESIAN_POINT('Ctrl Pts',(-0.0114800927087565,-0.0388616783828028,
-0.0127792539376614));
#47878=CARTESIAN_POINT('Ctrl Pts',(-0.0114106851287761,-0.0388706900440563,
-0.0126424380334966));
#47879=CARTESIAN_POINT('Ctrl Pts',(-0.0113268416643965,-0.0388916784719636,
-0.012346440634055));
#47880=CARTESIAN_POINT('Ctrl Pts',(-0.0113145891210247,-0.0389027851863762,
-0.0121898039103801));
#47881=CARTESIAN_POINT('Ctrl Pts',(-0.0113510906883082,-0.0389242784911866,
-0.0118866862896884));
#47882=CARTESIAN_POINT('Ctrl Pts',(-0.0113972432896594,-0.0389344832308502,
-0.011742770012788));
#47883=CARTESIAN_POINT('Ctrl Pts',(-0.0115440435453904,-0.0389534915350077,
-0.0114746980722283));
#47884=CARTESIAN_POINT('Ctrl Pts',(-0.011645362238405,-0.0389637570449468,
-0.0113542011536127));
#47885=CARTESIAN_POINT('Ctrl Pts',(-0.0118874769316534,-0.0389854691664807,
-0.011161148967723));
#47886=CARTESIAN_POINT('Ctrl Pts',(-0.0120252802075833,-0.0389964599974716,
-0.0110898263770345));
#47887=CARTESIAN_POINT('Ctrl Pts',(-0.012279411085358,-0.0390146763854293,
-0.0110161866952631));
#47888=CARTESIAN_POINT('Ctrl Pts',(-0.0123895096540082,-0.0390219894347465,
-0.0110006128129772));
#47889=CARTESIAN_POINT('Ctrl Pts',(-0.0125000000000005,-0.0390287743898722,
-0.0110006128129773));
#47890=CARTESIAN_POINT('Origin',(-0.0125,-0.0332787743898722,-0.0121758532865583));
#47891=CARTESIAN_POINT('',(-0.0125,-0.0395912743898723,-0.0110006128129773));
#47892=CARTESIAN_POINT('',(-0.0125000000000001,-0.0395287743898722,-0.0110006128129773));
#47893=CARTESIAN_POINT('',(-0.0125,-0.0332787743898722,-0.0110006128129775));
#47894=CARTESIAN_POINT('Ctrl Pts',(-0.0125,-0.0395912743898723,-0.0110006128129773));
#47895=CARTESIAN_POINT('Ctrl Pts',(-0.0124163471756474,-0.0395861374645212,
-0.0110006128129773));
#47896=CARTESIAN_POINT('Ctrl Pts',(-0.0123327666728288,-0.0395806884477098,
-0.0110095408579271));
#47897=CARTESIAN_POINT('Ctrl Pts',(-0.0121014577168271,-0.0395647037939129,
-0.0110597614842461));
#47898=CARTESIAN_POINT('Ctrl Pts',(-0.0119600159999679,-0.0395538502287097,
-0.0111209104229628));
#47899=CARTESIAN_POINT('Ctrl Pts',(-0.0117057896218844,-0.039532042745072,
-0.0112956743170487));
#47900=CARTESIAN_POINT('Ctrl Pts',(-0.011596152235659,-0.0395213039987005,
-0.011408671418606));
#47901=CARTESIAN_POINT('Ctrl Pts',(-0.0114311551249103,-0.0395020829923444,
-0.0116650313503914));
#47902=CARTESIAN_POINT('Ctrl Pts',(-0.0113750682010705,-0.0394926082737645,
-0.0118044695324368));
#47903=CARTESIAN_POINT('Ctrl Pts',(-0.0113169380912085,-0.0394714887657494,
-0.012102315539655));
#47904=CARTESIAN_POINT('Ctrl Pts',(-0.0113175223621992,-0.0394604314056039,
-0.0122582562257425));
#47905=CARTESIAN_POINT('Ctrl Pts',(-0.011379099913938,-0.0394389184205922,
-0.0125616513940631));
#47906=CARTESIAN_POINT('Ctrl Pts',(-0.0114397371892158,-0.0394292528808071,
-0.0127060216173676));
#47907=CARTESIAN_POINT('Ctrl Pts',(-0.0116109939109865,-0.0394097628455809,
-0.0129591277516267));
#47908=CARTESIAN_POINT('Ctrl Pts',(-0.0117185053767981,-0.0393993571534504,
-0.0130664130035824));
#47909=CARTESIAN_POINT('Ctrl Pts',(-0.0119729685420149,-0.0393776523683252,
-0.0132378700795595));
#47910=CARTESIAN_POINT('Ctrl Pts',(-0.0121188078296144,-0.0393665469964113,
-0.0132985046048348));
#47911=CARTESIAN_POINT('Ctrl Pts',(-0.0124198941510669,-0.0393459493763168,
-0.0133579795616833));
#47912=CARTESIAN_POINT('Ctrl Pts',(-0.0125717273653552,-0.0393371329748319,
-0.0133585173954677));
#47913=CARTESIAN_POINT('Ctrl Pts',(-0.0128691685211884,-0.0393168622654799,
-0.0133019495962233));
#47914=CARTESIAN_POINT('Ctrl Pts',(-0.0130117976041611,-0.0393060739741659,
-0.0132446983363376));
#47915=CARTESIAN_POINT('Ctrl Pts',(-0.013270316772168,-0.0392842541838535,
-0.0130770226532524));
#47916=CARTESIAN_POINT('Ctrl Pts',(-0.0133829629088728,-0.0392734356645072,
-0.0129669868021019));
#47917=CARTESIAN_POINT('Ctrl Pts',(-0.0135547660310336,-0.0392539567134342,
-0.0127151396981697));
#47918=CARTESIAN_POINT('Ctrl Pts',(-0.0136145473299957,-0.0392447403605457,
-0.0125773056168207));
#47919=CARTESIAN_POINT('Ctrl Pts',(-0.0136805657768665,-0.0392237720176859,
-0.0122815914745074));
#47920=CARTESIAN_POINT('Ctrl Pts',(-0.0136842469397555,-0.0392127480366382,
-0.0121261215300212));
#47921=CARTESIAN_POINT('Ctrl Pts',(-0.0136310082319303,-0.0391910538696436,
-0.0118201711729089));
#47922=CARTESIAN_POINT('Ctrl Pts',(-0.0135736543662515,-0.0391810414770292,
-0.0116729388373926));
#47923=CARTESIAN_POINT('Ctrl Pts',(-0.0134081123580706,-0.039161726943374,
-0.0114148846860343));
#47924=CARTESIAN_POINT('Ctrl Pts',(-0.013303569966771,-0.0391514193698006,
-0.0113052243557608));
#47925=CARTESIAN_POINT('Ctrl Pts',(-0.0130541739979964,-0.0391298143253974,
-0.0111278039020919));
#47926=CARTESIAN_POINT('Ctrl Pts',(-0.0129103359923623,-0.0391187046208255,
-0.0110635808488112));
#47927=CARTESIAN_POINT('Ctrl Pts',(-0.0126732202193077,-0.0391022511041286,
-0.0110101932849007));
#47928=CARTESIAN_POINT('Ctrl Pts',(-0.0125866562353605,-0.0390965957477068,
-0.0110006128129773));
#47929=CARTESIAN_POINT('Ctrl Pts',(-0.0124999999999999,-0.0390912743898723,
-0.0110006128129773));
#47930=CARTESIAN_POINT('Ctrl Pts',(-0.0125000000000005,-0.0390287743898722,
-0.0110006128129773));
#47931=CARTESIAN_POINT('Ctrl Pts',(-0.0125380043212259,-0.0390311081468334,
-0.0110006128129773));
#47932=CARTESIAN_POINT('Ctrl Pts',(-0.0125760469588011,-0.0390335096083526,
-0.0110024561063973));
#47933=CARTESIAN_POINT('Ctrl Pts',(-0.0127692440411077,-0.039046040941093,
-0.0110212848501554));
#47934=CARTESIAN_POINT('Ctrl Pts',(-0.0129199019936708,-0.0390569192236894,
-0.0110671679735217));
#47935=CARTESIAN_POINT('Ctrl Pts',(-0.0131909381848969,-0.0390787371639758,
-0.011213111355022));
#47936=CARTESIAN_POINT('Ctrl Pts',(-0.0133094877011632,-0.0390894662334035,
-0.011310399248883));
#47937=CARTESIAN_POINT('Ctrl Pts',(-0.0135024469069445,-0.0391096006828934,
-0.0115440917795719));
#47938=CARTESIAN_POINT('Ctrl Pts',(-0.0135752671756624,-0.0391184752188413,
-0.0116780331128062));
#47939=CARTESIAN_POINT('Ctrl Pts',(-0.0136677153550896,-0.0391392455068082,
-0.0119709541096058));
#47940=CARTESIAN_POINT('Ctrl Pts',(-0.013684570737312,-0.0391503550589178,
-0.0121276308529956));
#47941=CARTESIAN_POINT('Ctrl Pts',(-0.0136566562467006,-0.0391719743851289,
-0.0124325257390941));
#47942=CARTESIAN_POINT('Ctrl Pts',(-0.0136144353474513,-0.0391822955854814,
-0.0125780844477775));
#47943=CARTESIAN_POINT('Ctrl Pts',(-0.0134746925329525,-0.0392016341206397,
-0.0128508135983907));
#47944=CARTESIAN_POINT('Ctrl Pts',(-0.0133764261076692,-0.0392115960900017,
-0.0129742925408032));
#47945=CARTESIAN_POINT('Ctrl Pts',(-0.0131389501348909,-0.0392332660162748,
-0.0131741890763487));
#47946=CARTESIAN_POINT('Ctrl Pts',(-0.0130026967627076,-0.03924429501537,
-0.013249272739898));
#47947=CARTESIAN_POINT('Ctrl Pts',(-0.012713873067471,-0.0392652841591031,
-0.0133410304146222));
#47948=CARTESIAN_POINT('Ctrl Pts',(-0.0125646798355172,-0.0392745321348618,
-0.0133587210736983));
#47949=CARTESIAN_POINT('Ctrl Pts',(-0.012260598453781,-0.0392939760734432,
-0.0133369741904191));
#47950=CARTESIAN_POINT('Ctrl Pts',(-0.0121088297574482,-0.0393047841449024,
-0.0132949952909828));
#47951=CARTESIAN_POINT('Ctrl Pts',(-0.0118338010400032,-0.0393266031935076,
-0.0131559359067574));
#47952=CARTESIAN_POINT('Ctrl Pts',(-0.0117125205384294,-0.0393374008447962,
-0.0130614438139135));
#47953=CARTESIAN_POINT('Ctrl Pts',(-0.0115140252998137,-0.039357693913761,
-0.0128328659887244));
#47954=CARTESIAN_POINT('Ctrl Pts',(-0.0114381400426169,-0.0393665047562633,
-0.0127014626687907));
#47955=CARTESIAN_POINT('Ctrl Pts',(-0.0113380201532362,-0.0393870735158575,
-0.0124113838035935));
#47956=CARTESIAN_POINT('Ctrl Pts',(-0.0113170249850932,-0.0393981776653904,
-0.0122547832521241));
#47957=CARTESIAN_POINT('Ctrl Pts',(-0.0113371775917443,-0.0394198955701545,
-0.0119484981239624));
#47958=CARTESIAN_POINT('Ctrl Pts',(-0.0113758251818902,-0.0394303147579032,
-0.0118015575102327));
#47959=CARTESIAN_POINT('Ctrl Pts',(-0.011508376598657,-0.0394498294613337,
-0.011526343878615));
#47960=CARTESIAN_POINT('Ctrl Pts',(-0.0116025072219682,-0.039459450404398,
-0.0114014462064592));
#47961=CARTESIAN_POINT('Ctrl Pts',(-0.0118335592970148,-0.0394809371956775,
-0.0111955886174164));
#47962=CARTESIAN_POINT('Ctrl Pts',(-0.0119680626276684,-0.0394919986210786,
-0.0111165591840503));
#47963=CARTESIAN_POINT('Ctrl Pts',(-0.0122382704608941,-0.0395119227656996,
-0.0110225970119605));
#47964=CARTESIAN_POINT('Ctrl Pts',(-0.0123687365131833,-0.0395207138044907,
-0.0110006128129772));
#47965=CARTESIAN_POINT('Ctrl Pts',(-0.0125000000000001,-0.0395287743898722,
-0.0110006128129773));
#47966=CARTESIAN_POINT('Origin',(-0.0125,-0.0332787743898722,-0.0121758532865583));
#47967=CARTESIAN_POINT('',(-0.0125000000000002,-0.0400912743898723,-0.0110006128129772));
#47968=CARTESIAN_POINT('',(-0.0125,-0.0400287743898722,-0.0110006128129772));
#47969=CARTESIAN_POINT('',(-0.0125,-0.0332787743898722,-0.0110006128129775));
#47970=CARTESIAN_POINT('Ctrl Pts',(-0.0125000000000004,-0.0400912743898723,
-0.0110006128129772));
#47971=CARTESIAN_POINT('Ctrl Pts',(-0.0123962317877206,-0.0400849022253409,
-0.0110006128129772));
#47972=CARTESIAN_POINT('Ctrl Pts',(-0.0122927535448283,-0.0400780608560291,
-0.0110143493374508));
#47973=CARTESIAN_POINT('Ctrl Pts',(-0.0120441313791396,-0.0400604016002137,
-0.0110818160466131));
#47974=CARTESIAN_POINT('Ctrl Pts',(-0.0119053500422646,-0.0400494402872072,
-0.0111506120085336));
#47975=CARTESIAN_POINT('Ctrl Pts',(-0.0116600759365155,-0.0400276935027585,
-0.0113391696256987));
#47976=CARTESIAN_POINT('Ctrl Pts',(-0.0115566592011941,-0.0400171877730503,
-0.0114578276638657));
#47977=CARTESIAN_POINT('Ctrl Pts',(-0.0114052665283221,-0.0399983879548473,
-0.0117229593508435));
#47978=CARTESIAN_POINT('Ctrl Pts',(-0.0113565975937592,-0.0399882626657875,
-0.0118657551449614));
#47979=CARTESIAN_POINT('Ctrl Pts',(-0.0113145736351104,-0.039966859998235,
-0.0121675945187651));
#47980=CARTESIAN_POINT('Ctrl Pts',(-0.0113238530734446,-0.039955760091895,
-0.0123241352289692));
#47981=CARTESIAN_POINT('Ctrl Pts',(-0.0114020898978315,-0.0399346340959946,
-0.0126220727340926));
#47982=CARTESIAN_POINT('Ctrl Pts',(-0.0114692838554654,-0.0399254972306594,
-0.0127607762996261));
#47983=CARTESIAN_POINT('Ctrl Pts',(-0.0116521411573634,-0.0399056583403411,
-0.0130036293666762));
#47984=CARTESIAN_POINT('Ctrl Pts',(-0.0117656095383184,-0.0398950694984301,
-0.0131057628197797));
#47985=CARTESIAN_POINT('Ctrl Pts',(-0.0120300863970327,-0.0398732018276857,
-0.013264469984384));
#47986=CARTESIAN_POINT('Ctrl Pts',(-0.0121797814627849,-0.0398621289096384,
-0.0133175107196541));
#47987=CARTESIAN_POINT('Ctrl Pts',(-0.0124834558041281,-0.0398419589634149,
-0.0133604402231358));
#47988=CARTESIAN_POINT('Ctrl Pts',(-0.012634013305693,-0.0398331108801856,
-0.0133529535267219));
#47989=CARTESIAN_POINT('Ctrl Pts',(-0.0129278591315907,-0.0398125187473489,
-0.0132810924360404));
#47990=CARTESIAN_POINT('Ctrl Pts',(-0.0130679982489852,-0.0398016067620295,
-0.0132160395444263));
#47991=CARTESIAN_POINT('Ctrl Pts',(-0.0133177015541598,-0.0397798278255687,
-0.0130342466534));
#47992=CARTESIAN_POINT('Ctrl Pts',(-0.0134242270926281,-0.0397691774563157,
-0.0129183524182194));
#47993=CARTESIAN_POINT('Ctrl Pts',(-0.0135823238316769,-0.0397502213097931,
-0.0126575112679652));
#47994=CARTESIAN_POINT('Ctrl Pts',(-0.0136346764729176,-0.0397404217107833,
-0.0125164001929154));
#47995=CARTESIAN_POINT('Ctrl Pts',(-0.0136847056400201,-0.0397191519313817,
-0.0122164349255123));
#47996=CARTESIAN_POINT('Ctrl Pts',(-0.0136797396868606,-0.0397080688922195,
-0.0120601320911881));
#47997=CARTESIAN_POINT('Ctrl Pts',(-0.0136097146871464,-0.0396867480225824,
-0.0117594463040344));
#47998=CARTESIAN_POINT('Ctrl Pts',(-0.0135457545313975,-0.0396773789835379,
-0.0116179593148396));
#47999=CARTESIAN_POINT('Ctrl Pts',(-0.0133686469812788,-0.0396577117549183,
-0.0113699892362042));
#48000=CARTESIAN_POINT('Ctrl Pts',(-0.0132581174479979,-0.0396472108891491,
-0.0112652469845541));
#48001=CARTESIAN_POINT('Ctrl Pts',(-0.0129985543508686,-0.0396254171135893,
-0.0111001132059106));
#48002=CARTESIAN_POINT('Ctrl Pts',(-0.0128507338519276,-0.039614324056765,
-0.0110432575959414));
#48003=CARTESIAN_POINT('Ctrl Pts',(-0.0126311576369537,-0.0395995229692149,
-0.0110060986650045));
#48004=CARTESIAN_POINT('Ctrl Pts',(-0.0125655686602552,-0.0395953008087733,
-0.0110006128129773));
#48005=CARTESIAN_POINT('Ctrl Pts',(-0.0125,-0.0395912743898723,-0.0110006128129773));
#48006=CARTESIAN_POINT('Ctrl Pts',(-0.0125000000000001,-0.0395287743898722,
-0.0110006128129773));
#48007=CARTESIAN_POINT('Ctrl Pts',(-0.0125174245500157,-0.0395298443909558,
-0.0110006128129773));
#48008=CARTESIAN_POINT('Ctrl Pts',(-0.0125348614911154,-0.0395309288916245,
-0.0110010003229717));
#48009=CARTESIAN_POINT('Ctrl Pts',(-0.0127080845353512,-0.0395418396788189,
-0.0110087163783427));
#48010=CARTESIAN_POINT('Ctrl Pts',(-0.0128609013456591,-0.0395525665895324,
-0.0110465906896864));
#48011=CARTESIAN_POINT('Ctrl Pts',(-0.0131399095442775,-0.0395743710672021,
-0.0111783464258558));
#48012=CARTESIAN_POINT('Ctrl Pts',(-0.0132639717741701,-0.0395852332172042,
-0.0112698396598852));
#48013=CARTESIAN_POINT('Ctrl Pts',(-0.013468204796238,-0.0396056883974529,
-0.0114930518264234));
#48014=CARTESIAN_POINT('Ctrl Pts',(-0.0135472530135271,-0.0396144928452177,
-0.0116218701528459));
#48015=CARTESIAN_POINT('Ctrl Pts',(-0.0136552347883389,-0.0396348487923602,
-0.0119089477483654));
#48016=CARTESIAN_POINT('Ctrl Pts',(-0.0136805009641661,-0.0396459395008549,
-0.012065358742409));
#48017=CARTESIAN_POINT('Ctrl Pts',(-0.0136683944230493,-0.0396677445107659,
-0.0123728723045001));
#48018=CARTESIAN_POINT('Ctrl Pts',(-0.0136334700668644,-0.0396782581078943,
-0.0125211443629192));
#48019=CARTESIAN_POINT('Ctrl Pts',(-0.0135083008326579,-0.0396979496618003,
-0.0127988520965755));
#48020=CARTESIAN_POINT('Ctrl Pts',(-0.0134183203314263,-0.0397072824210437,
-0.0129251851045186));
#48021=CARTESIAN_POINT('Ctrl Pts',(-0.0131938431463073,-0.0397285761993604,
-0.0131369866574674));
#48022=CARTESIAN_POINT('Ctrl Pts',(-0.0130612323642198,-0.0397396621156901,
-0.0132199848666402));
#48023=CARTESIAN_POINT('Ctrl Pts',(-0.01277675232481,-0.0397609523237271,
-0.0133277577248656));
#48024=CARTESIAN_POINT('Ctrl Pts',(-0.0126284242873029,-0.0397708015612897,
-0.0133535361497418));
#48025=CARTESIAN_POINT('Ctrl Pts',(-0.0123234277900492,-0.03978972100852,
-0.0133481679761669));
#48026=CARTESIAN_POINT('Ctrl Pts',(-0.0121696760557943,-0.0398003586403142,
-0.013314431181386));
#48027=CARTESIAN_POINT('Ctrl Pts',(-0.0118868782278107,-0.0398221323996069,
-0.0131901057113366));
#48028=CARTESIAN_POINT('Ctrl Pts',(-0.0117601028558801,-0.0398330518152534,
-0.0131016965554965));
#48029=CARTESIAN_POINT('Ctrl Pts',(-0.0115501649361208,-0.0398536654999091,
-0.0128838948225458));
#48030=CARTESIAN_POINT('Ctrl Pts',(-0.0114679714101034,-0.0398625246798243,
-0.0127575932318192));
#48031=CARTESIAN_POINT('Ctrl Pts',(-0.0113522581725218,-0.0398826648293535,
-0.0124735590053716));
#48032=CARTESIAN_POINT('Ctrl Pts',(-0.011322768230276,-0.0398937343994475,
-0.012317446123776));
#48033=CARTESIAN_POINT('Ctrl Pts',(-0.0113268797739995,-0.0399156109968757,
-0.0120089229711124));
#48034=CARTESIAN_POINT('Ctrl Pts',(-0.0113580856030866,-0.0399262112921243,
-0.0118594282190164));
#48035=CARTESIAN_POINT('Ctrl Pts',(-0.0114759814413373,-0.0399460732013568,
-0.0115793179836641));
#48036=CARTESIAN_POINT('Ctrl Pts',(-0.0115619652282376,-0.0399551832485288,
-0.0114515838363079));
#48037=CARTESIAN_POINT('Ctrl Pts',(-0.0117799894325702,-0.0399762824589431,
-0.0112340933305413));
#48038=CARTESIAN_POINT('Ctrl Pts',(-0.0119106463487137,-0.0399873840102053,
-0.0111472699309539));
#48039=CARTESIAN_POINT('Ctrl Pts',(-0.0121927420742577,-0.0400088050361703,
-0.011031677499403));
#48040=CARTESIAN_POINT('Ctrl Pts',(-0.0123406887842786,-0.0400189461772311,
-0.0110018900118203));
#48041=CARTESIAN_POINT('Ctrl Pts',(-0.0124935218279313,-0.0400283761057175,
-0.0110006262016197));
#48042=CARTESIAN_POINT('Ctrl Pts',(-0.0124967611857696,-0.0400285755018244,
-0.0110006128129772));
#48043=CARTESIAN_POINT('Ctrl Pts',(-0.0125,-0.0400287743898722,-0.0110006128129772));
#48044=CARTESIAN_POINT('Origin',(-0.0125,-0.0332787743898722,-0.0121758532865583));
#48045=CARTESIAN_POINT('',(-0.0125000000000002,-0.0405912743898722,-0.0110006128129772));
#48046=CARTESIAN_POINT('',(-0.0124999999999998,-0.0405287743898722,-0.0110006128129772));
#48047=CARTESIAN_POINT('',(-0.0125,-0.0332787743898722,-0.0110006128129775));
#48048=CARTESIAN_POINT('Ctrl Pts',(-0.0125000000000003,-0.0405912743898722,
-0.0110006128129772));
#48049=CARTESIAN_POINT('Ctrl Pts',(-0.0123765027860332,-0.0405836907132406,
-0.0110006128129772));
#48050=CARTESIAN_POINT('Ctrl Pts',(-0.0122536356788734,-0.040575455876852,
-0.0110200706532127));
#48051=CARTESIAN_POINT('Ctrl Pts',(-0.0119892666271235,-0.0405561673436804,
-0.0111062179802573));
#48052=CARTESIAN_POINT('Ctrl Pts',(-0.0118534807529531,-0.0405451286580267,
-0.0111823845909718));
#48053=CARTESIAN_POINT('Ctrl Pts',(-0.0116177571092469,-0.0405235081326747,
-0.0113839228584159));
#48054=CARTESIAN_POINT('Ctrl Pts',(-0.0115206270855756,-0.0405136450041091,
-0.0115077909292436));
#48055=CARTESIAN_POINT('Ctrl Pts',(-0.0113828442745808,-0.0404942580696245,
-0.0117812026500237));
#48056=CARTESIAN_POINT('Ctrl Pts',(-0.0113415917858301,-0.0404839095858865,
-0.0119271461331726));
#48057=CARTESIAN_POINT('Ctrl Pts',(-0.0113157847889707,-0.0404622620663835,
-0.012232438626044));
#48058=CARTESIAN_POINT('Ctrl Pts',(-0.0113337661272027,-0.0404511532393016,
-0.0123891051444517));
#48059=CARTESIAN_POINT('Ctrl Pts',(-0.0114283067168395,-0.0404304372640064,
-0.0126812601758514));
#48060=CARTESIAN_POINT('Ctrl Pts',(-0.0115019605442114,-0.0404215856810574,
-0.0128145068882508));
#48061=CARTESIAN_POINT('Ctrl Pts',(-0.0116964238155177,-0.0404014078979584,
-0.0130468165589063));
#48062=CARTESIAN_POINT('Ctrl Pts',(-0.011815719401609,-0.0403906595979343,
-0.0131433546357287));
#48063=CARTESIAN_POINT('Ctrl Pts',(-0.0120878543646401,-0.0403688399030079,
-0.0132874443796119));
#48064=CARTESIAN_POINT('Ctrl Pts',(-0.0122388234685241,-0.0403579799081463,
-0.0133322727534152));
#48065=CARTESIAN_POINT('Ctrl Pts',(-0.0125425107587682,-0.0403383576467293,
-0.0133597319563076));
#48066=CARTESIAN_POINT('Ctrl Pts',(-0.0126920466391854,-0.040329259200383,
-0.0133448306089765));
#48067=CARTESIAN_POINT('Ctrl Pts',(-0.0129822936812903,-0.0403083769367371,
-0.0132585528786485));
#48068=CARTESIAN_POINT('Ctrl Pts',(-0.0131196891079668,-0.0402973750998214,
-0.0131862134417303));
#48069=CARTESIAN_POINT('Ctrl Pts',(-0.0133615704310672,-0.0402755828940664,
-0.01299049820966));
#48070=CARTESIAN_POINT('Ctrl Pts',(-0.013462721956479,-0.0402653532113436,
-0.0128680062952246));
#48071=CARTESIAN_POINT('Ctrl Pts',(-0.0136073879773797,-0.0402461375367459,
-0.012597009833051));
#48072=CARTESIAN_POINT('Ctrl Pts',(-0.0136520225196291,-0.0402358867362545,
-0.0124524439655626));
#48073=CARTESIAN_POINT('Ctrl Pts',(-0.0136852026385219,-0.0402143425507755,
-0.0121486087806181));
#48074=CARTESIAN_POINT('Ctrl Pts',(-0.0136711668426919,-0.0402032336289454,
-0.0119919409259875));
#48075=CARTESIAN_POINT('Ctrl Pts',(-0.0135839794615331,-0.040182328971783,
-0.0116971249357849));
#48076=CARTESIAN_POINT('Ctrl Pts',(-0.0135132482466612,-0.0401733786547133,
-0.0115614294913511));
#48077=CARTESIAN_POINT('Ctrl Pts',(-0.0133240514652581,-0.0401533533738992,
-0.0113242994371902));
#48078=CARTESIAN_POINT('Ctrl Pts',(-0.0132073807317541,-0.0401426743145306,
-0.0112251679684209));
#48079=CARTESIAN_POINT('Ctrl Pts',(-0.0129391373269841,-0.040120865440619,
-0.0110746430629777));
#48080=CARTESIAN_POINT('Ctrl Pts',(-0.0127892876420601,-0.0401099439672909,
-0.0110261417510927));
#48081=CARTESIAN_POINT('Ctrl Pts',(-0.0125896441023155,-0.0400968700373949,
-0.0110031742278326));
#48082=CARTESIAN_POINT('Ctrl Pts',(-0.0125448006302718,-0.0400940254923624,
-0.0110006128129773));
#48083=CARTESIAN_POINT('Ctrl Pts',(-0.0125000000000004,-0.0400912743898723,
-0.0110006128129772));
#48084=CARTESIAN_POINT('Ctrl Pts',(-0.0125,-0.0400287743898722,-0.0110006128129772));
#48085=CARTESIAN_POINT('Ctrl Pts',(-0.0126524836274197,-0.0400381380547259,
-0.0110006128129772));
#48086=CARTESIAN_POINT('Ctrl Pts',(-0.0128036345865955,-0.0400484720113026,
-0.0110302888885797));
#48087=CARTESIAN_POINT('Ctrl Pts',(-0.0130870257612733,-0.0400699845916909,
-0.0111462198995466));
#48088=CARTESIAN_POINT('Ctrl Pts',(-0.0132163319242825,-0.0400809519582966,
-0.0112315980904499));
#48089=CARTESIAN_POINT('Ctrl Pts',(-0.0134317041325933,-0.040101714069395,
-0.0114441738418315));
#48090=CARTESIAN_POINT('Ctrl Pts',(-0.0135168997092491,-0.0401106819416352,
-0.0115681254152743));
#48091=CARTESIAN_POINT('Ctrl Pts',(-0.0136392038154371,-0.0401305000981957,
-0.0118476186116939));
#48092=CARTESIAN_POINT('Ctrl Pts',(-0.0136726529119307,-0.0401414133243714,
-0.0120015265928821));
#48093=CARTESIAN_POINT('Ctrl Pts',(-0.0136774732976494,-0.0401632245157759,
-0.0123091273318683));
#48094=CARTESIAN_POINT('Ctrl Pts',(-0.0136504569969394,-0.0401739136715251,
-0.0124598752734477));
#48095=CARTESIAN_POINT('Ctrl Pts',(-0.0135406527323881,-0.0401939606135981,
-0.0127425950057959));
#48096=CARTESIAN_POINT('Ctrl Pts',(-0.01345901114667,-0.0402028938799324,
-0.0128718814767081));
#48097=CARTESIAN_POINT('Ctrl Pts',(-0.0132481302720589,-0.0402237721545124,
-0.0130955129268549));
#48098=CARTESIAN_POINT('Ctrl Pts',(-0.0131197436700429,-0.0402348814785963,
-0.0131864878642911));
#48099=CARTESIAN_POINT('Ctrl Pts',(-0.0128403567717934,-0.0402564410368315,
-0.0133106795318864));
#48100=CARTESIAN_POINT('Ctrl Pts',(-0.0126929068688548,-0.0402667059931346,
-0.0133448198189927));
#48101=CARTESIAN_POINT('Ctrl Pts',(-0.0123860726132381,-0.0402859461530712,
-0.0133560508509775));
#48102=CARTESIAN_POINT('Ctrl Pts',(-0.0122295329013218,-0.0402961205978299,
-0.0133302933411034));
#48103=CARTESIAN_POINT('Ctrl Pts',(-0.0119388113577665,-0.0403178887926647,
-0.0132198490988367));
#48104=CARTESIAN_POINT('Ctrl Pts',(-0.0118071040076832,-0.0403288963334232,
-0.0131374967429749));
#48105=CARTESIAN_POINT('Ctrl Pts',(-0.0115864593381179,-0.0403497999763606,
-0.0129300611476745));
#48106=CARTESIAN_POINT('Ctrl Pts',(-0.0114983407452764,-0.0403589257781446,
-0.0128083481307916));
#48107=CARTESIAN_POINT('Ctrl Pts',(-0.0113692502369099,-0.0403785126808822,
-0.0125321162805999));
#48108=CARTESIAN_POINT('Ctrl Pts',(-0.0113320153237119,-0.0403893626374941,
-0.0123791005828364));
#48109=CARTESIAN_POINT('Ctrl Pts',(-0.0113195765966316,-0.0404111828286165,
-0.0120713729218565));
#48110=CARTESIAN_POINT('Ctrl Pts',(-0.0113429835292453,-0.0404219412488868,
-0.0119196481506558));
#48111=CARTESIAN_POINT('Ctrl Pts',(-0.0114458917413749,-0.0404421421735211,
-0.0116347568198472));
#48112=CARTESIAN_POINT('Ctrl Pts',(-0.0115239158223177,-0.040450983191197,
-0.0115041461888807));
#48113=CARTESIAN_POINT('Ctrl Pts',(-0.0117287429465967,-0.0404716699333819,
-0.011275431654526));
#48114=CARTESIAN_POINT('Ctrl Pts',(-0.0118551205028745,-0.0404827781435009,
-0.0111810083680333));
#48115=CARTESIAN_POINT('Ctrl Pts',(-0.0121320294889581,-0.040504440333381,
-0.0110496300259603));
#48116=CARTESIAN_POINT('Ctrl Pts',(-0.0122789627531435,-0.0405148032305823,
-0.0110118323957042));
#48117=CARTESIAN_POINT('Ctrl Pts',(-0.0124527083563813,-0.040525845043314,
-0.0110013257627274));
#48118=CARTESIAN_POINT('Ctrl Pts',(-0.0124763651716116,-0.04052732303004,
-0.0110006128129772));
#48119=CARTESIAN_POINT('Ctrl Pts',(-0.0124999999999997,-0.0405287743898722,
-0.0110006128129772));
#48120=CARTESIAN_POINT('Origin',(-0.0125,-0.0332787743898722,-0.0121758532865583));
#48121=CARTESIAN_POINT('',(-0.0125,-0.0410912743898722,-0.0110006128129772));
#48122=CARTESIAN_POINT('',(-0.0124999999999998,-0.0410287743898722,-0.0110006128129772));
#48123=CARTESIAN_POINT('',(-0.0125,-0.0332787743898722,-0.0110006128129775));
#48124=CARTESIAN_POINT('Ctrl Pts',(-0.0125,-0.0410912743898722,-0.0110006128129772));
#48125=CARTESIAN_POINT('Ctrl Pts',(-0.0123548775896907,-0.0410823627602376,
-0.0110006128129772));
#48126=CARTESIAN_POINT('Ctrl Pts',(-0.0122108943568779,-0.041072568120321,
-0.0110274919124065));
#48127=CARTESIAN_POINT('Ctrl Pts',(-0.0119307969650165,-0.0410515199816448,
-0.0111360279858138));
#48128=CARTESIAN_POINT('Ctrl Pts',(-0.0117987260605142,-0.0410404288340674,
-0.0112201088417681));
#48129=CARTESIAN_POINT('Ctrl Pts',(-0.0115760633306248,-0.0410191892648834,
-0.011433524112961));
#48130=CARTESIAN_POINT('Ctrl Pts',(-0.0114872140610908,-0.0410099251588461,
-0.0115602514817448));
#48131=CARTESIAN_POINT('Ctrl Pts',(-0.011364086873253,-0.0409901853892517,
-0.0118386391957428));
#48132=CARTESIAN_POINT('Ctrl Pts',(-0.0113302016880243,-0.0409796468095926,
-0.0119872635799372));
#48133=CARTESIAN_POINT('Ctrl Pts',(-0.0113203334694503,-0.0409578202638131,
-0.0122950808599193));
#48134=CARTESIAN_POINT('Ctrl Pts',(-0.0113467841610049,-0.0409467346962911,
-0.0124514193514131));
#48135=CARTESIAN_POINT('Ctrl Pts',(-0.011456938022439,-0.0409264387295969,
-0.0127376510495263));
#48136=CARTESIAN_POINT('Ctrl Pts',(-0.011536866112814,-0.0409176251035845,
-0.0128657598126419));
#48137=CARTESIAN_POINT('Ctrl Pts',(-0.0117426955931429,-0.0408971252952279,
-0.0130874656025689));
#48138=CARTESIAN_POINT('Ctrl Pts',(-0.011867522589383,-0.0408862464190323,
-0.0131781059976171));
#48139=CARTESIAN_POINT('Ctrl Pts',(-0.01214760848416,-0.0408644488917028,
-0.0133077990695779));
#48140=CARTESIAN_POINT('Ctrl Pts',(-0.0123006978574228,-0.0408537461000921,
-0.0133445209901367));
#48141=CARTESIAN_POINT('Ctrl Pts',(-0.0126053999752747,-0.0408346351553067,
-0.0133558003800468));
#48142=CARTESIAN_POINT('Ctrl Pts',(-0.0127540204427141,-0.0408250326230259,
-0.0133329585108336));
#48143=CARTESIAN_POINT('Ctrl Pts',(-0.0130401150017559,-0.0408038500644697,
-0.0132310184192814));
#48144=CARTESIAN_POINT('Ctrl Pts',(-0.0131741043111917,-0.0407927809827804,
-0.0131508827235366));
#48145=CARTESIAN_POINT('Ctrl Pts',(-0.0134033354827007,-0.0407713470972686,
-0.0129433634850405));
#48146=CARTESIAN_POINT('Ctrl Pts',(-0.0134963085598998,-0.0407618121420599,
-0.0128180669999191));
#48147=CARTESIAN_POINT('Ctrl Pts',(-0.0136268179943227,-0.0407422481188121,
-0.0125421578165565));
#48148=CARTESIAN_POINT('Ctrl Pts',(-0.0136644411031342,-0.0407318021814487,
-0.0123948399560682));
#48149=CARTESIAN_POINT('Ctrl Pts',(-0.0136823755998282,-0.0407100587418727,
-0.0120881947133739));
#48150=CARTESIAN_POINT('Ctrl Pts',(-0.0136602009649822,-0.0406989575063841,
-0.011931635258338));
#48151=CARTESIAN_POINT('Ctrl Pts',(-0.0135579048804031,-0.0406784469761072,
-0.0116423775945446));
#48152=CARTESIAN_POINT('Ctrl Pts',(-0.013481147287524,-0.040669644045422,
-0.0115116924477378));
#48153=CARTESIAN_POINT('Ctrl Pts',(-0.0132810701416322,-0.0406493060166953,
-0.0112845864415585));
#48154=CARTESIAN_POINT('Ctrl Pts',(-0.0131590177303542,-0.0406384899075225,
-0.0111909107166815));
#48155=CARTESIAN_POINT('Ctrl Pts',(-0.012882875624152,-0.0406166732625263,
-0.0110538475739989));
#48156=CARTESIAN_POINT('Ctrl Pts',(-0.0127308073952225,-0.040605886706129,
-0.0110129943291534));
#48157=CARTESIAN_POINT('Ctrl Pts',(-0.0125501152010411,-0.0405943802337429,
-0.0110014134606557));
#48158=CARTESIAN_POINT('Ctrl Pts',(-0.0125250463681162,-0.0405928124290756,
-0.0110006128129772));
#48159=CARTESIAN_POINT('Ctrl Pts',(-0.0125000000000003,-0.0405912743898722,
-0.0110006128129772));
#48160=CARTESIAN_POINT('Ctrl Pts',(-0.0124999999999997,-0.0405287743898722,
-0.0110006128129772));
#48161=CARTESIAN_POINT('Ctrl Pts',(-0.0126316492011669,-0.0405368586610747,
-0.0110006128129772));
#48162=CARTESIAN_POINT('Ctrl Pts',(-0.01276252108623,-0.0405456791622419,
-0.0110227250980209));
#48163=CARTESIAN_POINT('Ctrl Pts',(-0.0130328277311265,-0.0405656219601255,
-0.0111170422529395));
#48164=CARTESIAN_POINT('Ctrl Pts',(-0.0131670559572858,-0.0405766655639931,
-0.0111960455111696));
#48165=CARTESIAN_POINT('Ctrl Pts',(-0.0133933766330118,-0.04059771872837,
-0.011397867342952));
#48166=CARTESIAN_POINT('Ctrl Pts',(-0.0134846584814694,-0.0406070718370568,
-0.0115172125231013));
#48167=CARTESIAN_POINT('Ctrl Pts',(-0.0136209585899284,-0.0406264070596672,
-0.01178989495723));
#48168=CARTESIAN_POINT('Ctrl Pts',(-0.0136622101576207,-0.040637181921104,
-0.0119418515963219));
#48169=CARTESIAN_POINT('Ctrl Pts',(-0.0136827973122141,-0.0406589967920181,
-0.0122495042270127));
#48170=CARTESIAN_POINT('Ctrl Pts',(-0.0136632805833491,-0.0406698224985453,
-0.0124021779286026));
#48171=CARTESIAN_POINT('Ctrl Pts',(-0.0135677388273238,-0.0406901843280577,
-0.0126893384825128));
#48172=CARTESIAN_POINT('Ctrl Pts',(-0.0134935014969514,-0.0406989849587138,
-0.0128213663775835));
#48173=CARTESIAN_POINT('Ctrl Pts',(-0.0132951011885483,-0.0407194644182024,
-0.0130553659152251));
#48174=CARTESIAN_POINT('Ctrl Pts',(-0.0131709389336876,-0.0407305638598057,
-0.013153378893578));
#48175=CARTESIAN_POINT('Ctrl Pts',(-0.0128968384027453,-0.0407523203922931,
-0.0132922826286567));
#48176=CARTESIAN_POINT('Ctrl Pts',(-0.0127505474487945,-0.040762780316068,
-0.0133339294822274));
#48177=CARTESIAN_POINT('Ctrl Pts',(-0.0124465718431961,-0.0407823703629212,
-0.0133599806716566));
#48178=CARTESIAN_POINT('Ctrl Pts',(-0.0122916981336773,-0.0407918616754559,
-0.0133427461909457));
#48179=CARTESIAN_POINT('Ctrl Pts',(-0.0119970897781494,-0.0408132673576658,
-0.0132492590527113));
#48180=CARTESIAN_POINT('Ctrl Pts',(-0.0118603276335144,-0.0408243402237439,
-0.0131738193068051));
#48181=CARTESIAN_POINT('Ctrl Pts',(-0.0116281332740182,-0.0408455448570753,
-0.0129778986950418));
#48182=CARTESIAN_POINT('Ctrl Pts',(-0.0115335545124742,-0.0408551950161598,
-0.0128609626405736));
#48183=CARTESIAN_POINT('Ctrl Pts',(-0.0113898949659606,-0.0408742670671095,
-0.0125919916862903));
#48184=CARTESIAN_POINT('Ctrl Pts',(-0.0113445553085114,-0.0408849568884158,
-0.0124412343584372));
#48185=CARTESIAN_POINT('Ctrl Pts',(-0.0113156036100202,-0.0409067502437709,
-0.0121338851592148));
#48186=CARTESIAN_POINT('Ctrl Pts',(-0.0113310948019909,-0.0409176377101116,
-0.0119803404660346));
#48187=CARTESIAN_POINT('Ctrl Pts',(-0.0114190735704893,-0.0409381609338805,
-0.0116909037873758));
#48188=CARTESIAN_POINT('Ctrl Pts',(-0.0114895011411379,-0.0409469813107143,
-0.0115574143384823));
#48189=CARTESIAN_POINT('Ctrl Pts',(-0.0116813502541496,-0.0409672455638847,
-0.0113181378577776));
#48190=CARTESIAN_POINT('Ctrl Pts',(-0.011803170496375,-0.0409783281814259,
-0.0112165429301995));
#48191=CARTESIAN_POINT('Ctrl Pts',(-0.0120742257497072,-0.0410001655970101,
-0.0110700832494386));
#48192=CARTESIAN_POINT('Ctrl Pts',(-0.0122197649150521,-0.0410107171066086,
-0.0110245510110078));
#48193=CARTESIAN_POINT('Ctrl Pts',(-0.012413223120115,-0.0410233605342975,
-0.0110030128206424));
#48194=CARTESIAN_POINT('Ctrl Pts',(-0.0124566341580664,-0.0410261113943963,
-0.0110006128129772));
#48195=CARTESIAN_POINT('Ctrl Pts',(-0.0124999999999995,-0.0410287743898722,
-0.0110006128129772));
#48196=CARTESIAN_POINT('Origin',(-0.0125,-0.0332787743898722,-0.0121758532865583));
#48197=CARTESIAN_POINT('',(-0.0125,-0.0412787743898722,-0.0133510937601389));
#48198=CARTESIAN_POINT('Ctrl Pts',(-0.0124999999999995,-0.0410287743898722,
-0.0110006128129772));
#48199=CARTESIAN_POINT('Ctrl Pts',(-0.0126092287281941,-0.0410354818719837,
-0.0110006128129772));
#48200=CARTESIAN_POINT('Ctrl Pts',(-0.0127181041723048,-0.041042707274917,
-0.0110158330752455));
#48201=CARTESIAN_POINT('Ctrl Pts',(-0.0129726558544088,-0.0410609229844915,
-0.0110887247682153));
#48202=CARTESIAN_POINT('Ctrl Pts',(-0.0131118546394638,-0.0410720166165589,
-0.011160529849858));
#48203=CARTESIAN_POINT('Ctrl Pts',(-0.0133498817563325,-0.0410933681826564,
-0.0113504921815146));
#48204=CARTESIAN_POINT('Ctrl Pts',(-0.01344776359209,-0.0411033746613979,
-0.0114650716774333));
#48205=CARTESIAN_POINT('Ctrl Pts',(-0.0135986340666582,-0.0411221828298088,
-0.0117303211264384));
#48206=CARTESIAN_POINT('Ctrl Pts',(-0.0136479608843726,-0.0411327811340702,
-0.0118797877998699));
#48207=CARTESIAN_POINT('Ctrl Pts',(-0.0136851419072229,-0.041154537430138,
-0.0121866143561989));
#48208=CARTESIAN_POINT('Ctrl Pts',(-0.0136736432711152,-0.0411654784113469,
-0.0123409137634469));
#48209=CARTESIAN_POINT('Ctrl Pts',(-0.0135931189592482,-0.0411861566755532,
-0.0126325369596714));
#48210=CARTESIAN_POINT('Ctrl Pts',(-0.0135263707615743,-0.0411950561575114,
-0.0127674827454629));
#48211=CARTESIAN_POINT('Ctrl Pts',(-0.0133409298539512,-0.0412151061529174,
-0.0130118152579657));
#48212=CARTESIAN_POINT('Ctrl Pts',(-0.0132214777881316,-0.0412261647845225,
-0.013116835445569));
#48213=CARTESIAN_POINT('Ctrl Pts',(-0.012994751607665,-0.0412447000772217,
-0.0132469364096699));
#48214=CARTESIAN_POINT('Ctrl Pts',(-0.0128981046712635,-0.0412520372742158,
-0.0132864903063074));
#48215=CARTESIAN_POINT('Ctrl Pts',(-0.0127003151194289,-0.0412660180234459,
-0.0133382465696333));
#48216=CARTESIAN_POINT('Ctrl Pts',(-0.0126003261699996,-0.0412726135931504,
-0.0133510937601389));
#48217=CARTESIAN_POINT('Ctrl Pts',(-0.0125,-0.0412787743898722,-0.0133510937601389));
#48218=CARTESIAN_POINT('',(-0.0133234078741649,-0.0412787743898722,-0.0130144173231741));
#48219=CARTESIAN_POINT('Origin',(-0.0125,-0.0412787743898622,-0.0121758532865681));
#48220=CARTESIAN_POINT('Ctrl Pts',(-0.0133234078741641,-0.0412787743898723,
-0.0130144173231748));
#48221=CARTESIAN_POINT('Ctrl Pts',(-0.0133804118658089,-0.0412732894303495,
-0.0129584436186877));
#48222=CARTESIAN_POINT('Ctrl Pts',(-0.0134315632959738,-0.0412679629049933,
-0.012896801738238));
#48223=CARTESIAN_POINT('Ctrl Pts',(-0.0135195542403086,-0.0412579077593073,
-0.0127655933841637));
#48224=CARTESIAN_POINT('Ctrl Pts',(-0.0135564571086821,-0.0412531998817753,
-0.0126966092776548));
#48225=CARTESIAN_POINT('Ctrl Pts',(-0.0136440663276741,-0.0412381566833437,
-0.0124844567698673));
#48226=CARTESIAN_POINT('Ctrl Pts',(-0.0136742623513739,-0.0412275341252433,
-0.0123346480473168));
#48227=CARTESIAN_POINT('Ctrl Pts',(-0.0136762096598467,-0.0412056406865503,
-0.0120258873842219));
#48228=CARTESIAN_POINT('Ctrl Pts',(-0.013645579755795,-0.0411945781586684,
-0.0118698738181379));
#48229=CARTESIAN_POINT('Ctrl Pts',(-0.0135277857927238,-0.0411744971694781,
-0.0115866739231869));
#48230=CARTESIAN_POINT('Ctrl Pts',(-0.0134447390385254,-0.041165612675012,
-0.0114610454727467));
#48231=CARTESIAN_POINT('Ctrl Pts',(-0.013233255127403,-0.0411449565068602,
-0.0112447231956079));
#48232=CARTESIAN_POINT('Ctrl Pts',(-0.0131057542452771,-0.041134022784958,
-0.0111571671413067));
#48233=CARTESIAN_POINT('Ctrl Pts',(-0.0128219593983773,-0.0411122601814962,
-0.0110348832174941));
#48234=CARTESIAN_POINT('Ctrl Pts',(-0.0126679731986536,-0.0411016482238126,
-0.0110022766869115));
#48235=CARTESIAN_POINT('Ctrl Pts',(-0.0125080492209149,-0.0410917694066109,
-0.0110006334823458));
#48236=CARTESIAN_POINT('Ctrl Pts',(-0.0125040242169056,-0.0410915215076713,
-0.0110006128129772));
#48237=CARTESIAN_POINT('Ctrl Pts',(-0.0125,-0.0410912743898722,-0.0110006128129772));
#48238=CARTESIAN_POINT('Origin',(-0.0125,-0.0332787743898722,-0.0121758532865583));
#48239=CARTESIAN_POINT('',(-0.0114490560961669,-0.0336537743898722,-0.0132461415239019));
#48240=CARTESIAN_POINT('Ctrl Pts',(-0.0125,-0.0340912743898723,-0.0136758532865583));
#48241=CARTESIAN_POINT('Ctrl Pts',(-0.0126865058990789,-0.034082301120619,
-0.0136758532865583));
#48242=CARTESIAN_POINT('Ctrl Pts',(-0.0128715278361501,-0.034072433085725,
-0.0136410714258962));
#48243=CARTESIAN_POINT('Ctrl Pts',(-0.0132281311189972,-0.0340514085142548,
-0.0135018418570036));
#48244=CARTESIAN_POINT('Ctrl Pts',(-0.0133949927443967,-0.0340404250085348,
-0.01339544846411));
#48245=CARTESIAN_POINT('Ctrl Pts',(-0.0136739994535825,-0.0340195903567862,
-0.0131286547971216));
#48246=CARTESIAN_POINT('Ctrl Pts',(-0.0137851071224222,-0.0340105306671531,
-0.0129724662776123));
#48247=CARTESIAN_POINT('Ctrl Pts',(-0.0139468394462665,-0.0339908834189933,
-0.0126188158107363));
#48248=CARTESIAN_POINT('Ctrl Pts',(-0.0139927523118229,-0.0339800215216224,
-0.0124233016580604));
#48249=CARTESIAN_POINT('Ctrl Pts',(-0.014005500907111,-0.0339582209318096,
-0.012030891041432));
#48250=CARTESIAN_POINT('Ctrl Pts',(-0.0139742069066131,-0.0339474941284978,
-0.0118378085818187));
#48251=CARTESIAN_POINT('Ctrl Pts',(-0.0138402998090658,-0.0339273583028217,
-0.0114753637196494));
#48252=CARTESIAN_POINT('Ctrl Pts',(-0.0137394094121885,-0.0339185005932602,
-0.0113092765352342));
#48253=CARTESIAN_POINT('Ctrl Pts',(-0.0134759260038074,-0.0338977738088027,
-0.0110194789450359));
#48254=CARTESIAN_POINT('Ctrl Pts',(-0.0133140161039499,-0.0338866737715003,
-0.0109003137749483));
#48255=CARTESIAN_POINT('Ctrl Pts',(-0.0129599674645763,-0.0338650565873608,
-0.0107353253776746));
#48256=CARTESIAN_POINT('Ctrl Pts',(-0.0127724186379477,-0.0338547298172228,
-0.0106884057493268));
#48257=CARTESIAN_POINT('Ctrl Pts',(-0.0123823768892991,-0.0338353773191225,
-0.0106672879434466));
#48258=CARTESIAN_POINT('Ctrl Pts',(-0.0121834681583582,-0.0338254806902787,
-0.0106961772399881));
#48259=CARTESIAN_POINT('Ctrl Pts',(-0.0118108159569984,-0.0338038583631424,
-0.0108291284705843));
#48260=CARTESIAN_POINT('Ctrl Pts',(-0.011640445856798,-0.03379283334398,
-0.0109309394907954));
#48261=CARTESIAN_POINT('Ctrl Pts',(-0.0113536108241396,-0.0337718363246642,
-0.011190019336208));
#48262=CARTESIAN_POINT('Ctrl Pts',(-0.0112381479744462,-0.0337625486841728,
-0.0113429159891473));
#48263=CARTESIAN_POINT('Ctrl Pts',(-0.0110664258426459,-0.0337431724471388,
-0.0116916882557595));
#48264=CARTESIAN_POINT('Ctrl Pts',(-0.0110149454443092,-0.0337323894588582,
-0.0118857820448108));
#48265=CARTESIAN_POINT('Ctrl Pts',(-0.0109909321084533,-0.0337105900329636,
-0.0122781717109137));
#48266=CARTESIAN_POINT('Ctrl Pts',(-0.0110168590975054,-0.0336997884198633,
-0.0124726007467192));
#48267=CARTESIAN_POINT('Ctrl Pts',(-0.0111164765646197,-0.0336834345323847,
-0.0127669707213344));
#48268=CARTESIAN_POINT('Ctrl Pts',(-0.0111664960347912,-0.0336777481173169,
-0.0128724957183858));
#48269=CARTESIAN_POINT('Ctrl Pts',(-0.0112907586203285,-0.0336662497993814,
-0.0130712060524302));
#48270=CARTESIAN_POINT('Ctrl Pts',(-0.0113648883876633,-0.0336601196457954,
-0.0131634950581508));
#48271=CARTESIAN_POINT('Ctrl Pts',(-0.0114490560961676,-0.0336537743898721,
-0.0132461415239026));
#48272=CARTESIAN_POINT('',(-0.011,-0.0336537743898722,-0.0121758532865583));
#48273=CARTESIAN_POINT('Origin',(-0.0125,-0.0336537743898622,-0.0121758532865683));
#48274=CARTESIAN_POINT('Ctrl Pts',(-0.011,-0.0336537743898722,-0.0121758532865583));
#48275=CARTESIAN_POINT('Ctrl Pts',(-0.011,-0.0336598131811276,-0.012067155043962));
#48276=CARTESIAN_POINT('Ctrl Pts',(-0.0110118138630113,-0.033665833784502,
-0.0119587841832224));
#48277=CARTESIAN_POINT('Ctrl Pts',(-0.0110581181358939,-0.033677491560012,
-0.0117489442240407));
#48278=CARTESIAN_POINT('Ctrl Pts',(-0.0110919458322686,-0.0336831013287107,
-0.0116479683874627));
#48279=CARTESIAN_POINT('Ctrl Pts',(-0.0112152450407584,-0.0336980621721267,
-0.0113786732059739));
#48280=CARTESIAN_POINT('Ctrl Pts',(-0.0113264197757561,-0.0337071248536072,
-0.0112225360169443));
#48281=CARTESIAN_POINT('Ctrl Pts',(-0.0116055473928061,-0.0337279620395113,
-0.0109558605389212));
#48282=CARTESIAN_POINT('Ctrl Pts',(-0.0117724639540535,-0.0337389462523888,
-0.010849536840037));
#48283=CARTESIAN_POINT('Ctrl Pts',(-0.0121403888485598,-0.0337606329661552,
-0.0107060797551005));
#48284=CARTESIAN_POINT('Ctrl Pts',(-0.0123381557525508,-0.0337708645442542,
-0.0106714213038118));
#48285=CARTESIAN_POINT('Ctrl Pts',(-0.0127278533839575,-0.033789880000058,
-0.0106810016155603));
#48286=CARTESIAN_POINT('Ctrl Pts',(-0.0129161653791794,-0.0338000829023891,
-0.0107221401560805));
#48287=CARTESIAN_POINT('Ctrl Pts',(-0.0132740104284418,-0.0338215665082543,
-0.0108757441606687));
#48288=CARTESIAN_POINT('Ctrl Pts',(-0.0134390322491703,-0.0338326640503305,
-0.0109894294975537));
#48289=CARTESIAN_POINT('Ctrl Pts',(-0.0137120587246422,-0.0338536255042462,
-0.0112711461111903));
#48290=CARTESIAN_POINT('Ctrl Pts',(-0.013818692018525,-0.0338626247106024,
-0.0114351590597035));
#48291=CARTESIAN_POINT('Ctrl Pts',(-0.0139634404810105,-0.0338825695688823,
-0.0117941665087412));
#48292=CARTESIAN_POINT('Ctrl Pts',(-0.014000384202204,-0.033893207922565,
-0.0119856568750299));
#48293=CARTESIAN_POINT('Ctrl Pts',(-0.0139995943191151,-0.0339151032556719,
-0.0123797728709541));
#48294=CARTESIAN_POINT('Ctrl Pts',(-0.0139588294412269,-0.0339261489516028,
-0.0125785953977098));
#48295=CARTESIAN_POINT('Ctrl Pts',(-0.0138055677454885,-0.0339461458362204,
-0.0129385393208265));
#48296=CARTESIAN_POINT('Ctrl Pts',(-0.0136984249594945,-0.033955058052392,
-0.0130977980561763));
#48297=CARTESIAN_POINT('Ctrl Pts',(-0.0134265815783181,-0.0339757411420657,
-0.0133715427365305));
#48298=CARTESIAN_POINT('Ctrl Pts',(-0.0132630145914569,-0.0339866791278434,
-0.0134820038928433));
#48299=CARTESIAN_POINT('Ctrl Pts',(-0.0128997595351416,-0.0340084116489645,
-0.0136351984395573));
#48300=CARTESIAN_POINT('Ctrl Pts',(-0.0127030752966334,-0.0340189880275693,
-0.0136752809751883));
#48301=CARTESIAN_POINT('Ctrl Pts',(-0.0125028480827704,-0.0340286373050992,
-0.0136758512587937));
#48302=CARTESIAN_POINT('Ctrl Pts',(-0.0125014239907197,-0.0340287058780863,
-0.0136758532865732));
#48303=CARTESIAN_POINT('Ctrl Pts',(-0.0124999999842539,-0.0340287743906298,
-0.0136758532865583));
#48304=CARTESIAN_POINT('Origin',(-0.0125,-0.0429287743898722,-0.012175853286558));
#48305=CARTESIAN_POINT('',(-0.0115,-0.0429287743898722,-0.0127532035557476));
#48306=CARTESIAN_POINT('',(-0.0115,-0.0429287743898722,-0.0115985030173684));
#48307=CARTESIAN_POINT('Ctrl Pts',(-0.01149999999999,-0.0429287743898622,
-0.0127532035557576));
#48308=CARTESIAN_POINT('Ctrl Pts',(-0.01149999999999,-0.0426400992552674,
-0.012175853286548));
#48309=CARTESIAN_POINT('Ctrl Pts',(-0.01149999999999,-0.0429287743898621,
-0.0115985030173584));
#48310=CARTESIAN_POINT('Origin',(-0.0125,-0.0429287743898722,-0.012175853286558));
#48311=CARTESIAN_POINT('Origin',(-0.0125,-0.0429287743898722,-0.012175853286558));
#48312=CARTESIAN_POINT('',(-0.01535,-0.0415262743898622,-0.0121758532865581));
#48313=CARTESIAN_POINT('Origin',(-0.0125,-0.0415262743898622,-0.012175853286558));
#48314=CARTESIAN_POINT('',(-0.01535,-0.0412787743898622,-0.0121758532865581));
#48315=CARTESIAN_POINT('',(-0.01535,-0.0429287743898722,-0.012175853286558));
#48316=CARTESIAN_POINT('Origin',(-0.0125,-0.0412787743898622,-0.0121758532865581));
#48317=CARTESIAN_POINT('Origin',(-0.0125,-0.0401339415021717,-0.0121758532865581));
#48318=CARTESIAN_POINT('',(-0.01099999999999,-0.0429287743898722,-0.012175853286558));
#48319=CARTESIAN_POINT('Origin',(-0.0125,-0.0429287743898722,-0.012175853286558));
#48320=CARTESIAN_POINT('Origin',(-0.0125,-0.0332787743898722,-0.0121758532865583));
#48321=CARTESIAN_POINT('',(-0.0125000000000002,-0.0334556573285548,-0.0108739703478756));
#48322=CARTESIAN_POINT('Ctrl Pts',(-0.0125000000000003,-0.0334556573285548,
-0.0108739703478756));
#48323=CARTESIAN_POINT('Ctrl Pts',(-0.0125169619654304,-0.0334562534372814,
-0.0108733742391491));
#48324=CARTESIAN_POINT('Ctrl Pts',(-0.0125342659303904,-0.0334568674696437,
-0.010873091500204));
#48325=CARTESIAN_POINT('Ctrl Pts',(-0.0127142374842031,-0.0334633195025884,
-0.0108738056395374));
#48326=CARTESIAN_POINT('Ctrl Pts',(-0.0128750636210282,-0.0334696175052002,
-0.0109042115888364));
#48327=CARTESIAN_POINT('Ctrl Pts',(-0.0131894625396203,-0.0334829915682975,
-0.0110260726974655));
#48328=CARTESIAN_POINT('Ctrl Pts',(-0.0133384354713308,-0.0334899589420527,
-0.0111208842865654));
#48329=CARTESIAN_POINT('Ctrl Pts',(-0.0136233142077324,-0.0335048715041686,
-0.0113937017075726));
#48330=CARTESIAN_POINT('Ctrl Pts',(-0.0137145126457393,-0.0335107921955676,
-0.0115560798170348));
#48331=CARTESIAN_POINT('Ctrl Pts',(-0.013836412057102,-0.0335218194362954,
-0.0118362950864762));
#48332=CARTESIAN_POINT('Ctrl Pts',(-0.0138749679863545,-0.0335284104154649,
-0.0120060666246319));
#48333=CARTESIAN_POINT('Ctrl Pts',(-0.0138878583928345,-0.0335419895541559,
-0.0123611092928754));
#48334=CARTESIAN_POINT('Ctrl Pts',(-0.013858168381701,-0.0335488446104762,
-0.012543202792378));
#48335=CARTESIAN_POINT('Ctrl Pts',(-0.0137239184314785,-0.0335621176892281,
-0.0129003899279641));
#48336=CARTESIAN_POINT('Ctrl Pts',(-0.0136197865853707,-0.0335679593652523,
-0.0130553133704129));
#48337=CARTESIAN_POINT('Ctrl Pts',(-0.0133828554998308,-0.0335804785640777,
-0.0133114304431047));
#48338=CARTESIAN_POINT('Ctrl Pts',(-0.0132339030198478,-0.0335872828023574,
-0.0134207688274427));
#48339=CARTESIAN_POINT('Ctrl Pts',(-0.0128973989337005,-0.0336008366112022,
-0.013580065947054));
#48340=CARTESIAN_POINT('Ctrl Pts',(-0.0127120297926521,-0.0336074446543075,
-0.013626361460001));
#48341=CARTESIAN_POINT('Ctrl Pts',(-0.0123890809311569,-0.0336176648068571,
-0.0136416742981176));
#48342=CARTESIAN_POINT('Ctrl Pts',(-0.0122064915470854,-0.0336235752447987,
-0.0136317811264738));
#48343=CARTESIAN_POINT('Ctrl Pts',(-0.0119011769375834,-0.033634839900917,
-0.0135346618859548));
#48344=CARTESIAN_POINT('Ctrl Pts',(-0.011803178818122,-0.0336386438976925,
-0.01349140338373));
#48345=CARTESIAN_POINT('Ctrl Pts',(-0.011616721475776,-0.0336462744782102,
-0.0133837962791914));
#48346=CARTESIAN_POINT('Ctrl Pts',(-0.0115290003612504,-0.0336500773154259,
-0.0133194594616579));
#48347=CARTESIAN_POINT('Ctrl Pts',(-0.0114490560961663,-0.0336537743898722,
-0.0132461415239012));
#48348=CARTESIAN_POINT('',(-0.0125,-0.0332787743898522,-0.0110508532865583));
#48349=CARTESIAN_POINT('',(-0.0125,-0.0332787743898722,-0.0110508532865583));
#48350=CARTESIAN_POINT('Origin',(-0.0125,-0.0332787743898622,-0.0121758532865683));
#48351=CARTESIAN_POINT('Ctrl Pts',(-0.0118107823295555,-0.0333290148634531,
-0.0131277824716817));
#48352=CARTESIAN_POINT('Ctrl Pts',(-0.0117098836135435,-0.0333344102607298,
-0.0130613906751724));
#48353=CARTESIAN_POINT('Ctrl Pts',(-0.0116198784781834,-0.0333396492883259,
-0.0129797529105212));
#48354=CARTESIAN_POINT('Ctrl Pts',(-0.0114414223014775,-0.0333512035863472,
-0.0127588129791921));
#48355=CARTESIAN_POINT('Ctrl Pts',(-0.0113846754137903,-0.0333562632427286,
-0.012634703796091));
#48356=CARTESIAN_POINT('Ctrl Pts',(-0.0112970495906885,-0.0333667457898664,
-0.0123985832942005));
#48357=CARTESIAN_POINT('Ctrl Pts',(-0.011271377129027,-0.0333736872268549,
-0.012239621846769));
#48358=CARTESIAN_POINT('Ctrl Pts',(-0.0112822066210525,-0.0333869145783074,
-0.0119314481530083));
#48359=CARTESIAN_POINT('Ctrl Pts',(-0.0113145866019927,-0.0333931041250635,
-0.0117848682419702));
#48360=CARTESIAN_POINT('Ctrl Pts',(-0.0114373374471298,-0.0334052173218674,
-0.0114942642325391));
#48361=CARTESIAN_POINT('Ctrl Pts',(-0.0115333961603035,-0.0334113688630093,
-0.0113542906673467));
#48362=CARTESIAN_POINT('Ctrl Pts',(-0.0117691046885344,-0.0334248437865918,
-0.0111232097728938));
#48363=CARTESIAN_POINT('Ctrl Pts',(-0.0119066804715653,-0.033431670970877,
-0.0110323315484945));
#48364=CARTESIAN_POINT('Ctrl Pts',(-0.0121561556995369,-0.03344260130431,
-0.0109291835302698));
#48365=CARTESIAN_POINT('Ctrl Pts',(-0.0123055738989379,-0.0334488244473071,
-0.0108808032291233));
#48366=CARTESIAN_POINT('Ctrl Pts',(-0.0125000000000003,-0.0334556573285548,
-0.0108739703478756));
#48367=CARTESIAN_POINT('Ctrl Pts',(-0.0126906536866924,-0.033329014863453,
-0.013335526232907));
#48368=CARTESIAN_POINT('Ctrl Pts',(-0.0125279740652511,-0.0333555799941742,
-0.0133891929900586));
#48369=CARTESIAN_POINT('Ctrl Pts',(-0.0123661654682192,-0.0333769910786535,
-0.0134004654915067));
#48370=CARTESIAN_POINT('Ctrl Pts',(-0.0120636132777685,-0.033422430336011,
-0.0133770070013701));
#48371=CARTESIAN_POINT('Ctrl Pts',(-0.0119118500123405,-0.033446157237979,
-0.0133369191787743));
#48372=CARTESIAN_POINT('Ctrl Pts',(-0.0116282619419881,-0.0334925065907822,
-0.0132037360390814));
#48373=CARTESIAN_POINT('Ctrl Pts',(-0.0114990164583931,-0.0335147508070644,
-0.0131111612382107));
#48374=CARTESIAN_POINT('Ctrl Pts',(-0.0112596605338127,-0.0335595060136002,
-0.0128628817337503));
#48375=CARTESIAN_POINT('Ctrl Pts',(-0.0111769727528737,-0.0335788237730028,
-0.0127188109969073));
#48376=CARTESIAN_POINT('Ctrl Pts',(-0.0110621505149206,-0.0336140810688488,
-0.0124717801731789));
#48377=CARTESIAN_POINT('Ctrl Pts',(-0.0110197071274521,-0.0336340672624201,
-0.012325779104587));
#48378=CARTESIAN_POINT('Ctrl Pts',(-0.011,-0.0336537743898722,-0.0121758532865583));
#48379=CARTESIAN_POINT('Origin',(-0.0125,-0.0332787743898722,-0.0136758532865583));
#48380=CARTESIAN_POINT('Ctrl Pts',(-0.0124879391534221,-0.033279517212585,
-0.0133510318715922));
#48381=CARTESIAN_POINT('Ctrl Pts',(-0.0118174660837529,-0.0333209333633904,
-0.0133441508128911));
#48382=CARTESIAN_POINT('Ctrl Pts',(-0.0114822118943233,-0.0333621077232055,
-0.0127634735233487));
#48383=CARTESIAN_POINT('Ctrl Pts',(-0.0111429491924311,-0.0334037743898722,
-0.0121758532865583));
#48384=CARTESIAN_POINT('Ctrl Pts',(-0.0114822118943233,-0.0334454410565388,
-0.0115882330497679));
#48385=CARTESIAN_POINT('Ctrl Pts',(-0.0118214745962156,-0.0334871077232055,
-0.0110006128129775));
#48386=CARTESIAN_POINT('Ctrl Pts',(-0.0125,-0.0335287743898722,-0.0110006128129775));
#48387=CARTESIAN_POINT('Ctrl Pts',(-0.0131785254037844,-0.0335704410565388,
-0.0110006128129775));
#48388=CARTESIAN_POINT('Ctrl Pts',(-0.0135177881056766,-0.0336121077232055,
-0.0115882330497679));
#48389=CARTESIAN_POINT('Ctrl Pts',(-0.0138570508075689,-0.0336537743898722,
-0.0121758532865583));
#48390=CARTESIAN_POINT('Ctrl Pts',(-0.0135177881056766,-0.0336954410565389,
-0.0127634735233487));
#48391=CARTESIAN_POINT('Ctrl Pts',(-0.0131785254037844,-0.0337371077232056,
-0.0133510937601391));
#48392=CARTESIAN_POINT('Ctrl Pts',(-0.0125,-0.0337787743898723,-0.0133510937601391));
#48393=CARTESIAN_POINT('Ctrl Pts',(-0.0118214745962156,-0.0338204410565389,
-0.0133510937601391));
#48394=CARTESIAN_POINT('Ctrl Pts',(-0.0114822118943233,-0.0338621077232055,
-0.0127634735233487));
#48395=CARTESIAN_POINT('Ctrl Pts',(-0.0111429491924311,-0.0339037743898722,
-0.0121758532865583));
#48396=CARTESIAN_POINT('Ctrl Pts',(-0.0114822118943233,-0.0339454410565388,
-0.0115882330497679));
#48397=CARTESIAN_POINT('Ctrl Pts',(-0.0118214745962156,-0.0339871077232055,
-0.0110006128129775));
#48398=CARTESIAN_POINT('Ctrl Pts',(-0.0125,-0.0340287743898722,-0.0110006128129775));
#48399=CARTESIAN_POINT('Ctrl Pts',(-0.0131785254037844,-0.0340704410565388,
-0.0110006128129775));
#48400=CARTESIAN_POINT('Ctrl Pts',(-0.0135177881056766,-0.0341121077232055,
-0.0115882330497679));
#48401=CARTESIAN_POINT('Ctrl Pts',(-0.0138570508075689,-0.0341537743898722,
-0.0121758532865583));
#48402=CARTESIAN_POINT('Ctrl Pts',(-0.0135177881056766,-0.0341954410565389,
-0.0127634735233487));
#48403=CARTESIAN_POINT('Ctrl Pts',(-0.0131785254037844,-0.0342371077232056,
-0.0133510937601391));
#48404=CARTESIAN_POINT('Ctrl Pts',(-0.0125,-0.0342787743898723,-0.0133510937601391));
#48405=CARTESIAN_POINT('Ctrl Pts',(-0.0118214745962156,-0.0343204410565389,
-0.0133510937601391));
#48406=CARTESIAN_POINT('Ctrl Pts',(-0.0114822118943233,-0.0343621077232055,
-0.0127634735233487));
#48407=CARTESIAN_POINT('Ctrl Pts',(-0.0111429491924311,-0.0344037743898722,
-0.0121758532865583));
#48408=CARTESIAN_POINT('Ctrl Pts',(-0.0114822118943233,-0.0344454410565389,
-0.0115882330497679));
#48409=CARTESIAN_POINT('Ctrl Pts',(-0.0118214745962156,-0.0344871077232055,
-0.0110006128129775));
#48410=CARTESIAN_POINT('Ctrl Pts',(-0.0125,-0.0345287743898722,-0.0110006128129775));
#48411=CARTESIAN_POINT('Ctrl Pts',(-0.0131785254037844,-0.0345704410565388,
-0.0110006128129775));
#48412=CARTESIAN_POINT('Ctrl Pts',(-0.0135177881056766,-0.0346121077232055,
-0.0115882330497679));
#48413=CARTESIAN_POINT('Ctrl Pts',(-0.0138570508075689,-0.0346537743898722,
-0.0121758532865583));
#48414=CARTESIAN_POINT('Ctrl Pts',(-0.0135177881056766,-0.0346954410565389,
-0.0127634735233487));
#48415=CARTESIAN_POINT('Ctrl Pts',(-0.0131785254037844,-0.0347371077232056,
-0.0133510937601391));
#48416=CARTESIAN_POINT('Ctrl Pts',(-0.0125,-0.0347787743898723,-0.0133510937601391));
#48417=CARTESIAN_POINT('Ctrl Pts',(-0.0118214745962156,-0.0348204410565389,
-0.0133510937601391));
#48418=CARTESIAN_POINT('Ctrl Pts',(-0.0114822118943233,-0.0348621077232055,
-0.0127634735233487));
#48419=CARTESIAN_POINT('Ctrl Pts',(-0.0111429491924311,-0.0349037743898722,
-0.0121758532865583));
#48420=CARTESIAN_POINT('Ctrl Pts',(-0.0114822118943233,-0.0349454410565389,
-0.0115882330497679));
#48421=CARTESIAN_POINT('Ctrl Pts',(-0.0118214745962156,-0.0349871077232055,
-0.0110006128129774));
#48422=CARTESIAN_POINT('Ctrl Pts',(-0.0125,-0.0350287743898722,-0.0110006128129774));
#48423=CARTESIAN_POINT('Ctrl Pts',(-0.0131785254037844,-0.0350704410565388,
-0.0110006128129774));
#48424=CARTESIAN_POINT('Ctrl Pts',(-0.0135177881056766,-0.0351121077232055,
-0.0115882330497678));
#48425=CARTESIAN_POINT('Ctrl Pts',(-0.0138570508075689,-0.0351537743898722,
-0.0121758532865583));
#48426=CARTESIAN_POINT('Ctrl Pts',(-0.0135177881056766,-0.0351954410565389,
-0.0127634735233487));
#48427=CARTESIAN_POINT('Ctrl Pts',(-0.0131785254037844,-0.0352371077232056,
-0.0133510937601391));
#48428=CARTESIAN_POINT('Ctrl Pts',(-0.0125,-0.0352787743898723,-0.0133510937601391));
#48429=CARTESIAN_POINT('Ctrl Pts',(-0.0118214745962156,-0.0353204410565389,
-0.0133510937601391));
#48430=CARTESIAN_POINT('Ctrl Pts',(-0.0114822118943233,-0.0353621077232055,
-0.0127634735233487));
#48431=CARTESIAN_POINT('Ctrl Pts',(-0.0111429491924311,-0.0354037743898722,
-0.0121758532865583));
#48432=CARTESIAN_POINT('Ctrl Pts',(-0.0114822118943233,-0.0354454410565389,
-0.0115882330497678));
#48433=CARTESIAN_POINT('Ctrl Pts',(-0.0118214745962156,-0.0354871077232055,
-0.0110006128129774));
#48434=CARTESIAN_POINT('Ctrl Pts',(-0.0125,-0.0355287743898722,-0.0110006128129774));
#48435=CARTESIAN_POINT('Ctrl Pts',(-0.0131785254037844,-0.0355704410565388,
-0.0110006128129774));
#48436=CARTESIAN_POINT('Ctrl Pts',(-0.0135177881056766,-0.0356121077232055,
-0.0115882330497678));
#48437=CARTESIAN_POINT('Ctrl Pts',(-0.0138570508075689,-0.0356537743898722,
-0.0121758532865583));
#48438=CARTESIAN_POINT('Ctrl Pts',(-0.0135177881056766,-0.0356954410565389,
-0.0127634735233487));
#48439=CARTESIAN_POINT('Ctrl Pts',(-0.0131785254037844,-0.0357371077232056,
-0.0133510937601391));
#48440=CARTESIAN_POINT('Ctrl Pts',(-0.0125,-0.0357787743898723,-0.0133510937601391));
#48441=CARTESIAN_POINT('Ctrl Pts',(-0.0118214745962156,-0.0358204410565389,
-0.0133510937601391));
#48442=CARTESIAN_POINT('Ctrl Pts',(-0.0114822118943233,-0.0358621077232055,
-0.0127634735233487));
#48443=CARTESIAN_POINT('Ctrl Pts',(-0.0111429491924311,-0.0359037743898722,
-0.0121758532865583));
#48444=CARTESIAN_POINT('Ctrl Pts',(-0.0114822118943233,-0.0359454410565389,
-0.0115882330497678));
#48445=CARTESIAN_POINT('Ctrl Pts',(-0.0118214745962156,-0.0359871077232055,
-0.0110006128129774));
#48446=CARTESIAN_POINT('Ctrl Pts',(-0.0125,-0.0360287743898721,-0.0110006128129774));
#48447=CARTESIAN_POINT('Ctrl Pts',(-0.0131785254037844,-0.0360704410565388,
-0.0110006128129774));
#48448=CARTESIAN_POINT('Ctrl Pts',(-0.0135177881056766,-0.0361121077232055,
-0.0115882330497678));
#48449=CARTESIAN_POINT('Ctrl Pts',(-0.0138570508075689,-0.0361537743898722,
-0.0121758532865582));
#48450=CARTESIAN_POINT('Ctrl Pts',(-0.0135177881056766,-0.0361954410565389,
-0.0127634735233486));
#48451=CARTESIAN_POINT('Ctrl Pts',(-0.0131785254037844,-0.0362371077232056,
-0.013351093760139));
#48452=CARTESIAN_POINT('Ctrl Pts',(-0.0125,-0.0362787743898722,-0.0133510937601391));
#48453=CARTESIAN_POINT('Ctrl Pts',(-0.0118214745962156,-0.0363204410565389,
-0.013351093760139));
#48454=CARTESIAN_POINT('Ctrl Pts',(-0.0114822118943233,-0.0363621077232055,
-0.0127634735233486));
#48455=CARTESIAN_POINT('Ctrl Pts',(-0.0111429491924311,-0.0364037743898722,
-0.0121758532865582));
#48456=CARTESIAN_POINT('Ctrl Pts',(-0.0114822118943233,-0.0364454410565389,
-0.0115882330497678));
#48457=CARTESIAN_POINT('Ctrl Pts',(-0.0118214745962156,-0.0364871077232055,
-0.0110006128129774));
#48458=CARTESIAN_POINT('Ctrl Pts',(-0.0125,-0.0365287743898721,-0.0110006128129774));
#48459=CARTESIAN_POINT('Ctrl Pts',(-0.0131785254037844,-0.0365704410565388,
-0.0110006128129774));
#48460=CARTESIAN_POINT('Ctrl Pts',(-0.0135177881056766,-0.0366121077232055,
-0.0115882330497678));
#48461=CARTESIAN_POINT('Ctrl Pts',(-0.0138570508075689,-0.0366537743898722,
-0.0121758532865582));
#48462=CARTESIAN_POINT('Ctrl Pts',(-0.0135177881056766,-0.0366954410565389,
-0.0127634735233486));
#48463=CARTESIAN_POINT('Ctrl Pts',(-0.0131785254037844,-0.0367371077232056,
-0.013351093760139));
#48464=CARTESIAN_POINT('Ctrl Pts',(-0.0125,-0.0367787743898722,-0.013351093760139));
#48465=CARTESIAN_POINT('Ctrl Pts',(-0.0118214745962156,-0.0368204410565389,
-0.013351093760139));
#48466=CARTESIAN_POINT('Ctrl Pts',(-0.0114822118943233,-0.0368621077232055,
-0.0127634735233486));
#48467=CARTESIAN_POINT('Ctrl Pts',(-0.0111429491924311,-0.0369037743898722,
-0.0121758532865582));
#48468=CARTESIAN_POINT('Ctrl Pts',(-0.0114822118943233,-0.0369454410565389,
-0.0115882330497678));
#48469=CARTESIAN_POINT('Ctrl Pts',(-0.0118214745962156,-0.0369871077232055,
-0.0110006128129774));
#48470=CARTESIAN_POINT('Ctrl Pts',(-0.0125,-0.0370287743898721,-0.0110006128129774));
#48471=CARTESIAN_POINT('Ctrl Pts',(-0.0131785254037844,-0.0370704410565389,
-0.0110006128129774));
#48472=CARTESIAN_POINT('Ctrl Pts',(-0.0135177881056766,-0.0371121077232055,
-0.0115882330497678));
#48473=CARTESIAN_POINT('Ctrl Pts',(-0.0138570508075689,-0.0371537743898722,
-0.0121758532865582));
#48474=CARTESIAN_POINT('Ctrl Pts',(-0.0135177881056766,-0.0371954410565389,
-0.0127634735233486));
#48475=CARTESIAN_POINT('Ctrl Pts',(-0.0131785254037844,-0.0372371077232056,
-0.013351093760139));
#48476=CARTESIAN_POINT('Ctrl Pts',(-0.0125,-0.0372787743898722,-0.013351093760139));
#48477=CARTESIAN_POINT('Ctrl Pts',(-0.0118214745962156,-0.0373204410565389,
-0.013351093760139));
#48478=CARTESIAN_POINT('Ctrl Pts',(-0.0114822118943233,-0.0373621077232055,
-0.0127634735233486));
#48479=CARTESIAN_POINT('Ctrl Pts',(-0.0111429491924311,-0.0374037743898722,
-0.0121758532865582));
#48480=CARTESIAN_POINT('Ctrl Pts',(-0.0114822118943233,-0.0374454410565389,
-0.0115882330497678));
#48481=CARTESIAN_POINT('Ctrl Pts',(-0.0118214745962156,-0.0374871077232055,
-0.0110006128129774));
#48482=CARTESIAN_POINT('Ctrl Pts',(-0.0125,-0.0375287743898721,-0.0110006128129774));
#48483=CARTESIAN_POINT('Ctrl Pts',(-0.0131785254037844,-0.0375704410565388,
-0.0110006128129773));
#48484=CARTESIAN_POINT('Ctrl Pts',(-0.0135177881056766,-0.0376121077232055,
-0.0115882330497678));
#48485=CARTESIAN_POINT('Ctrl Pts',(-0.0138570508075689,-0.0376537743898722,
-0.0121758532865582));
#48486=CARTESIAN_POINT('Ctrl Pts',(-0.0135177881056766,-0.0376954410565389,
-0.0127634735233486));
#48487=CARTESIAN_POINT('Ctrl Pts',(-0.0131785254037844,-0.0377371077232055,
-0.013351093760139));
#48488=CARTESIAN_POINT('Ctrl Pts',(-0.0125,-0.0377787743898722,-0.013351093760139));
#48489=CARTESIAN_POINT('Ctrl Pts',(-0.0118214745962156,-0.0378204410565389,
-0.013351093760139));
#48490=CARTESIAN_POINT('Ctrl Pts',(-0.0114822118943233,-0.0378621077232056,
-0.0127634735233486));
#48491=CARTESIAN_POINT('Ctrl Pts',(-0.0111429491924311,-0.0379037743898722,
-0.0121758532865582));
#48492=CARTESIAN_POINT('Ctrl Pts',(-0.0114822118943233,-0.0379454410565389,
-0.0115882330497678));
#48493=CARTESIAN_POINT('Ctrl Pts',(-0.0118214745962156,-0.0379871077232055,
-0.0110006128129773));
#48494=CARTESIAN_POINT('Ctrl Pts',(-0.0125,-0.0380287743898721,-0.0110006128129773));
#48495=CARTESIAN_POINT('Ctrl Pts',(-0.0131785254037844,-0.0380704410565388,
-0.0110006128129773));
#48496=CARTESIAN_POINT('Ctrl Pts',(-0.0135177881056766,-0.0381121077232055,
-0.0115882330497677));
#48497=CARTESIAN_POINT('Ctrl Pts',(-0.0138570508075689,-0.0381537743898722,
-0.0121758532865582));
#48498=CARTESIAN_POINT('Ctrl Pts',(-0.0135177881056766,-0.0381954410565388,
-0.0127634735233486));
#48499=CARTESIAN_POINT('Ctrl Pts',(-0.0131785254037844,-0.0382371077232056,
-0.013351093760139));
#48500=CARTESIAN_POINT('Ctrl Pts',(-0.0125,-0.0382787743898722,-0.013351093760139));
#48501=CARTESIAN_POINT('Ctrl Pts',(-0.0118214745962156,-0.0383204410565389,
-0.013351093760139));
#48502=CARTESIAN_POINT('Ctrl Pts',(-0.0114822118943233,-0.0383621077232056,
-0.0127634735233486));
#48503=CARTESIAN_POINT('Ctrl Pts',(-0.0111429491924311,-0.0384037743898722,
-0.0121758532865581));
#48504=CARTESIAN_POINT('Ctrl Pts',(-0.0114822118943233,-0.0384454410565388,
-0.0115882330497677));
#48505=CARTESIAN_POINT('Ctrl Pts',(-0.0118214745962156,-0.0384871077232055,
-0.0110006128129773));
#48506=CARTESIAN_POINT('Ctrl Pts',(-0.0125,-0.0385287743898722,-0.0110006128129773));
#48507=CARTESIAN_POINT('Ctrl Pts',(-0.0131785254037844,-0.0385704410565388,
-0.0110006128129773));
#48508=CARTESIAN_POINT('Ctrl Pts',(-0.0135177881056766,-0.0386121077232055,
-0.0115882330497677));
#48509=CARTESIAN_POINT('Ctrl Pts',(-0.0138570508075689,-0.0386537743898722,
-0.0121758532865581));
#48510=CARTESIAN_POINT('Ctrl Pts',(-0.0135177881056766,-0.0386954410565388,
-0.0127634735233486));
#48511=CARTESIAN_POINT('Ctrl Pts',(-0.0131785254037844,-0.0387371077232056,
-0.013351093760139));
#48512=CARTESIAN_POINT('Ctrl Pts',(-0.0125,-0.0387787743898722,-0.013351093760139));
#48513=CARTESIAN_POINT('Ctrl Pts',(-0.0118214745962156,-0.0388204410565389,
-0.013351093760139));
#48514=CARTESIAN_POINT('Ctrl Pts',(-0.0114822118943233,-0.0388621077232056,
-0.0127634735233486));
#48515=CARTESIAN_POINT('Ctrl Pts',(-0.0111429491924311,-0.0389037743898722,
-0.0121758532865581));
#48516=CARTESIAN_POINT('Ctrl Pts',(-0.0114822118943233,-0.0389454410565388,
-0.0115882330497677));
#48517=CARTESIAN_POINT('Ctrl Pts',(-0.0118214745962156,-0.0389871077232055,
-0.0110006128129773));
#48518=CARTESIAN_POINT('Ctrl Pts',(-0.0125,-0.0390287743898722,-0.0110006128129773));
#48519=CARTESIAN_POINT('Ctrl Pts',(-0.0131785254037844,-0.0390704410565388,
-0.0110006128129773));
#48520=CARTESIAN_POINT('Ctrl Pts',(-0.0135177881056766,-0.0391121077232055,
-0.0115882330497677));
#48521=CARTESIAN_POINT('Ctrl Pts',(-0.0138570508075689,-0.0391537743898722,
-0.0121758532865581));
#48522=CARTESIAN_POINT('Ctrl Pts',(-0.0135177881056766,-0.0391954410565388,
-0.0127634735233485));
#48523=CARTESIAN_POINT('Ctrl Pts',(-0.0131785254037844,-0.0392371077232056,
-0.013351093760139));
#48524=CARTESIAN_POINT('Ctrl Pts',(-0.0125,-0.0392787743898722,-0.013351093760139));
#48525=CARTESIAN_POINT('Ctrl Pts',(-0.0118214745962156,-0.0393204410565389,
-0.013351093760139));
#48526=CARTESIAN_POINT('Ctrl Pts',(-0.0114822118943233,-0.0393621077232056,
-0.0127634735233485));
#48527=CARTESIAN_POINT('Ctrl Pts',(-0.0111429491924311,-0.0394037743898722,
-0.0121758532865581));
#48528=CARTESIAN_POINT('Ctrl Pts',(-0.0114822118943233,-0.0394454410565388,
-0.0115882330497677));
#48529=CARTESIAN_POINT('Ctrl Pts',(-0.0118214745962156,-0.0394871077232055,
-0.0110006128129773));
#48530=CARTESIAN_POINT('Ctrl Pts',(-0.0125,-0.0395287743898722,-0.0110006128129773));
#48531=CARTESIAN_POINT('Ctrl Pts',(-0.0131785254037844,-0.0395704410565388,
-0.0110006128129773));
#48532=CARTESIAN_POINT('Ctrl Pts',(-0.0135177881056766,-0.0396121077232055,
-0.0115882330497677));
#48533=CARTESIAN_POINT('Ctrl Pts',(-0.0138570508075689,-0.0396537743898722,
-0.0121758532865581));
#48534=CARTESIAN_POINT('Ctrl Pts',(-0.0135177881056766,-0.0396954410565388,
-0.0127634735233485));
#48535=CARTESIAN_POINT('Ctrl Pts',(-0.0131785254037844,-0.0397371077232056,
-0.0133510937601389));
#48536=CARTESIAN_POINT('Ctrl Pts',(-0.0125,-0.0397787743898722,-0.0133510937601389));
#48537=CARTESIAN_POINT('Ctrl Pts',(-0.0118214745962156,-0.0398204410565389,
-0.0133510937601389));
#48538=CARTESIAN_POINT('Ctrl Pts',(-0.0114822118943233,-0.0398621077232056,
-0.0127634735233485));
#48539=CARTESIAN_POINT('Ctrl Pts',(-0.0111429491924311,-0.0399037743898722,
-0.0121758532865581));
#48540=CARTESIAN_POINT('Ctrl Pts',(-0.0114822118943233,-0.0399454410565388,
-0.0115882330497677));
#48541=CARTESIAN_POINT('Ctrl Pts',(-0.0118214745962156,-0.0399871077232055,
-0.0110006128129773));
#48542=CARTESIAN_POINT('Ctrl Pts',(-0.0125,-0.0400287743898722,-0.0110006128129773));
#48543=CARTESIAN_POINT('Ctrl Pts',(-0.0131785254037844,-0.0400704410565388,
-0.0110006128129773));
#48544=CARTESIAN_POINT('Ctrl Pts',(-0.0135177881056766,-0.0401121077232055,
-0.0115882330497677));
#48545=CARTESIAN_POINT('Ctrl Pts',(-0.0138570508075689,-0.0401537743898722,
-0.0121758532865581));
#48546=CARTESIAN_POINT('Ctrl Pts',(-0.0135177881056766,-0.0401954410565388,
-0.0127634735233485));
#48547=CARTESIAN_POINT('Ctrl Pts',(-0.0131785254037844,-0.0402371077232055,
-0.0133510937601389));
#48548=CARTESIAN_POINT('Ctrl Pts',(-0.0125,-0.0402787743898722,-0.0133510937601389));
#48549=CARTESIAN_POINT('Ctrl Pts',(-0.0118214745962156,-0.0403204410565389,
-0.0133510937601389));
#48550=CARTESIAN_POINT('Ctrl Pts',(-0.0114822118943233,-0.0403621077232055,
-0.0127634735233485));
#48551=CARTESIAN_POINT('Ctrl Pts',(-0.0111429491924311,-0.0404037743898722,
-0.0121758532865581));
#48552=CARTESIAN_POINT('Ctrl Pts',(-0.0114822118943233,-0.0404454410565388,
-0.0115882330497677));
#48553=CARTESIAN_POINT('Ctrl Pts',(-0.0118214745962156,-0.0404871077232055,
-0.0110006128129773));
#48554=CARTESIAN_POINT('Ctrl Pts',(-0.0125,-0.0405287743898722,-0.0110006128129772));
#48555=CARTESIAN_POINT('Ctrl Pts',(-0.0131785254037844,-0.0405704410565388,
-0.0110006128129773));
#48556=CARTESIAN_POINT('Ctrl Pts',(-0.0135177881056766,-0.0406121077232055,
-0.0115882330497677));
#48557=CARTESIAN_POINT('Ctrl Pts',(-0.0138570508075689,-0.0406537743898722,
-0.0121758532865581));
#48558=CARTESIAN_POINT('Ctrl Pts',(-0.0135177881056766,-0.0406954410565388,
-0.0127634735233485));
#48559=CARTESIAN_POINT('Ctrl Pts',(-0.0131785254037844,-0.0407371077232055,
-0.0133510937601389));
#48560=CARTESIAN_POINT('Ctrl Pts',(-0.0125,-0.0407787743898722,-0.0133510937601389));
#48561=CARTESIAN_POINT('Ctrl Pts',(-0.0118214745962156,-0.0408204410565389,
-0.0133510937601389));
#48562=CARTESIAN_POINT('Ctrl Pts',(-0.0114822118943233,-0.0408621077232055,
-0.0127634735233485));
#48563=CARTESIAN_POINT('Ctrl Pts',(-0.0111429491924311,-0.0409037743898722,
-0.0121758532865581));
#48564=CARTESIAN_POINT('Ctrl Pts',(-0.0114822118943233,-0.0409454410565388,
-0.0115882330497676));
#48565=CARTESIAN_POINT('Ctrl Pts',(-0.0118214745962156,-0.0409871077232055,
-0.0110006128129772));
#48566=CARTESIAN_POINT('Ctrl Pts',(-0.0125,-0.0410287743898722,-0.0110006128129772));
#48567=CARTESIAN_POINT('Ctrl Pts',(-0.0131785254037844,-0.0410704410565388,
-0.0110006128129772));
#48568=CARTESIAN_POINT('Ctrl Pts',(-0.0135177881056766,-0.0411121077232055,
-0.0115882330497676));
#48569=CARTESIAN_POINT('Ctrl Pts',(-0.0138570508075689,-0.0411537743898722,
-0.012175853286558));
#48570=CARTESIAN_POINT('Ctrl Pts',(-0.0135177881056766,-0.0411954410565388,
-0.0127634735233485));
#48571=CARTESIAN_POINT('Ctrl Pts',(-0.0131785254037844,-0.0412371077232056,
-0.0133510937601389));
#48572=CARTESIAN_POINT('Ctrl Pts',(-0.0125,-0.0412787743898722,-0.0133510937601389));
#48573=CARTESIAN_POINT('Ctrl Pts',(-0.0118214745962156,-0.0413204410565389,
-0.0133510937601389));
#48574=CARTESIAN_POINT('Ctrl Pts',(-0.0114822118943233,-0.0413621077232055,
-0.0127634735233485));
#48575=CARTESIAN_POINT('Ctrl Pts',(-0.0111429491924311,-0.0414037743898722,
-0.012175853286558));
#48576=CARTESIAN_POINT('Ctrl Pts',(-0.0114822118943233,-0.0414454410565388,
-0.0115882330497676));
#48577=CARTESIAN_POINT('Ctrl Pts',(-0.0117636651570184,-0.0414800078368349,
-0.0111007416988237));
#48578=CARTESIAN_POINT('Ctrl Pts',(-0.0123199245616647,-0.0415172243523708,
-0.0110144907216151));
#48579=CARTESIAN_POINT('Ctrl Pts',(-0.012484606188608,-0.033092009537925,
-0.0136757875882698));
#48580=CARTESIAN_POINT('Ctrl Pts',(-0.0116288506733376,-0.0331334256887305,
-0.0136670049776016));
#48581=CARTESIAN_POINT('Ctrl Pts',(-0.0112009503823333,-0.0331746000485455,
-0.0129258599330088));
#48582=CARTESIAN_POINT('Ctrl Pts',(-0.0107679338431112,-0.0332162667152122,
-0.0121758532865583));
#48583=CARTESIAN_POINT('Ctrl Pts',(-0.0112009503823333,-0.0332579333818788,
-0.0114258466401078));
#48584=CARTESIAN_POINT('Ctrl Pts',(-0.0116339669215556,-0.0332996000485455,
-0.0106758399936573));
#48585=CARTESIAN_POINT('Ctrl Pts',(-0.0125,-0.0333412667152122,-0.0106758399936573));
#48586=CARTESIAN_POINT('Ctrl Pts',(-0.0133660330784445,-0.0333829333818788,
-0.0106758399936573));
#48587=CARTESIAN_POINT('Ctrl Pts',(-0.0137990496176667,-0.0334246000485455,
-0.0114258466401078));
#48588=CARTESIAN_POINT('Ctrl Pts',(-0.0142320661568888,-0.0334662667152122,
-0.0121758532865583));
#48589=CARTESIAN_POINT('Ctrl Pts',(-0.0137990496176667,-0.0335079333818789,
-0.0129258599330088));
#48590=CARTESIAN_POINT('Ctrl Pts',(-0.0133660330784445,-0.0335496000485456,
-0.0136758665794593));
#48591=CARTESIAN_POINT('Ctrl Pts',(-0.0125,-0.0335912667152122,-0.0136758665794593));
#48592=CARTESIAN_POINT('Ctrl Pts',(-0.0116339669215556,-0.0336329333818789,
-0.0136758665794593));
#48593=CARTESIAN_POINT('Ctrl Pts',(-0.0112009503823333,-0.0336746000485455,
-0.0129258599330088));
#48594=CARTESIAN_POINT('Ctrl Pts',(-0.0107679338431112,-0.0337162667152122,
-0.0121758532865583));
#48595=CARTESIAN_POINT('Ctrl Pts',(-0.0112009503823333,-0.0337579333818788,
-0.0114258466401078));
#48596=CARTESIAN_POINT('Ctrl Pts',(-0.0116339669215556,-0.0337996000485455,
-0.0106758399936573));
#48597=CARTESIAN_POINT('Ctrl Pts',(-0.0125,-0.0338412667152122,-0.0106758399936573));
#48598=CARTESIAN_POINT('Ctrl Pts',(-0.0133660330784445,-0.0338829333818788,
-0.0106758399936573));
#48599=CARTESIAN_POINT('Ctrl Pts',(-0.0137990496176667,-0.0339246000485455,
-0.0114258466401078));
#48600=CARTESIAN_POINT('Ctrl Pts',(-0.0142320661568888,-0.0339662667152122,
-0.0121758532865583));
#48601=CARTESIAN_POINT('Ctrl Pts',(-0.0137990496176667,-0.0340079333818789,
-0.0129258599330088));
#48602=CARTESIAN_POINT('Ctrl Pts',(-0.0133660330784445,-0.0340496000485456,
-0.0136758665794593));
#48603=CARTESIAN_POINT('Ctrl Pts',(-0.0125,-0.0340912667152123,-0.0136758665794593));
#48604=CARTESIAN_POINT('Ctrl Pts',(-0.0116339669215556,-0.0341329333818789,
-0.0136758665794593));
#48605=CARTESIAN_POINT('Ctrl Pts',(-0.0112009503823333,-0.0341746000485455,
-0.0129258599330088));
#48606=CARTESIAN_POINT('Ctrl Pts',(-0.0107679338431112,-0.0342162667152122,
-0.0121758532865583));
#48607=CARTESIAN_POINT('Ctrl Pts',(-0.0112009503823333,-0.0342579333818789,
-0.0114258466401078));
#48608=CARTESIAN_POINT('Ctrl Pts',(-0.0116339669215556,-0.0342996000485455,
-0.0106758399936573));
#48609=CARTESIAN_POINT('Ctrl Pts',(-0.0125,-0.0343412667152122,-0.0106758399936573));
#48610=CARTESIAN_POINT('Ctrl Pts',(-0.0133660330784445,-0.0343829333818788,
-0.0106758399936573));
#48611=CARTESIAN_POINT('Ctrl Pts',(-0.0137990496176667,-0.0344246000485455,
-0.0114258466401078));
#48612=CARTESIAN_POINT('Ctrl Pts',(-0.0142320661568888,-0.0344662667152122,
-0.0121758532865583));
#48613=CARTESIAN_POINT('Ctrl Pts',(-0.0137990496176667,-0.0345079333818789,
-0.0129258599330088));
#48614=CARTESIAN_POINT('Ctrl Pts',(-0.0133660330784445,-0.0345496000485456,
-0.0136758665794593));
#48615=CARTESIAN_POINT('Ctrl Pts',(-0.0125,-0.0345912667152123,-0.0136758665794593));
#48616=CARTESIAN_POINT('Ctrl Pts',(-0.0116339669215556,-0.0346329333818789,
-0.0136758665794593));
#48617=CARTESIAN_POINT('Ctrl Pts',(-0.0112009503823333,-0.0346746000485455,
-0.0129258599330088));
#48618=CARTESIAN_POINT('Ctrl Pts',(-0.0107679338431112,-0.0347162667152122,
-0.0121758532865583));
#48619=CARTESIAN_POINT('Ctrl Pts',(-0.0112009503823333,-0.0347579333818789,
-0.0114258466401078));
#48620=CARTESIAN_POINT('Ctrl Pts',(-0.0116339669215556,-0.0347996000485455,
-0.0106758399936573));
#48621=CARTESIAN_POINT('Ctrl Pts',(-0.0125,-0.0348412667152122,-0.0106758399936573));
#48622=CARTESIAN_POINT('Ctrl Pts',(-0.0133660330784445,-0.0348829333818788,
-0.0106758399936573));
#48623=CARTESIAN_POINT('Ctrl Pts',(-0.0137990496176667,-0.0349246000485455,
-0.0114258466401078));
#48624=CARTESIAN_POINT('Ctrl Pts',(-0.0142320661568888,-0.0349662667152122,
-0.0121758532865583));
#48625=CARTESIAN_POINT('Ctrl Pts',(-0.0137990496176667,-0.0350079333818789,
-0.0129258599330088));
#48626=CARTESIAN_POINT('Ctrl Pts',(-0.0133660330784445,-0.0350496000485456,
-0.0136758665794593));
#48627=CARTESIAN_POINT('Ctrl Pts',(-0.0125,-0.0350912667152123,-0.0136758665794593));
#48628=CARTESIAN_POINT('Ctrl Pts',(-0.0116339669215556,-0.0351329333818789,
-0.0136758665794593));
#48629=CARTESIAN_POINT('Ctrl Pts',(-0.0112009503823333,-0.0351746000485455,
-0.0129258599330088));
#48630=CARTESIAN_POINT('Ctrl Pts',(-0.0107679338431112,-0.0352162667152122,
-0.0121758532865583));
#48631=CARTESIAN_POINT('Ctrl Pts',(-0.0112009503823333,-0.0352579333818789,
-0.0114258466401078));
#48632=CARTESIAN_POINT('Ctrl Pts',(-0.0116339669215556,-0.0352996000485455,
-0.0106758399936573));
#48633=CARTESIAN_POINT('Ctrl Pts',(-0.0125,-0.0353412667152122,-0.0106758399936573));
#48634=CARTESIAN_POINT('Ctrl Pts',(-0.0133660330784445,-0.0353829333818788,
-0.0106758399936573));
#48635=CARTESIAN_POINT('Ctrl Pts',(-0.0137990496176667,-0.0354246000485455,
-0.0114258466401078));
#48636=CARTESIAN_POINT('Ctrl Pts',(-0.0142320661568888,-0.0354662667152122,
-0.0121758532865583));
#48637=CARTESIAN_POINT('Ctrl Pts',(-0.0137990496176667,-0.0355079333818789,
-0.0129258599330088));
#48638=CARTESIAN_POINT('Ctrl Pts',(-0.0133660330784445,-0.0355496000485456,
-0.0136758665794593));
#48639=CARTESIAN_POINT('Ctrl Pts',(-0.0125,-0.0355912667152123,-0.0136758665794592));
#48640=CARTESIAN_POINT('Ctrl Pts',(-0.0116339669215556,-0.0356329333818789,
-0.0136758665794593));
#48641=CARTESIAN_POINT('Ctrl Pts',(-0.0112009503823333,-0.0356746000485455,
-0.0129258599330087));
#48642=CARTESIAN_POINT('Ctrl Pts',(-0.0107679338431112,-0.0357162667152122,
-0.0121758532865583));
#48643=CARTESIAN_POINT('Ctrl Pts',(-0.0112009503823333,-0.0357579333818789,
-0.0114258466401077));
#48644=CARTESIAN_POINT('Ctrl Pts',(-0.0116339669215556,-0.0357996000485455,
-0.0106758399936572));
#48645=CARTESIAN_POINT('Ctrl Pts',(-0.0125,-0.0358412667152122,-0.0106758399936572));
#48646=CARTESIAN_POINT('Ctrl Pts',(-0.0133660330784445,-0.0358829333818788,
-0.0106758399936572));
#48647=CARTESIAN_POINT('Ctrl Pts',(-0.0137990496176667,-0.0359246000485455,
-0.0114258466401077));
#48648=CARTESIAN_POINT('Ctrl Pts',(-0.0142320661568888,-0.0359662667152122,
-0.0121758532865582));
#48649=CARTESIAN_POINT('Ctrl Pts',(-0.0137990496176667,-0.0360079333818789,
-0.0129258599330087));
#48650=CARTESIAN_POINT('Ctrl Pts',(-0.0133660330784445,-0.0360496000485456,
-0.0136758665794592));
#48651=CARTESIAN_POINT('Ctrl Pts',(-0.0125,-0.0360912667152122,-0.0136758665794592));
#48652=CARTESIAN_POINT('Ctrl Pts',(-0.0116339669215556,-0.0361329333818789,
-0.0136758665794592));
#48653=CARTESIAN_POINT('Ctrl Pts',(-0.0112009503823333,-0.0361746000485455,
-0.0129258599330087));
#48654=CARTESIAN_POINT('Ctrl Pts',(-0.0107679338431112,-0.0362162667152122,
-0.0121758532865582));
#48655=CARTESIAN_POINT('Ctrl Pts',(-0.0112009503823333,-0.0362579333818789,
-0.0114258466401077));
#48656=CARTESIAN_POINT('Ctrl Pts',(-0.0116339669215556,-0.0362996000485455,
-0.0106758399936572));
#48657=CARTESIAN_POINT('Ctrl Pts',(-0.0125,-0.0363412667152121,-0.0106758399936572));
#48658=CARTESIAN_POINT('Ctrl Pts',(-0.0133660330784445,-0.0363829333818788,
-0.0106758399936572));
#48659=CARTESIAN_POINT('Ctrl Pts',(-0.0137990496176667,-0.0364246000485455,
-0.0114258466401077));
#48660=CARTESIAN_POINT('Ctrl Pts',(-0.0142320661568888,-0.0364662667152122,
-0.0121758532865582));
#48661=CARTESIAN_POINT('Ctrl Pts',(-0.0137990496176667,-0.0365079333818789,
-0.0129258599330087));
#48662=CARTESIAN_POINT('Ctrl Pts',(-0.0133660330784445,-0.0365496000485456,
-0.0136758665794592));
#48663=CARTESIAN_POINT('Ctrl Pts',(-0.0125,-0.0365912667152122,-0.0136758665794592));
#48664=CARTESIAN_POINT('Ctrl Pts',(-0.0116339669215556,-0.0366329333818789,
-0.0136758665794592));
#48665=CARTESIAN_POINT('Ctrl Pts',(-0.0112009503823333,-0.0366746000485455,
-0.0129258599330087));
#48666=CARTESIAN_POINT('Ctrl Pts',(-0.0107679338431112,-0.0367162667152122,
-0.0121758532865582));
#48667=CARTESIAN_POINT('Ctrl Pts',(-0.0112009503823333,-0.0367579333818789,
-0.0114258466401077));
#48668=CARTESIAN_POINT('Ctrl Pts',(-0.0116339669215556,-0.0367996000485454,
-0.0106758399936572));
#48669=CARTESIAN_POINT('Ctrl Pts',(-0.0125,-0.0368412667152121,-0.0106758399936572));
#48670=CARTESIAN_POINT('Ctrl Pts',(-0.0133660330784445,-0.0368829333818788,
-0.0106758399936572));
#48671=CARTESIAN_POINT('Ctrl Pts',(-0.0137990496176667,-0.0369246000485455,
-0.0114258466401077));
#48672=CARTESIAN_POINT('Ctrl Pts',(-0.0142320661568888,-0.0369662667152122,
-0.0121758532865582));
#48673=CARTESIAN_POINT('Ctrl Pts',(-0.0137990496176667,-0.0370079333818789,
-0.0129258599330087));
#48674=CARTESIAN_POINT('Ctrl Pts',(-0.0133660330784445,-0.0370496000485455,
-0.0136758665794592));
#48675=CARTESIAN_POINT('Ctrl Pts',(-0.0125,-0.0370912667152122,-0.0136758665794592));
#48676=CARTESIAN_POINT('Ctrl Pts',(-0.0116339669215556,-0.0371329333818789,
-0.0136758665794592));
#48677=CARTESIAN_POINT('Ctrl Pts',(-0.0112009503823333,-0.0371746000485455,
-0.0129258599330087));
#48678=CARTESIAN_POINT('Ctrl Pts',(-0.0107679338431112,-0.0372162667152122,
-0.0121758532865582));
#48679=CARTESIAN_POINT('Ctrl Pts',(-0.0112009503823333,-0.0372579333818789,
-0.0114258466401077));
#48680=CARTESIAN_POINT('Ctrl Pts',(-0.0116339669215556,-0.0372996000485455,
-0.0106758399936572));
#48681=CARTESIAN_POINT('Ctrl Pts',(-0.0125,-0.0373412667152121,-0.0106758399936572));
#48682=CARTESIAN_POINT('Ctrl Pts',(-0.0133660330784445,-0.0373829333818788,
-0.0106758399936572));
#48683=CARTESIAN_POINT('Ctrl Pts',(-0.0137990496176667,-0.0374246000485455,
-0.0114258466401077));
#48684=CARTESIAN_POINT('Ctrl Pts',(-0.0142320661568888,-0.0374662667152122,
-0.0121758532865582));
#48685=CARTESIAN_POINT('Ctrl Pts',(-0.0137990496176667,-0.0375079333818789,
-0.0129258599330087));
#48686=CARTESIAN_POINT('Ctrl Pts',(-0.0133660330784445,-0.0375496000485456,
-0.0136758665794592));
#48687=CARTESIAN_POINT('Ctrl Pts',(-0.0125,-0.0375912667152122,-0.0136758665794592));
#48688=CARTESIAN_POINT('Ctrl Pts',(-0.0116339669215556,-0.0376329333818789,
-0.0136758665794592));
#48689=CARTESIAN_POINT('Ctrl Pts',(-0.0112009503823333,-0.0376746000485455,
-0.0129258599330087));
#48690=CARTESIAN_POINT('Ctrl Pts',(-0.0107679338431112,-0.0377162667152122,
-0.0121758532865582));
#48691=CARTESIAN_POINT('Ctrl Pts',(-0.0112009503823333,-0.0377579333818789,
-0.0114258466401077));
#48692=CARTESIAN_POINT('Ctrl Pts',(-0.0116339669215556,-0.0377996000485455,
-0.0106758399936572));
#48693=CARTESIAN_POINT('Ctrl Pts',(-0.0125,-0.0378412667152121,-0.0106758399936572));
#48694=CARTESIAN_POINT('Ctrl Pts',(-0.0133660330784445,-0.0378829333818788,
-0.0106758399936572));
#48695=CARTESIAN_POINT('Ctrl Pts',(-0.0137990496176667,-0.0379246000485455,
-0.0114258466401077));
#48696=CARTESIAN_POINT('Ctrl Pts',(-0.0142320661568888,-0.0379662667152122,
-0.0121758532865582));
#48697=CARTESIAN_POINT('Ctrl Pts',(-0.0137990496176667,-0.0380079333818789,
-0.0129258599330087));
#48698=CARTESIAN_POINT('Ctrl Pts',(-0.0133660330784445,-0.0380496000485456,
-0.0136758665794592));
#48699=CARTESIAN_POINT('Ctrl Pts',(-0.0125,-0.0380912667152122,-0.0136758665794592));
#48700=CARTESIAN_POINT('Ctrl Pts',(-0.0116339669215556,-0.0381329333818789,
-0.0136758665794592));
#48701=CARTESIAN_POINT('Ctrl Pts',(-0.0112009503823333,-0.0381746000485456,
-0.0129258599330087));
#48702=CARTESIAN_POINT('Ctrl Pts',(-0.0107679338431112,-0.0382162667152122,
-0.0121758532865582));
#48703=CARTESIAN_POINT('Ctrl Pts',(-0.0112009503823333,-0.0382579333818788,
-0.0114258466401077));
#48704=CARTESIAN_POINT('Ctrl Pts',(-0.0116339669215556,-0.0382996000485455,
-0.0106758399936572));
#48705=CARTESIAN_POINT('Ctrl Pts',(-0.0125,-0.0383412667152122,-0.0106758399936572));
#48706=CARTESIAN_POINT('Ctrl Pts',(-0.0133660330784445,-0.0383829333818788,
-0.0106758399936572));
#48707=CARTESIAN_POINT('Ctrl Pts',(-0.0137990496176667,-0.0384246000485455,
-0.0114258466401076));
#48708=CARTESIAN_POINT('Ctrl Pts',(-0.0142320661568888,-0.0384662667152122,
-0.0121758532865581));
#48709=CARTESIAN_POINT('Ctrl Pts',(-0.0137990496176667,-0.0385079333818789,
-0.0129258599330086));
#48710=CARTESIAN_POINT('Ctrl Pts',(-0.0133660330784445,-0.0385496000485456,
-0.0136758665794591));
#48711=CARTESIAN_POINT('Ctrl Pts',(-0.0125,-0.0385912667152122,-0.0136758665794591));
#48712=CARTESIAN_POINT('Ctrl Pts',(-0.0116339669215556,-0.0386329333818789,
-0.0136758665794591));
#48713=CARTESIAN_POINT('Ctrl Pts',(-0.0112009503823333,-0.0386746000485456,
-0.0129258599330086));
#48714=CARTESIAN_POINT('Ctrl Pts',(-0.0107679338431112,-0.0387162667152122,
-0.0121758532865581));
#48715=CARTESIAN_POINT('Ctrl Pts',(-0.0112009503823333,-0.0387579333818788,
-0.0114258466401076));
#48716=CARTESIAN_POINT('Ctrl Pts',(-0.0116339669215556,-0.0387996000485455,
-0.0106758399936571));
#48717=CARTESIAN_POINT('Ctrl Pts',(-0.0125,-0.0388412667152122,-0.0106758399936571));
#48718=CARTESIAN_POINT('Ctrl Pts',(-0.0133660330784445,-0.0388829333818788,
-0.0106758399936571));
#48719=CARTESIAN_POINT('Ctrl Pts',(-0.0137990496176667,-0.0389246000485455,
-0.0114258466401076));
#48720=CARTESIAN_POINT('Ctrl Pts',(-0.0142320661568888,-0.0389662667152122,
-0.0121758532865581));
#48721=CARTESIAN_POINT('Ctrl Pts',(-0.0137990496176667,-0.0390079333818789,
-0.0129258599330086));
#48722=CARTESIAN_POINT('Ctrl Pts',(-0.0133660330784445,-0.0390496000485456,
-0.0136758665794591));
#48723=CARTESIAN_POINT('Ctrl Pts',(-0.0125,-0.0390912667152122,-0.0136758665794591));
#48724=CARTESIAN_POINT('Ctrl Pts',(-0.0116339669215556,-0.0391329333818789,
-0.0136758665794591));
#48725=CARTESIAN_POINT('Ctrl Pts',(-0.0112009503823333,-0.0391746000485456,
-0.0129258599330086));
#48726=CARTESIAN_POINT('Ctrl Pts',(-0.0107679338431112,-0.0392162667152122,
-0.0121758532865581));
#48727=CARTESIAN_POINT('Ctrl Pts',(-0.0112009503823333,-0.0392579333818788,
-0.0114258466401076));
#48728=CARTESIAN_POINT('Ctrl Pts',(-0.0116339669215556,-0.0392996000485454,
-0.0106758399936571));
#48729=CARTESIAN_POINT('Ctrl Pts',(-0.0125,-0.0393412667152122,-0.0106758399936571));
#48730=CARTESIAN_POINT('Ctrl Pts',(-0.0133660330784445,-0.0393829333818788,
-0.0106758399936571));
#48731=CARTESIAN_POINT('Ctrl Pts',(-0.0137990496176667,-0.0394246000485455,
-0.0114258466401076));
#48732=CARTESIAN_POINT('Ctrl Pts',(-0.0142320661568888,-0.0394662667152122,
-0.0121758532865581));
#48733=CARTESIAN_POINT('Ctrl Pts',(-0.0137990496176667,-0.0395079333818789,
-0.0129258599330086));
#48734=CARTESIAN_POINT('Ctrl Pts',(-0.0133660330784445,-0.0395496000485456,
-0.0136758665794591));
#48735=CARTESIAN_POINT('Ctrl Pts',(-0.0125,-0.0395912667152122,-0.0136758665794591));
#48736=CARTESIAN_POINT('Ctrl Pts',(-0.0116339669215556,-0.0396329333818789,
-0.0136758665794591));
#48737=CARTESIAN_POINT('Ctrl Pts',(-0.0112009503823333,-0.0396746000485456,
-0.0129258599330086));
#48738=CARTESIAN_POINT('Ctrl Pts',(-0.0107679338431112,-0.0397162667152122,
-0.0121758532865581));
#48739=CARTESIAN_POINT('Ctrl Pts',(-0.0112009503823333,-0.0397579333818788,
-0.0114258466401076));
#48740=CARTESIAN_POINT('Ctrl Pts',(-0.0116339669215556,-0.0397996000485455,
-0.0106758399936571));
#48741=CARTESIAN_POINT('Ctrl Pts',(-0.0125,-0.0398412667152122,-0.0106758399936571));
#48742=CARTESIAN_POINT('Ctrl Pts',(-0.0133660330784445,-0.0398829333818788,
-0.0106758399936571));
#48743=CARTESIAN_POINT('Ctrl Pts',(-0.0137990496176667,-0.0399246000485455,
-0.0114258466401076));
#48744=CARTESIAN_POINT('Ctrl Pts',(-0.0142320661568888,-0.0399662667152122,
-0.0121758532865581));
#48745=CARTESIAN_POINT('Ctrl Pts',(-0.0137990496176667,-0.0400079333818789,
-0.0129258599330086));
#48746=CARTESIAN_POINT('Ctrl Pts',(-0.0133660330784445,-0.0400496000485456,
-0.0136758665794591));
#48747=CARTESIAN_POINT('Ctrl Pts',(-0.0125,-0.0400912667152122,-0.0136758665794591));
#48748=CARTESIAN_POINT('Ctrl Pts',(-0.0116339669215556,-0.0401329333818789,
-0.0136758665794591));
#48749=CARTESIAN_POINT('Ctrl Pts',(-0.0112009503823333,-0.0401746000485455,
-0.0129258599330086));
#48750=CARTESIAN_POINT('Ctrl Pts',(-0.0107679338431112,-0.0402162667152122,
-0.0121758532865581));
#48751=CARTESIAN_POINT('Ctrl Pts',(-0.0112009503823333,-0.0402579333818788,
-0.0114258466401076));
#48752=CARTESIAN_POINT('Ctrl Pts',(-0.0116339669215556,-0.0402996000485455,
-0.0106758399936571));
#48753=CARTESIAN_POINT('Ctrl Pts',(-0.0125,-0.0403412667152122,-0.0106758399936571));
#48754=CARTESIAN_POINT('Ctrl Pts',(-0.0133660330784445,-0.0403829333818788,
-0.0106758399936571));
#48755=CARTESIAN_POINT('Ctrl Pts',(-0.0137990496176667,-0.0404246000485455,
-0.0114258466401076));
#48756=CARTESIAN_POINT('Ctrl Pts',(-0.0142320661568888,-0.0404662667152122,
-0.0121758532865581));
#48757=CARTESIAN_POINT('Ctrl Pts',(-0.0137990496176667,-0.0405079333818789,
-0.0129258599330086));
#48758=CARTESIAN_POINT('Ctrl Pts',(-0.0133660330784445,-0.0405496000485456,
-0.0136758665794591));
#48759=CARTESIAN_POINT('Ctrl Pts',(-0.0125,-0.0405912667152122,-0.0136758665794591));
#48760=CARTESIAN_POINT('Ctrl Pts',(-0.0116339669215556,-0.0406329333818789,
-0.0136758665794591));
#48761=CARTESIAN_POINT('Ctrl Pts',(-0.0112009503823333,-0.0406746000485455,
-0.0129258599330086));
#48762=CARTESIAN_POINT('Ctrl Pts',(-0.0107679338431112,-0.0407162667152122,
-0.0121758532865581));
#48763=CARTESIAN_POINT('Ctrl Pts',(-0.0112009503823333,-0.0407579333818788,
-0.0114258466401076));
#48764=CARTESIAN_POINT('Ctrl Pts',(-0.0116339669215556,-0.0407996000485454,
-0.0106758399936571));
#48765=CARTESIAN_POINT('Ctrl Pts',(-0.0125,-0.0408412667152122,-0.0106758399936571));
#48766=CARTESIAN_POINT('Ctrl Pts',(-0.0133660330784445,-0.0408829333818788,
-0.0106758399936571));
#48767=CARTESIAN_POINT('Ctrl Pts',(-0.0137990496176667,-0.0409246000485455,
-0.0114258466401076));
#48768=CARTESIAN_POINT('Ctrl Pts',(-0.0142320661568888,-0.0409662667152122,
-0.0121758532865581));
#48769=CARTESIAN_POINT('Ctrl Pts',(-0.0137990496176667,-0.0410079333818789,
-0.0129258599330086));
#48770=CARTESIAN_POINT('Ctrl Pts',(-0.0133660330784445,-0.0410496000485455,
-0.0136758665794591));
#48771=CARTESIAN_POINT('Ctrl Pts',(-0.0125,-0.0410912667152122,-0.0136758665794591));
#48772=CARTESIAN_POINT('Ctrl Pts',(-0.0116339669215556,-0.0411329333818789,
-0.0136758665794591));
#48773=CARTESIAN_POINT('Ctrl Pts',(-0.0112009503823333,-0.0411746000485455,
-0.0129258599330086));
#48774=CARTESIAN_POINT('Ctrl Pts',(-0.0107679338431112,-0.0412162667152122,
-0.012175853286558));
#48775=CARTESIAN_POINT('Ctrl Pts',(-0.0112009503823333,-0.0412579333818788,
-0.0114258466401076));
#48776=CARTESIAN_POINT('Ctrl Pts',(-0.011560182084154,-0.0412925001621749,
-0.0108036390808646));
#48777=CARTESIAN_POINT('Ctrl Pts',(-0.0122701614628665,-0.0413297166777108,
-0.0106935530046557));
#48778=CARTESIAN_POINT('Ctrl Pts',(-0.0124999999999993,-0.0412787743898722,
-0.0133510937601389));
#48779=CARTESIAN_POINT('Ctrl Pts',(-0.012358363960416,-0.0412787743898722,
-0.0133661583408318));
#48780=CARTESIAN_POINT('Ctrl Pts',(-0.0122152415795414,-0.0412787743898722,
-0.0133567697507035));
#48781=CARTESIAN_POINT('Ctrl Pts',(-0.0119414505804856,-0.0412787743898722,
-0.013290480504866));
#48782=CARTESIAN_POINT('Ctrl Pts',(-0.0118126101483348,-0.0412787743898715,
-0.0132351257070212));
#48783=CARTESIAN_POINT('Ctrl Pts',(-0.011583418002351,-0.0412787743898715,
-0.0130869866720988));
#48784=CARTESIAN_POINT('Ctrl Pts',(-0.0114581988285637,-0.0412787743898735,
-0.0129841339295786));
#48785=CARTESIAN_POINT('Ctrl Pts',(-0.0112456182130333,-0.0412787743898735,
-0.0126725262993937));
#48786=CARTESIAN_POINT('Ctrl Pts',(-0.0111762705577612,-0.0412787743898722,
-0.0125149575896434));
#48787=CARTESIAN_POINT('Ctrl Pts',(-0.0110953627121927,-0.0412787743898722,
-0.0121694782739801));
#48788=CARTESIAN_POINT('Ctrl Pts',(-0.0110895688642527,-0.0412787743898722,
-0.0119837162050846));
#48789=CARTESIAN_POINT('Ctrl Pts',(-0.0111490989927533,-0.0412787743898722,
-0.0116312177889278));
#48790=CARTESIAN_POINT('Ctrl Pts',(-0.0112035576011838,-0.0412787743898722,
-0.0115039539015553));
#48791=CARTESIAN_POINT('Ctrl Pts',(-0.0112928253083772,-0.0412787743898722,
-0.0113166320658545));
#48792=CARTESIAN_POINT('Ctrl Pts',(-0.0113643003226613,-0.0412787743898722,
-0.0112058612590309));
#48793=CARTESIAN_POINT('Ctrl Pts',(-0.0114490560961843,-0.0412787743898722,
-0.011105565049194));
#48794=CARTESIAN_POINT('Ctrl Pts',(-0.0135456685377107,-0.033466680519734,
-0.0132513163635058));
#48795=CARTESIAN_POINT('Ctrl Pts',(-0.0131090202398857,-0.0334994815488067,
-0.0136758677933666));
#48796=CARTESIAN_POINT('Ctrl Pts',(-0.0125,-0.0335287827653819,-0.0136758677933666));
#48797=CARTESIAN_POINT('Ctrl Pts',(-0.0116339662207059,-0.0335704494320486,
-0.0136758677933666));
#48798=CARTESIAN_POINT('Ctrl Pts',(-0.0112009493310588,-0.0336121160987153,
-0.0129258605399625));
#48799=CARTESIAN_POINT('Ctrl Pts',(-0.0107679324414118,-0.0336537827653819,
-0.0121758532865583));
#48800=CARTESIAN_POINT('Ctrl Pts',(-0.0112009493310588,-0.0336954494320485,
-0.0114258460331541));
#48801=CARTESIAN_POINT('Ctrl Pts',(-0.0116339662207059,-0.0337371160987151,
-0.01067583877975));
#48802=CARTESIAN_POINT('Ctrl Pts',(-0.0125,-0.0337787827653818,-0.01067583877975));
#48803=CARTESIAN_POINT('Ctrl Pts',(-0.0133660337792941,-0.0338204494320485,
-0.01067583877975));
#48804=CARTESIAN_POINT('Ctrl Pts',(-0.0137990506689412,-0.0338621160987152,
-0.0114258460331541));
#48805=CARTESIAN_POINT('Ctrl Pts',(-0.0142320675585882,-0.0339037827653818,
-0.0121758532865583));
#48806=CARTESIAN_POINT('Ctrl Pts',(-0.0137990506689412,-0.0339454494320486,
-0.0129258605399625));
#48807=CARTESIAN_POINT('Ctrl Pts',(-0.0133660337792941,-0.0339871160987152,
-0.0136758677933666));
#48808=CARTESIAN_POINT('Ctrl Pts',(-0.0125,-0.0340287827653819,-0.0136758677933666));
#48809=CARTESIAN_POINT('Ctrl Pts',(-0.0116339662207059,-0.0340704494320486,
-0.0136758677933666));
#48810=CARTESIAN_POINT('Ctrl Pts',(-0.0112009493310588,-0.0341121160987153,
-0.0129258605399625));
#48811=CARTESIAN_POINT('Ctrl Pts',(-0.0107679324414118,-0.0341537827653819,
-0.0121758532865583));
#48812=CARTESIAN_POINT('Ctrl Pts',(-0.0112009493310588,-0.0341954494320485,
-0.0114258460331541));
#48813=CARTESIAN_POINT('Ctrl Pts',(-0.0116339662207059,-0.0342371160987152,
-0.01067583877975));
#48814=CARTESIAN_POINT('Ctrl Pts',(-0.0125,-0.0342787827653818,-0.01067583877975));
#48815=CARTESIAN_POINT('Ctrl Pts',(-0.0133660337792941,-0.0343204494320485,
-0.01067583877975));
#48816=CARTESIAN_POINT('Ctrl Pts',(-0.0137990506689412,-0.0343621160987152,
-0.0114258460331541));
#48817=CARTESIAN_POINT('Ctrl Pts',(-0.0142320675585882,-0.0344037827653819,
-0.0121758532865583));
#48818=CARTESIAN_POINT('Ctrl Pts',(-0.0137990506689412,-0.0344454494320486,
-0.0129258605399625));
#48819=CARTESIAN_POINT('Ctrl Pts',(-0.0133660337792941,-0.0344871160987153,
-0.0136758677933666));
#48820=CARTESIAN_POINT('Ctrl Pts',(-0.0125,-0.0345287827653819,-0.0136758677933666));
#48821=CARTESIAN_POINT('Ctrl Pts',(-0.0116339662207059,-0.0345704494320486,
-0.0136758677933666));
#48822=CARTESIAN_POINT('Ctrl Pts',(-0.0112009493310588,-0.0346121160987153,
-0.0129258605399625));
#48823=CARTESIAN_POINT('Ctrl Pts',(-0.0107679324414118,-0.0346537827653819,
-0.0121758532865583));
#48824=CARTESIAN_POINT('Ctrl Pts',(-0.0112009493310588,-0.0346954494320485,
-0.0114258460331541));
#48825=CARTESIAN_POINT('Ctrl Pts',(-0.0116339662207059,-0.0347371160987151,
-0.01067583877975));
#48826=CARTESIAN_POINT('Ctrl Pts',(-0.0125,-0.0347787827653818,-0.01067583877975));
#48827=CARTESIAN_POINT('Ctrl Pts',(-0.0133660337792941,-0.0348204494320485,
-0.01067583877975));
#48828=CARTESIAN_POINT('Ctrl Pts',(-0.0137990506689412,-0.0348621160987152,
-0.0114258460331541));
#48829=CARTESIAN_POINT('Ctrl Pts',(-0.0142320675585882,-0.0349037827653819,
-0.0121758532865583));
#48830=CARTESIAN_POINT('Ctrl Pts',(-0.0137990506689412,-0.0349454494320486,
-0.0129258605399625));
#48831=CARTESIAN_POINT('Ctrl Pts',(-0.0133660337792941,-0.0349871160987152,
-0.0136758677933666));
#48832=CARTESIAN_POINT('Ctrl Pts',(-0.0125,-0.0350287827653819,-0.0136758677933666));
#48833=CARTESIAN_POINT('Ctrl Pts',(-0.0116339662207059,-0.0350704494320486,
-0.0136758677933666));
#48834=CARTESIAN_POINT('Ctrl Pts',(-0.0112009493310588,-0.0351121160987153,
-0.0129258605399625));
#48835=CARTESIAN_POINT('Ctrl Pts',(-0.0107679324414118,-0.0351537827653818,
-0.0121758532865583));
#48836=CARTESIAN_POINT('Ctrl Pts',(-0.0112009493310588,-0.0351954494320485,
-0.0114258460331541));
#48837=CARTESIAN_POINT('Ctrl Pts',(-0.0116339662207059,-0.0352371160987152,
-0.0106758387797499));
#48838=CARTESIAN_POINT('Ctrl Pts',(-0.0125,-0.0352787827653818,-0.01067583877975));
#48839=CARTESIAN_POINT('Ctrl Pts',(-0.0133660337792941,-0.0353204494320485,
-0.0106758387797499));
#48840=CARTESIAN_POINT('Ctrl Pts',(-0.0137990506689412,-0.0353621160987152,
-0.011425846033154));
#48841=CARTESIAN_POINT('Ctrl Pts',(-0.0142320675585882,-0.0354037827653818,
-0.0121758532865583));
#48842=CARTESIAN_POINT('Ctrl Pts',(-0.0137990506689412,-0.0354454494320486,
-0.0129258605399625));
#48843=CARTESIAN_POINT('Ctrl Pts',(-0.0133660337792941,-0.0354871160987153,
-0.0136758677933666));
#48844=CARTESIAN_POINT('Ctrl Pts',(-0.0125,-0.0355287827653819,-0.0136758677933666));
#48845=CARTESIAN_POINT('Ctrl Pts',(-0.0116339662207059,-0.0355704494320486,
-0.0136758677933666));
#48846=CARTESIAN_POINT('Ctrl Pts',(-0.0112009493310588,-0.0356121160987152,
-0.0129258605399625));
#48847=CARTESIAN_POINT('Ctrl Pts',(-0.0107679324414118,-0.0356537827653819,
-0.0121758532865583));
#48848=CARTESIAN_POINT('Ctrl Pts',(-0.0112009493310588,-0.0356954494320485,
-0.011425846033154));
#48849=CARTESIAN_POINT('Ctrl Pts',(-0.0116339662207059,-0.0357371160987152,
-0.0106758387797499));
#48850=CARTESIAN_POINT('Ctrl Pts',(-0.0125,-0.0357787827653818,-0.0106758387797499));
#48851=CARTESIAN_POINT('Ctrl Pts',(-0.0133660337792941,-0.0358204494320485,
-0.0106758387797499));
#48852=CARTESIAN_POINT('Ctrl Pts',(-0.0137990506689412,-0.0358621160987152,
-0.011425846033154));
#48853=CARTESIAN_POINT('Ctrl Pts',(-0.0142320675585882,-0.0359037827653819,
-0.0121758532865583));
#48854=CARTESIAN_POINT('Ctrl Pts',(-0.0137990506689412,-0.0359454494320486,
-0.0129258605399624));
#48855=CARTESIAN_POINT('Ctrl Pts',(-0.0133660337792941,-0.0359871160987153,
-0.0136758677933665));
#48856=CARTESIAN_POINT('Ctrl Pts',(-0.0125,-0.0360287827653819,-0.0136758677933665));
#48857=CARTESIAN_POINT('Ctrl Pts',(-0.0116339662207059,-0.0360704494320486,
-0.0136758677933665));
#48858=CARTESIAN_POINT('Ctrl Pts',(-0.0112009493310588,-0.0361121160987152,
-0.0129258605399624));
#48859=CARTESIAN_POINT('Ctrl Pts',(-0.0107679324414118,-0.0361537827653819,
-0.0121758532865582));
#48860=CARTESIAN_POINT('Ctrl Pts',(-0.0112009493310588,-0.0361954494320485,
-0.011425846033154));
#48861=CARTESIAN_POINT('Ctrl Pts',(-0.0116339662207059,-0.0362371160987151,
-0.0106758387797499));
#48862=CARTESIAN_POINT('Ctrl Pts',(-0.0125,-0.0362787827653818,-0.0106758387797499));
#48863=CARTESIAN_POINT('Ctrl Pts',(-0.0133660337792941,-0.0363204494320485,
-0.0106758387797499));
#48864=CARTESIAN_POINT('Ctrl Pts',(-0.0137990506689412,-0.0363621160987152,
-0.011425846033154));
#48865=CARTESIAN_POINT('Ctrl Pts',(-0.0142320675585882,-0.0364037827653818,
-0.0121758532865582));
#48866=CARTESIAN_POINT('Ctrl Pts',(-0.0137990506689412,-0.0364454494320486,
-0.0129258605399624));
#48867=CARTESIAN_POINT('Ctrl Pts',(-0.0133660337792941,-0.0364871160987152,
-0.0136758677933665));
#48868=CARTESIAN_POINT('Ctrl Pts',(-0.0125,-0.0365287827653819,-0.0136758677933665));
#48869=CARTESIAN_POINT('Ctrl Pts',(-0.0116339662207059,-0.0365704494320486,
-0.0136758677933665));
#48870=CARTESIAN_POINT('Ctrl Pts',(-0.0112009493310588,-0.0366121160987152,
-0.0129258605399624));
#48871=CARTESIAN_POINT('Ctrl Pts',(-0.0107679324414118,-0.0366537827653819,
-0.0121758532865582));
#48872=CARTESIAN_POINT('Ctrl Pts',(-0.0112009493310588,-0.0366954494320485,
-0.011425846033154));
#48873=CARTESIAN_POINT('Ctrl Pts',(-0.0116339662207059,-0.0367371160987152,
-0.0106758387797499));
#48874=CARTESIAN_POINT('Ctrl Pts',(-0.0125,-0.0367787827653818,-0.0106758387797499));
#48875=CARTESIAN_POINT('Ctrl Pts',(-0.0133660337792941,-0.0368204494320485,
-0.0106758387797499));
#48876=CARTESIAN_POINT('Ctrl Pts',(-0.0137990506689412,-0.0368621160987152,
-0.011425846033154));
#48877=CARTESIAN_POINT('Ctrl Pts',(-0.0142320675585882,-0.0369037827653819,
-0.0121758532865582));
#48878=CARTESIAN_POINT('Ctrl Pts',(-0.0137990506689412,-0.0369454494320486,
-0.0129258605399624));
#48879=CARTESIAN_POINT('Ctrl Pts',(-0.0133660337792941,-0.0369871160987153,
-0.0136758677933665));
#48880=CARTESIAN_POINT('Ctrl Pts',(-0.0125,-0.0370287827653819,-0.0136758677933665));
#48881=CARTESIAN_POINT('Ctrl Pts',(-0.0116339662207059,-0.0370704494320486,
-0.0136758677933665));
#48882=CARTESIAN_POINT('Ctrl Pts',(-0.0112009493310588,-0.0371121160987152,
-0.0129258605399624));
#48883=CARTESIAN_POINT('Ctrl Pts',(-0.0107679324414118,-0.0371537827653819,
-0.0121758532865582));
#48884=CARTESIAN_POINT('Ctrl Pts',(-0.0112009493310588,-0.0371954494320485,
-0.011425846033154));
#48885=CARTESIAN_POINT('Ctrl Pts',(-0.0116339662207059,-0.0372371160987152,
-0.0106758387797499));
#48886=CARTESIAN_POINT('Ctrl Pts',(-0.0125,-0.0372787827653818,-0.0106758387797499));
#48887=CARTESIAN_POINT('Ctrl Pts',(-0.0133660337792941,-0.0373204494320485,
-0.0106758387797499));
#48888=CARTESIAN_POINT('Ctrl Pts',(-0.0137990506689412,-0.0373621160987152,
-0.011425846033154));
#48889=CARTESIAN_POINT('Ctrl Pts',(-0.0142320675585882,-0.0374037827653819,
-0.0121758532865582));
#48890=CARTESIAN_POINT('Ctrl Pts',(-0.0137990506689412,-0.0374454494320486,
-0.0129258605399624));
#48891=CARTESIAN_POINT('Ctrl Pts',(-0.0133660337792941,-0.0374871160987152,
-0.0136758677933665));
#48892=CARTESIAN_POINT('Ctrl Pts',(-0.0125,-0.0375287827653819,-0.0136758677933665));
#48893=CARTESIAN_POINT('Ctrl Pts',(-0.0116339662207059,-0.0375704494320486,
-0.0136758677933665));
#48894=CARTESIAN_POINT('Ctrl Pts',(-0.0112009493310588,-0.0376121160987152,
-0.0129258605399624));
#48895=CARTESIAN_POINT('Ctrl Pts',(-0.0107679324414118,-0.0376537827653818,
-0.0121758532865582));
#48896=CARTESIAN_POINT('Ctrl Pts',(-0.0112009493310588,-0.0376954494320485,
-0.011425846033154));
#48897=CARTESIAN_POINT('Ctrl Pts',(-0.0116339662207059,-0.0377371160987151,
-0.0106758387797499));
#48898=CARTESIAN_POINT('Ctrl Pts',(-0.0125,-0.0377787827653818,-0.0106758387797499));
#48899=CARTESIAN_POINT('Ctrl Pts',(-0.0133660337792941,-0.0378204494320485,
-0.0106758387797499));
#48900=CARTESIAN_POINT('Ctrl Pts',(-0.0137990506689412,-0.0378621160987152,
-0.011425846033154));
#48901=CARTESIAN_POINT('Ctrl Pts',(-0.0142320675585882,-0.0379037827653818,
-0.0121758532865582));
#48902=CARTESIAN_POINT('Ctrl Pts',(-0.0137990506689412,-0.0379454494320486,
-0.0129258605399624));
#48903=CARTESIAN_POINT('Ctrl Pts',(-0.0133660337792941,-0.0379871160987152,
-0.0136758677933665));
#48904=CARTESIAN_POINT('Ctrl Pts',(-0.0125,-0.0380287827653819,-0.0136758677933665));
#48905=CARTESIAN_POINT('Ctrl Pts',(-0.0116339662207059,-0.0380704494320486,
-0.0136758677933665));
#48906=CARTESIAN_POINT('Ctrl Pts',(-0.0112009493310588,-0.0381121160987152,
-0.0129258605399624));
#48907=CARTESIAN_POINT('Ctrl Pts',(-0.0107679324414118,-0.0381537827653819,
-0.0121758532865582));
#48908=CARTESIAN_POINT('Ctrl Pts',(-0.0112009493310588,-0.0381954494320485,
-0.011425846033154));
#48909=CARTESIAN_POINT('Ctrl Pts',(-0.0116339662207059,-0.0382371160987152,
-0.0106758387797498));
#48910=CARTESIAN_POINT('Ctrl Pts',(-0.0125,-0.0382787827653818,-0.0106758387797499));
#48911=CARTESIAN_POINT('Ctrl Pts',(-0.0133660337792941,-0.0383204494320485,
-0.0106758387797498));
#48912=CARTESIAN_POINT('Ctrl Pts',(-0.0137990506689412,-0.0383621160987152,
-0.0114258460331539));
#48913=CARTESIAN_POINT('Ctrl Pts',(-0.0142320675585882,-0.0384037827653819,
-0.0121758532865581));
#48914=CARTESIAN_POINT('Ctrl Pts',(-0.0137990506689412,-0.0384454494320486,
-0.0129258605399624));
#48915=CARTESIAN_POINT('Ctrl Pts',(-0.0133660337792941,-0.0384871160987153,
-0.0136758677933665));
#48916=CARTESIAN_POINT('Ctrl Pts',(-0.0125,-0.0385287827653819,-0.0136758677933665));
#48917=CARTESIAN_POINT('Ctrl Pts',(-0.0116339662207059,-0.0385704494320486,
-0.0136758677933665));
#48918=CARTESIAN_POINT('Ctrl Pts',(-0.0112009493310588,-0.0386121160987152,
-0.0129258605399623));
#48919=CARTESIAN_POINT('Ctrl Pts',(-0.0107679324414118,-0.0386537827653819,
-0.0121758532865581));
#48920=CARTESIAN_POINT('Ctrl Pts',(-0.0112009493310588,-0.0386954494320485,
-0.0114258460331539));
#48921=CARTESIAN_POINT('Ctrl Pts',(-0.0116339662207059,-0.0387371160987151,
-0.0106758387797498));
#48922=CARTESIAN_POINT('Ctrl Pts',(-0.0125,-0.0387787827653818,-0.0106758387797498));
#48923=CARTESIAN_POINT('Ctrl Pts',(-0.0133660337792941,-0.0388204494320485,
-0.0106758387797498));
#48924=CARTESIAN_POINT('Ctrl Pts',(-0.0137990506689412,-0.0388621160987152,
-0.0114258460331539));
#48925=CARTESIAN_POINT('Ctrl Pts',(-0.0142320675585882,-0.0389037827653818,
-0.0121758532865581));
#48926=CARTESIAN_POINT('Ctrl Pts',(-0.0137990506689412,-0.0389454494320486,
-0.0129258605399623));
#48927=CARTESIAN_POINT('Ctrl Pts',(-0.0133660337792941,-0.0389871160987152,
-0.0136758677933665));
#48928=CARTESIAN_POINT('Ctrl Pts',(-0.0125,-0.0390287827653819,-0.0136758677933664));
#48929=CARTESIAN_POINT('Ctrl Pts',(-0.0116339662207059,-0.0390704494320486,
-0.0136758677933665));
#48930=CARTESIAN_POINT('Ctrl Pts',(-0.0112009493310588,-0.0391121160987152,
-0.0129258605399623));
#48931=CARTESIAN_POINT('Ctrl Pts',(-0.0107679324414118,-0.0391537827653818,
-0.0121758532865581));
#48932=CARTESIAN_POINT('Ctrl Pts',(-0.0112009493310588,-0.0391954494320485,
-0.0114258460331539));
#48933=CARTESIAN_POINT('Ctrl Pts',(-0.0116339662207059,-0.0392371160987152,
-0.0106758387797498));
#48934=CARTESIAN_POINT('Ctrl Pts',(-0.0125,-0.0392787827653818,-0.0106758387797498));
#48935=CARTESIAN_POINT('Ctrl Pts',(-0.0133660337792941,-0.0393204494320485,
-0.0106758387797498));
#48936=CARTESIAN_POINT('Ctrl Pts',(-0.0137990506689412,-0.0393621160987152,
-0.0114258460331539));
#48937=CARTESIAN_POINT('Ctrl Pts',(-0.0142320675585882,-0.0394037827653818,
-0.0121758532865581));
#48938=CARTESIAN_POINT('Ctrl Pts',(-0.0137990506689412,-0.0394454494320486,
-0.0129258605399623));
#48939=CARTESIAN_POINT('Ctrl Pts',(-0.0133660337792941,-0.0394871160987153,
-0.0136758677933664));
#48940=CARTESIAN_POINT('Ctrl Pts',(-0.0125,-0.0395287827653819,-0.0136758677933664));
#48941=CARTESIAN_POINT('Ctrl Pts',(-0.0116339662207059,-0.0395704494320486,
-0.0136758677933664));
#48942=CARTESIAN_POINT('Ctrl Pts',(-0.0112009493310588,-0.0396121160987152,
-0.0129258605399623));
#48943=CARTESIAN_POINT('Ctrl Pts',(-0.0107679324414118,-0.0396537827653819,
-0.0121758532865581));
#48944=CARTESIAN_POINT('Ctrl Pts',(-0.0112009493310588,-0.0396954494320485,
-0.0114258460331539));
#48945=CARTESIAN_POINT('Ctrl Pts',(-0.0116339662207059,-0.0397371160987151,
-0.0106758387797498));
#48946=CARTESIAN_POINT('Ctrl Pts',(-0.0125,-0.0397787827653818,-0.0106758387797498));
#48947=CARTESIAN_POINT('Ctrl Pts',(-0.0133660337792941,-0.0398204494320485,
-0.0106758387797498));
#48948=CARTESIAN_POINT('Ctrl Pts',(-0.0137990506689412,-0.0398621160987152,
-0.0114258460331539));
#48949=CARTESIAN_POINT('Ctrl Pts',(-0.0142320675585882,-0.0399037827653819,
-0.0121758532865581));
#48950=CARTESIAN_POINT('Ctrl Pts',(-0.0137990506689412,-0.0399454494320486,
-0.0129258605399623));
#48951=CARTESIAN_POINT('Ctrl Pts',(-0.0133660337792941,-0.0399871160987153,
-0.0136758677933664));
#48952=CARTESIAN_POINT('Ctrl Pts',(-0.0125,-0.0400287827653819,-0.0136758677933664));
#48953=CARTESIAN_POINT('Ctrl Pts',(-0.0116339662207059,-0.0400704494320486,
-0.0136758677933664));
#48954=CARTESIAN_POINT('Ctrl Pts',(-0.0112009493310588,-0.0401121160987152,
-0.0129258605399623));
#48955=CARTESIAN_POINT('Ctrl Pts',(-0.0107679324414118,-0.0401537827653819,
-0.0121758532865581));
#48956=CARTESIAN_POINT('Ctrl Pts',(-0.0112009493310588,-0.0401954494320485,
-0.0114258460331539));
#48957=CARTESIAN_POINT('Ctrl Pts',(-0.0116339662207059,-0.0402371160987151,
-0.0106758387797498));
#48958=CARTESIAN_POINT('Ctrl Pts',(-0.0125,-0.0402787827653818,-0.0106758387797498));
#48959=CARTESIAN_POINT('Ctrl Pts',(-0.0133660337792941,-0.0403204494320485,
-0.0106758387797498));
#48960=CARTESIAN_POINT('Ctrl Pts',(-0.0137990506689412,-0.0403621160987152,
-0.0114258460331539));
#48961=CARTESIAN_POINT('Ctrl Pts',(-0.0142320675585882,-0.0404037827653818,
-0.0121758532865581));
#48962=CARTESIAN_POINT('Ctrl Pts',(-0.0137990506689412,-0.0404454494320486,
-0.0129258605399623));
#48963=CARTESIAN_POINT('Ctrl Pts',(-0.0133660337792941,-0.0404871160987152,
-0.0136758677933664));
#48964=CARTESIAN_POINT('Ctrl Pts',(-0.0125,-0.0405287827653819,-0.0136758677933664));
#48965=CARTESIAN_POINT('Ctrl Pts',(-0.0116339662207059,-0.0405704494320486,
-0.0136758677933664));
#48966=CARTESIAN_POINT('Ctrl Pts',(-0.0112009493310588,-0.0406121160987152,
-0.0129258605399623));
#48967=CARTESIAN_POINT('Ctrl Pts',(-0.0107679324414118,-0.0406537827653819,
-0.0121758532865581));
#48968=CARTESIAN_POINT('Ctrl Pts',(-0.0112009493310588,-0.0406954494320485,
-0.0114258460331539));
#48969=CARTESIAN_POINT('Ctrl Pts',(-0.0116339662207059,-0.0407371160987152,
-0.0106758387797498));
#48970=CARTESIAN_POINT('Ctrl Pts',(-0.0125,-0.0407787827653818,-0.0106758387797498));
#48971=CARTESIAN_POINT('Ctrl Pts',(-0.0133660337792941,-0.0408204494320485,
-0.0106758387797498));
#48972=CARTESIAN_POINT('Ctrl Pts',(-0.0137990506689412,-0.0408621160987152,
-0.0114258460331539));
#48973=CARTESIAN_POINT('Ctrl Pts',(-0.0142320675585882,-0.0409037827653819,
-0.0121758532865581));
#48974=CARTESIAN_POINT('Ctrl Pts',(-0.0137990506689412,-0.0409454494320486,
-0.0129258605399623));
#48975=CARTESIAN_POINT('Ctrl Pts',(-0.0133660337792941,-0.0409871160987153,
-0.0136758677933664));
#48976=CARTESIAN_POINT('Ctrl Pts',(-0.0125,-0.0410287827653819,-0.0136758677933664));
#48977=CARTESIAN_POINT('Ctrl Pts',(-0.0116339662207059,-0.0410704494320486,
-0.0136758677933664));
#48978=CARTESIAN_POINT('Ctrl Pts',(-0.0112009493310588,-0.0411121160987152,
-0.0129258605399623));
#48979=CARTESIAN_POINT('Ctrl Pts',(-0.0107679324414118,-0.0411537827653819,
-0.012175853286558));
#48980=CARTESIAN_POINT('Ctrl Pts',(-0.0112009493310588,-0.0411954494320485,
-0.0114258460331539));
#48981=CARTESIAN_POINT('Ctrl Pts',(-0.0116339662207059,-0.0412371160987151,
-0.0106758387797497));
#48982=CARTESIAN_POINT('Ctrl Pts',(-0.0125,-0.0412787827653818,-0.0106758387797498));
#48983=CARTESIAN_POINT('Ctrl Pts',(-0.0133660337792941,-0.0413204494320485,
-0.0106758387797497));
#48984=CARTESIAN_POINT('Ctrl Pts',(-0.0137990506689412,-0.0413621160987152,
-0.0114258460331538));
#48985=CARTESIAN_POINT('Ctrl Pts',(-0.0142320675585882,-0.0414037827653819,
-0.012175853286558));
#48986=CARTESIAN_POINT('Ctrl Pts',(-0.0137990506689412,-0.0414454494320486,
-0.0129258605399623));
#48987=CARTESIAN_POINT('Ctrl Pts',(-0.0134462336521574,-0.0414793989369851,
-0.0135369575388066));
#48988=CARTESIAN_POINT('Ctrl Pts',(-0.012750509472736,-0.0415161450767976,
-0.0136548017389069));
#48989=CARTESIAN_POINT('Ctrl Pts',(-0.013319256622239,-0.0332791637687162,
-0.0130184532271587));
#48990=CARTESIAN_POINT('Ctrl Pts',(-0.0129771529854922,-0.0333119647977888,
-0.0133510792533334));
#48991=CARTESIAN_POINT('Ctrl Pts',(-0.0125,-0.033341266014364,-0.0133510792533334));
#48992=CARTESIAN_POINT('Ctrl Pts',(-0.0118214829717238,-0.0333829326810307,
-0.0133510792533334));
#48993=CARTESIAN_POINT('Ctrl Pts',(-0.0114822244575857,-0.0334245993476973,
-0.0127634662699458));
#48994=CARTESIAN_POINT('Ctrl Pts',(-0.0111429659434476,-0.033466266014364,
-0.0121758532865583));
#48995=CARTESIAN_POINT('Ctrl Pts',(-0.0114822244575857,-0.0335079326810306,
-0.0115882403031708));
#48996=CARTESIAN_POINT('Ctrl Pts',(-0.0118214829717238,-0.0335495993476973,
-0.0110006273197833));
#48997=CARTESIAN_POINT('Ctrl Pts',(-0.0125,-0.033591266014364,-0.0110006273197833));
#48998=CARTESIAN_POINT('Ctrl Pts',(-0.0131785170282762,-0.0336329326810306,
-0.0110006273197833));
#48999=CARTESIAN_POINT('Ctrl Pts',(-0.0135177755424142,-0.0336745993476973,
-0.0115882403031708));
#49000=CARTESIAN_POINT('Ctrl Pts',(-0.0138570340565524,-0.033716266014364,
-0.0121758532865583));
#49001=CARTESIAN_POINT('Ctrl Pts',(-0.0135177755424142,-0.0337579326810307,
-0.0127634662699458));
#49002=CARTESIAN_POINT('Ctrl Pts',(-0.0131785170282762,-0.0337995993476974,
-0.0133510792533333));
#49003=CARTESIAN_POINT('Ctrl Pts',(-0.0125,-0.0338412660143641,-0.0133510792533333));
#49004=CARTESIAN_POINT('Ctrl Pts',(-0.0118214829717238,-0.0338829326810307,
-0.0133510792533333));
#49005=CARTESIAN_POINT('Ctrl Pts',(-0.0114822244575857,-0.0339245993476973,
-0.0127634662699458));
#49006=CARTESIAN_POINT('Ctrl Pts',(-0.0111429659434476,-0.033966266014364,
-0.0121758532865583));
#49007=CARTESIAN_POINT('Ctrl Pts',(-0.0114822244575857,-0.0340079326810306,
-0.0115882403031708));
#49008=CARTESIAN_POINT('Ctrl Pts',(-0.0118214829717238,-0.0340495993476973,
-0.0110006273197833));
#49009=CARTESIAN_POINT('Ctrl Pts',(-0.0125,-0.034091266014364,-0.0110006273197833));
#49010=CARTESIAN_POINT('Ctrl Pts',(-0.0131785170282762,-0.0341329326810306,
-0.0110006273197833));
#49011=CARTESIAN_POINT('Ctrl Pts',(-0.0135177755424142,-0.0341745993476973,
-0.0115882403031708));
#49012=CARTESIAN_POINT('Ctrl Pts',(-0.0138570340565524,-0.034216266014364,
-0.0121758532865583));
#49013=CARTESIAN_POINT('Ctrl Pts',(-0.0135177755424142,-0.0342579326810307,
-0.0127634662699458));
#49014=CARTESIAN_POINT('Ctrl Pts',(-0.0131785170282762,-0.0342995993476974,
-0.0133510792533333));
#49015=CARTESIAN_POINT('Ctrl Pts',(-0.0125,-0.0343412660143641,-0.0133510792533333));
#49016=CARTESIAN_POINT('Ctrl Pts',(-0.0118214829717238,-0.0343829326810307,
-0.0133510792533333));
#49017=CARTESIAN_POINT('Ctrl Pts',(-0.0114822244575857,-0.0344245993476973,
-0.0127634662699458));
#49018=CARTESIAN_POINT('Ctrl Pts',(-0.0111429659434476,-0.034466266014364,
-0.0121758532865583));
#49019=CARTESIAN_POINT('Ctrl Pts',(-0.0114822244575857,-0.0345079326810307,
-0.0115882403031708));
#49020=CARTESIAN_POINT('Ctrl Pts',(-0.0118214829717238,-0.0345495993476973,
-0.0110006273197833));
#49021=CARTESIAN_POINT('Ctrl Pts',(-0.0125,-0.034591266014364,-0.0110006273197833));
#49022=CARTESIAN_POINT('Ctrl Pts',(-0.0131785170282762,-0.0346329326810306,
-0.0110006273197833));
#49023=CARTESIAN_POINT('Ctrl Pts',(-0.0135177755424142,-0.0346745993476973,
-0.0115882403031708));
#49024=CARTESIAN_POINT('Ctrl Pts',(-0.0138570340565524,-0.034716266014364,
-0.0121758532865583));
#49025=CARTESIAN_POINT('Ctrl Pts',(-0.0135177755424142,-0.0347579326810307,
-0.0127634662699458));
#49026=CARTESIAN_POINT('Ctrl Pts',(-0.0131785170282762,-0.0347995993476974,
-0.0133510792533333));
#49027=CARTESIAN_POINT('Ctrl Pts',(-0.0125,-0.0348412660143641,-0.0133510792533333));
#49028=CARTESIAN_POINT('Ctrl Pts',(-0.0118214829717238,-0.0348829326810306,
-0.0133510792533333));
#49029=CARTESIAN_POINT('Ctrl Pts',(-0.0114822244575857,-0.0349245993476973,
-0.0127634662699458));
#49030=CARTESIAN_POINT('Ctrl Pts',(-0.0111429659434476,-0.034966266014364,
-0.0121758532865583));
#49031=CARTESIAN_POINT('Ctrl Pts',(-0.0114822244575857,-0.0350079326810307,
-0.0115882403031708));
#49032=CARTESIAN_POINT('Ctrl Pts',(-0.0118214829717238,-0.0350495993476973,
-0.0110006273197832));
#49033=CARTESIAN_POINT('Ctrl Pts',(-0.0125,-0.035091266014364,-0.0110006273197832));
#49034=CARTESIAN_POINT('Ctrl Pts',(-0.0131785170282762,-0.0351329326810307,
-0.0110006273197832));
#49035=CARTESIAN_POINT('Ctrl Pts',(-0.0135177755424142,-0.0351745993476973,
-0.0115882403031707));
#49036=CARTESIAN_POINT('Ctrl Pts',(-0.0138570340565524,-0.035216266014364,
-0.0121758532865583));
#49037=CARTESIAN_POINT('Ctrl Pts',(-0.0135177755424142,-0.0352579326810307,
-0.0127634662699458));
#49038=CARTESIAN_POINT('Ctrl Pts',(-0.0131785170282762,-0.0352995993476974,
-0.0133510792533333));
#49039=CARTESIAN_POINT('Ctrl Pts',(-0.0125,-0.0353412660143641,-0.0133510792533333));
#49040=CARTESIAN_POINT('Ctrl Pts',(-0.0118214829717238,-0.0353829326810307,
-0.0133510792533333));
#49041=CARTESIAN_POINT('Ctrl Pts',(-0.0114822244575857,-0.0354245993476973,
-0.0127634662699458));
#49042=CARTESIAN_POINT('Ctrl Pts',(-0.0111429659434476,-0.035466266014364,
-0.0121758532865583));
#49043=CARTESIAN_POINT('Ctrl Pts',(-0.0114822244575857,-0.0355079326810307,
-0.0115882403031707));
#49044=CARTESIAN_POINT('Ctrl Pts',(-0.0118214829717238,-0.0355495993476973,
-0.0110006273197832));
#49045=CARTESIAN_POINT('Ctrl Pts',(-0.0125,-0.035591266014364,-0.0110006273197832));
#49046=CARTESIAN_POINT('Ctrl Pts',(-0.0131785170282762,-0.0356329326810306,
-0.0110006273197832));
#49047=CARTESIAN_POINT('Ctrl Pts',(-0.0135177755424142,-0.0356745993476973,
-0.0115882403031707));
#49048=CARTESIAN_POINT('Ctrl Pts',(-0.0138570340565524,-0.035716266014364,
-0.0121758532865583));
#49049=CARTESIAN_POINT('Ctrl Pts',(-0.0135177755424142,-0.0357579326810307,
-0.0127634662699458));
#49050=CARTESIAN_POINT('Ctrl Pts',(-0.0131785170282762,-0.0357995993476973,
-0.0133510792533333));
#49051=CARTESIAN_POINT('Ctrl Pts',(-0.0125,-0.0358412660143641,-0.0133510792533333));
#49052=CARTESIAN_POINT('Ctrl Pts',(-0.0118214829717238,-0.0358829326810307,
-0.0133510792533333));
#49053=CARTESIAN_POINT('Ctrl Pts',(-0.0114822244575857,-0.0359245993476973,
-0.0127634662699458));
#49054=CARTESIAN_POINT('Ctrl Pts',(-0.0111429659434476,-0.035966266014364,
-0.0121758532865583));
#49055=CARTESIAN_POINT('Ctrl Pts',(-0.0114822244575857,-0.0360079326810307,
-0.0115882403031707));
#49056=CARTESIAN_POINT('Ctrl Pts',(-0.0118214829717238,-0.0360495993476973,
-0.0110006273197832));
#49057=CARTESIAN_POINT('Ctrl Pts',(-0.0125,-0.0360912660143639,-0.0110006273197832));
#49058=CARTESIAN_POINT('Ctrl Pts',(-0.0131785170282762,-0.0361329326810306,
-0.0110006273197832));
#49059=CARTESIAN_POINT('Ctrl Pts',(-0.0135177755424142,-0.0361745993476973,
-0.0115882403031707));
#49060=CARTESIAN_POINT('Ctrl Pts',(-0.0138570340565524,-0.036216266014364,
-0.0121758532865582));
#49061=CARTESIAN_POINT('Ctrl Pts',(-0.0135177755424142,-0.0362579326810307,
-0.0127634662699457));
#49062=CARTESIAN_POINT('Ctrl Pts',(-0.0131785170282762,-0.0362995993476974,
-0.0133510792533332));
#49063=CARTESIAN_POINT('Ctrl Pts',(-0.0125,-0.036341266014364,-0.0133510792533333));
#49064=CARTESIAN_POINT('Ctrl Pts',(-0.0118214829717238,-0.0363829326810307,
-0.0133510792533332));
#49065=CARTESIAN_POINT('Ctrl Pts',(-0.0114822244575857,-0.0364245993476973,
-0.0127634662699457));
#49066=CARTESIAN_POINT('Ctrl Pts',(-0.0111429659434476,-0.036466266014364,
-0.0121758532865582));
#49067=CARTESIAN_POINT('Ctrl Pts',(-0.0114822244575857,-0.0365079326810307,
-0.0115882403031707));
#49068=CARTESIAN_POINT('Ctrl Pts',(-0.0118214829717238,-0.0365495993476973,
-0.0110006273197832));
#49069=CARTESIAN_POINT('Ctrl Pts',(-0.0125,-0.0365912660143639,-0.0110006273197832));
#49070=CARTESIAN_POINT('Ctrl Pts',(-0.0131785170282762,-0.0366329326810306,
-0.0110006273197832));
#49071=CARTESIAN_POINT('Ctrl Pts',(-0.0135177755424142,-0.0366745993476973,
-0.0115882403031707));
#49072=CARTESIAN_POINT('Ctrl Pts',(-0.0138570340565524,-0.036716266014364,
-0.0121758532865582));
#49073=CARTESIAN_POINT('Ctrl Pts',(-0.0135177755424142,-0.0367579326810307,
-0.0127634662699457));
#49074=CARTESIAN_POINT('Ctrl Pts',(-0.0131785170282762,-0.0367995993476974,
-0.0133510792533332));
#49075=CARTESIAN_POINT('Ctrl Pts',(-0.0125,-0.036841266014364,-0.0133510792533332));
#49076=CARTESIAN_POINT('Ctrl Pts',(-0.0118214829717238,-0.0368829326810307,
-0.0133510792533332));
#49077=CARTESIAN_POINT('Ctrl Pts',(-0.0114822244575857,-0.0369245993476973,
-0.0127634662699457));
#49078=CARTESIAN_POINT('Ctrl Pts',(-0.0111429659434476,-0.036966266014364,
-0.0121758532865582));
#49079=CARTESIAN_POINT('Ctrl Pts',(-0.0114822244575857,-0.0370079326810307,
-0.0115882403031707));
#49080=CARTESIAN_POINT('Ctrl Pts',(-0.0118214829717238,-0.0370495993476973,
-0.0110006273197832));
#49081=CARTESIAN_POINT('Ctrl Pts',(-0.0125,-0.0370912660143639,-0.0110006273197832));
#49082=CARTESIAN_POINT('Ctrl Pts',(-0.0131785170282762,-0.0371329326810306,
-0.0110006273197832));
#49083=CARTESIAN_POINT('Ctrl Pts',(-0.0135177755424142,-0.0371745993476973,
-0.0115882403031707));
#49084=CARTESIAN_POINT('Ctrl Pts',(-0.0138570340565524,-0.037216266014364,
-0.0121758532865582));
#49085=CARTESIAN_POINT('Ctrl Pts',(-0.0135177755424142,-0.0372579326810307,
-0.0127634662699457));
#49086=CARTESIAN_POINT('Ctrl Pts',(-0.0131785170282762,-0.0372995993476973,
-0.0133510792533332));
#49087=CARTESIAN_POINT('Ctrl Pts',(-0.0125,-0.037341266014364,-0.0133510792533332));
#49088=CARTESIAN_POINT('Ctrl Pts',(-0.0118214829717238,-0.0373829326810307,
-0.0133510792533332));
#49089=CARTESIAN_POINT('Ctrl Pts',(-0.0114822244575857,-0.0374245993476973,
-0.0127634662699457));
#49090=CARTESIAN_POINT('Ctrl Pts',(-0.0111429659434476,-0.037466266014364,
-0.0121758532865582));
#49091=CARTESIAN_POINT('Ctrl Pts',(-0.0114822244575857,-0.0375079326810307,
-0.0115882403031707));
#49092=CARTESIAN_POINT('Ctrl Pts',(-0.0118214829717238,-0.0375495993476973,
-0.0110006273197832));
#49093=CARTESIAN_POINT('Ctrl Pts',(-0.0125,-0.0375912660143639,-0.0110006273197831));
#49094=CARTESIAN_POINT('Ctrl Pts',(-0.0131785170282762,-0.0376329326810306,
-0.0110006273197831));
#49095=CARTESIAN_POINT('Ctrl Pts',(-0.0135177755424142,-0.0376745993476973,
-0.0115882403031707));
#49096=CARTESIAN_POINT('Ctrl Pts',(-0.0138570340565524,-0.037716266014364,
-0.0121758532865582));
#49097=CARTESIAN_POINT('Ctrl Pts',(-0.0135177755424142,-0.0377579326810307,
-0.0127634662699457));
#49098=CARTESIAN_POINT('Ctrl Pts',(-0.0131785170282762,-0.0377995993476974,
-0.0133510792533332));
#49099=CARTESIAN_POINT('Ctrl Pts',(-0.0125,-0.037841266014364,-0.0133510792533332));
#49100=CARTESIAN_POINT('Ctrl Pts',(-0.0118214829717238,-0.0378829326810307,
-0.0133510792533332));
#49101=CARTESIAN_POINT('Ctrl Pts',(-0.0114822244575857,-0.0379245993476974,
-0.0127634662699457));
#49102=CARTESIAN_POINT('Ctrl Pts',(-0.0111429659434476,-0.037966266014364,
-0.0121758532865582));
#49103=CARTESIAN_POINT('Ctrl Pts',(-0.0114822244575857,-0.0380079326810307,
-0.0115882403031707));
#49104=CARTESIAN_POINT('Ctrl Pts',(-0.0118214829717238,-0.0380495993476973,
-0.0110006273197831));
#49105=CARTESIAN_POINT('Ctrl Pts',(-0.0125,-0.0380912660143639,-0.0110006273197831));
#49106=CARTESIAN_POINT('Ctrl Pts',(-0.0131785170282762,-0.0381329326810306,
-0.0110006273197831));
#49107=CARTESIAN_POINT('Ctrl Pts',(-0.0135177755424142,-0.0381745993476973,
-0.0115882403031706));
#49108=CARTESIAN_POINT('Ctrl Pts',(-0.0138570340565524,-0.038216266014364,
-0.0121758532865582));
#49109=CARTESIAN_POINT('Ctrl Pts',(-0.0135177755424142,-0.0382579326810306,
-0.0127634662699457));
#49110=CARTESIAN_POINT('Ctrl Pts',(-0.0131785170282762,-0.0382995993476974,
-0.0133510792533332));
#49111=CARTESIAN_POINT('Ctrl Pts',(-0.0125,-0.038341266014364,-0.0133510792533332));
#49112=CARTESIAN_POINT('Ctrl Pts',(-0.0118214829717238,-0.0383829326810307,
-0.0133510792533332));
#49113=CARTESIAN_POINT('Ctrl Pts',(-0.0114822244575857,-0.0384245993476974,
-0.0127634662699457));
#49114=CARTESIAN_POINT('Ctrl Pts',(-0.0111429659434476,-0.0384662660143639,
-0.0121758532865581));
#49115=CARTESIAN_POINT('Ctrl Pts',(-0.0114822244575857,-0.0385079326810306,
-0.0115882403031706));
#49116=CARTESIAN_POINT('Ctrl Pts',(-0.0118214829717238,-0.0385495993476973,
-0.0110006273197831));
#49117=CARTESIAN_POINT('Ctrl Pts',(-0.0125,-0.038591266014364,-0.0110006273197831));
#49118=CARTESIAN_POINT('Ctrl Pts',(-0.0131785170282762,-0.0386329326810306,
-0.0110006273197831));
#49119=CARTESIAN_POINT('Ctrl Pts',(-0.0135177755424142,-0.0386745993476973,
-0.0115882403031706));
#49120=CARTESIAN_POINT('Ctrl Pts',(-0.0138570340565524,-0.038716266014364,
-0.0121758532865581));
#49121=CARTESIAN_POINT('Ctrl Pts',(-0.0135177755424142,-0.0387579326810306,
-0.0127634662699457));
#49122=CARTESIAN_POINT('Ctrl Pts',(-0.0131785170282762,-0.0387995993476974,
-0.0133510792533332));
#49123=CARTESIAN_POINT('Ctrl Pts',(-0.0125,-0.038841266014364,-0.0133510792533332));
#49124=CARTESIAN_POINT('Ctrl Pts',(-0.0118214829717238,-0.0388829326810307,
-0.0133510792533332));
#49125=CARTESIAN_POINT('Ctrl Pts',(-0.0114822244575857,-0.0389245993476974,
-0.0127634662699456));
#49126=CARTESIAN_POINT('Ctrl Pts',(-0.0111429659434476,-0.038966266014364,
-0.0121758532865581));
#49127=CARTESIAN_POINT('Ctrl Pts',(-0.0114822244575857,-0.0390079326810306,
-0.0115882403031706));
#49128=CARTESIAN_POINT('Ctrl Pts',(-0.0118214829717238,-0.0390495993476973,
-0.0110006273197831));
#49129=CARTESIAN_POINT('Ctrl Pts',(-0.0125,-0.039091266014364,-0.0110006273197831));
#49130=CARTESIAN_POINT('Ctrl Pts',(-0.0131785170282762,-0.0391329326810306,
-0.0110006273197831));
#49131=CARTESIAN_POINT('Ctrl Pts',(-0.0135177755424142,-0.0391745993476973,
-0.0115882403031706));
#49132=CARTESIAN_POINT('Ctrl Pts',(-0.0138570340565524,-0.039216266014364,
-0.0121758532865581));
#49133=CARTESIAN_POINT('Ctrl Pts',(-0.0135177755424142,-0.0392579326810306,
-0.0127634662699456));
#49134=CARTESIAN_POINT('Ctrl Pts',(-0.0131785170282762,-0.0392995993476974,
-0.0133510792533332));
#49135=CARTESIAN_POINT('Ctrl Pts',(-0.0125,-0.039341266014364,-0.0133510792533331));
#49136=CARTESIAN_POINT('Ctrl Pts',(-0.0118214829717238,-0.0393829326810307,
-0.0133510792533332));
#49137=CARTESIAN_POINT('Ctrl Pts',(-0.0114822244575857,-0.0394245993476974,
-0.0127634662699456));
#49138=CARTESIAN_POINT('Ctrl Pts',(-0.0111429659434476,-0.039466266014364,
-0.0121758532865581));
#49139=CARTESIAN_POINT('Ctrl Pts',(-0.0114822244575857,-0.0395079326810306,
-0.0115882403031706));
#49140=CARTESIAN_POINT('Ctrl Pts',(-0.0118214829717238,-0.0395495993476973,
-0.0110006273197831));
#49141=CARTESIAN_POINT('Ctrl Pts',(-0.0125,-0.039591266014364,-0.0110006273197831));
#49142=CARTESIAN_POINT('Ctrl Pts',(-0.0131785170282762,-0.0396329326810306,
-0.0110006273197831));
#49143=CARTESIAN_POINT('Ctrl Pts',(-0.0135177755424142,-0.0396745993476973,
-0.0115882403031706));
#49144=CARTESIAN_POINT('Ctrl Pts',(-0.0138570340565524,-0.039716266014364,
-0.0121758532865581));
#49145=CARTESIAN_POINT('Ctrl Pts',(-0.0135177755424142,-0.0397579326810306,
-0.0127634662699456));
#49146=CARTESIAN_POINT('Ctrl Pts',(-0.0131785170282762,-0.0397995993476973,
-0.0133510792533331));
#49147=CARTESIAN_POINT('Ctrl Pts',(-0.0125,-0.039841266014364,-0.0133510792533331));
#49148=CARTESIAN_POINT('Ctrl Pts',(-0.0118214829717238,-0.0398829326810307,
-0.0133510792533331));
#49149=CARTESIAN_POINT('Ctrl Pts',(-0.0114822244575857,-0.0399245993476974,
-0.0127634662699456));
#49150=CARTESIAN_POINT('Ctrl Pts',(-0.0111429659434476,-0.039966266014364,
-0.0121758532865581));
#49151=CARTESIAN_POINT('Ctrl Pts',(-0.0114822244575857,-0.0400079326810306,
-0.0115882403031706));
#49152=CARTESIAN_POINT('Ctrl Pts',(-0.0118214829717238,-0.0400495993476973,
-0.0110006273197831));
#49153=CARTESIAN_POINT('Ctrl Pts',(-0.0125,-0.040091266014364,-0.0110006273197831));
#49154=CARTESIAN_POINT('Ctrl Pts',(-0.0131785170282762,-0.0401329326810306,
-0.0110006273197831));
#49155=CARTESIAN_POINT('Ctrl Pts',(-0.0135177755424142,-0.0401745993476973,
-0.0115882403031706));
#49156=CARTESIAN_POINT('Ctrl Pts',(-0.0138570340565524,-0.040216266014364,
-0.0121758532865581));
#49157=CARTESIAN_POINT('Ctrl Pts',(-0.0135177755424142,-0.0402579326810306,
-0.0127634662699456));
#49158=CARTESIAN_POINT('Ctrl Pts',(-0.0131785170282762,-0.0402995993476974,
-0.0133510792533331));
#49159=CARTESIAN_POINT('Ctrl Pts',(-0.0125,-0.040341266014364,-0.0133510792533331));
#49160=CARTESIAN_POINT('Ctrl Pts',(-0.0118214829717238,-0.0403829326810307,
-0.0133510792533331));
#49161=CARTESIAN_POINT('Ctrl Pts',(-0.0114822244575857,-0.0404245993476973,
-0.0127634662699456));
#49162=CARTESIAN_POINT('Ctrl Pts',(-0.0111429659434476,-0.040466266014364,
-0.0121758532865581));
#49163=CARTESIAN_POINT('Ctrl Pts',(-0.0114822244575857,-0.0405079326810306,
-0.0115882403031706));
#49164=CARTESIAN_POINT('Ctrl Pts',(-0.0118214829717238,-0.0405495993476973,
-0.0110006273197831));
#49165=CARTESIAN_POINT('Ctrl Pts',(-0.0125,-0.040591266014364,-0.011000627319783));
#49166=CARTESIAN_POINT('Ctrl Pts',(-0.0131785170282762,-0.0406329326810306,
-0.011000627319783));
#49167=CARTESIAN_POINT('Ctrl Pts',(-0.0135177755424142,-0.0406745993476973,
-0.0115882403031706));
#49168=CARTESIAN_POINT('Ctrl Pts',(-0.0138570340565524,-0.040716266014364,
-0.0121758532865581));
#49169=CARTESIAN_POINT('Ctrl Pts',(-0.0135177755424142,-0.0407579326810306,
-0.0127634662699456));
#49170=CARTESIAN_POINT('Ctrl Pts',(-0.0131785170282762,-0.0407995993476974,
-0.0133510792533331));
#49171=CARTESIAN_POINT('Ctrl Pts',(-0.0125,-0.040841266014364,-0.0133510792533331));
#49172=CARTESIAN_POINT('Ctrl Pts',(-0.0118214829717238,-0.0408829326810307,
-0.0133510792533331));
#49173=CARTESIAN_POINT('Ctrl Pts',(-0.0114822244575857,-0.0409245993476973,
-0.0127634662699456));
#49174=CARTESIAN_POINT('Ctrl Pts',(-0.0111429659434476,-0.040966266014364,
-0.0121758532865581));
#49175=CARTESIAN_POINT('Ctrl Pts',(-0.0114822244575857,-0.0410079326810306,
-0.0115882403031705));
#49176=CARTESIAN_POINT('Ctrl Pts',(-0.0118214829717238,-0.0410495993476973,
-0.011000627319783));
#49177=CARTESIAN_POINT('Ctrl Pts',(-0.0125,-0.041091266014364,-0.011000627319783));
#49178=CARTESIAN_POINT('Ctrl Pts',(-0.0131785170282762,-0.0411329326810306,
-0.011000627319783));
#49179=CARTESIAN_POINT('Ctrl Pts',(-0.0135177755424142,-0.0411745993476973,
-0.0115882403031705));
#49180=CARTESIAN_POINT('Ctrl Pts',(-0.0138570340565524,-0.041216266014364,
-0.012175853286558));
#49181=CARTESIAN_POINT('Ctrl Pts',(-0.0135177755424142,-0.0412579326810306,
-0.0127634662699456));
#49182=CARTESIAN_POINT('Ctrl Pts',(-0.0132413517360028,-0.0412918821859672,
-0.0132422463470719));
#49183=CARTESIAN_POINT('Ctrl Pts',(-0.0126962682600376,-0.0413286283257797,
-0.0133345744968084));
#49184=CARTESIAN_POINT('Ctrl Pts',(-0.0125000000004755,-0.0412787743898721,
-0.0106758532865977));
#49185=CARTESIAN_POINT('Ctrl Pts',(-0.0125791534151202,-0.0412787743898721,
-0.0106824494045114));
#49186=CARTESIAN_POINT('Ctrl Pts',(-0.012747840893727,-0.0412787743898722,
-0.0107019181802518));
#49187=CARTESIAN_POINT('Ctrl Pts',(-0.0130748131830085,-0.0412787743898722,
-0.0108429922798694));
#49188=CARTESIAN_POINT('Ctrl Pts',(-0.0131946039736345,-0.0412787743898722,
-0.0109172484796293));
#49189=CARTESIAN_POINT('Ctrl Pts',(-0.0134365405523043,-0.0412787743898722,
-0.0111221468405966));
#49190=CARTESIAN_POINT('Ctrl Pts',(-0.0135489323007065,-0.0412787743876939,
-0.0112606089599943));
#49191=CARTESIAN_POINT('Ctrl Pts',(-0.0136815652166612,-0.041278774387694,
-0.0115057517085288));
#49192=CARTESIAN_POINT('Ctrl Pts',(-0.0137143235950122,-0.0412787743898722,
-0.0115888928601645));
#49193=CARTESIAN_POINT('Ctrl Pts',(-0.0137820146531768,-0.0412787743898722,
-0.011813467117283));
#49194=CARTESIAN_POINT('Ctrl Pts',(-0.0137993725080859,-0.0412787743898722,
-0.0119695136960876));
#49195=CARTESIAN_POINT('Ctrl Pts',(-0.0137763187378415,-0.0412787743898722,
-0.012289886224141));
#49196=CARTESIAN_POINT('Ctrl Pts',(-0.0137324577582181,-0.0412787743898722,
-0.012450985065106));
#49197=CARTESIAN_POINT('Ctrl Pts',(-0.0136184626350962,-0.0412787743898722,
-0.0126812497443392));
#49198=CARTESIAN_POINT('Ctrl Pts',(-0.0135679181647976,-0.0412787743897922,
-0.0127611938063621));
#49199=CARTESIAN_POINT('Ctrl Pts',(-0.0134548766008996,-0.0412787743897922,
-0.012900132909092));
#49200=CARTESIAN_POINT('Ctrl Pts',(-0.0133923323265011,-0.0412787743898722,
-0.0129611541294956));
#49201=CARTESIAN_POINT('Ctrl Pts',(-0.0133234078741649,-0.0412787743898722,
-0.013014417323174));
#49202=CARTESIAN_POINT('Origin',(-0.0125,-0.0429287743898722,-0.013675853286558));
#49203=CARTESIAN_POINT('',(-0.0135,-0.0429287743898722,-0.0115985030173684));
#49204=CARTESIAN_POINT('',(-0.0135,-0.0429287743898722,-0.0127532035557476));
#49205=CARTESIAN_POINT('Origin',(-0.0125,-0.0429287743898722,-0.012175853286558));
#49206=CARTESIAN_POINT('',(-0.0125,-0.0429287743898722,-0.0110211527481787));
#49207=CARTESIAN_POINT('Origin',(-0.0125,-0.0429287743898722,-0.012175853286558));
#49208=CARTESIAN_POINT('Origin',(-0.0125,-0.0429287743898722,-0.012175853286558));
#49209=CARTESIAN_POINT('',(-0.0125,-0.0429287743898722,-0.0133305538249372));
#49210=CARTESIAN_POINT('Origin',(-0.0125,-0.0429287743898722,-0.012175853286558));
#49211=CARTESIAN_POINT('Origin',(-0.0125,-0.0429287743898722,-0.012175853286558));
#49212=CARTESIAN_POINT('Origin',(-0.0125,-0.0412787743898723,-0.015025853286558));
#49213=CARTESIAN_POINT('Origin',(-0.0125,-0.0429287743898722,-0.012175853286558));
#49214=CARTESIAN_POINT('Ctrl Pts',(-0.0114999999999901,-0.0429287743898621,
-0.0115985030173583));
#49215=CARTESIAN_POINT('Ctrl Pts',(-0.01199999999999,-0.0426400992552674,
-0.0113098278827636));
#49216=CARTESIAN_POINT('Ctrl Pts',(-0.01249999999999,-0.0429287743898621,
-0.0110211527481688));
#49217=CARTESIAN_POINT('Origin',(-0.0125,-0.0429287743898722,-0.012175853286558));
#49218=CARTESIAN_POINT('Ctrl Pts',(-0.01250000000001,-0.0429287743898621,
-0.0110211527481688));
#49219=CARTESIAN_POINT('Ctrl Pts',(-0.01300000000001,-0.0426400992552674,
-0.0113098278827636));
#49220=CARTESIAN_POINT('Ctrl Pts',(-0.01350000000001,-0.0429287743898621,
-0.0115985030173583));
#49221=CARTESIAN_POINT('Origin',(-0.0125,-0.0429287743898722,-0.012175853286558));
#49222=CARTESIAN_POINT('Ctrl Pts',(-0.01350000000001,-0.0429287743898621,
-0.0115985030173584));
#49223=CARTESIAN_POINT('Ctrl Pts',(-0.01350000000001,-0.0426400992552674,
-0.012175853286548));
#49224=CARTESIAN_POINT('Ctrl Pts',(-0.01350000000001,-0.0429287743898622,
-0.0127532035557576));
#49225=CARTESIAN_POINT('Origin',(-0.0125,-0.0429287743898722,-0.012175853286558));
#49226=CARTESIAN_POINT('Ctrl Pts',(-0.01350000000001,-0.0429287743898622,
-0.0127532035557576));
#49227=CARTESIAN_POINT('Ctrl Pts',(-0.01300000000001,-0.0426400992552675,
-0.0130418786903524));
#49228=CARTESIAN_POINT('Ctrl Pts',(-0.01250000000001,-0.0429287743898622,
-0.0133305538249472));
#49229=CARTESIAN_POINT('Origin',(-0.0125,-0.0429287743898722,-0.012175853286558));
#49230=CARTESIAN_POINT('Ctrl Pts',(-0.01249999999999,-0.0429287743898622,
-0.0133305538249472));
#49231=CARTESIAN_POINT('Ctrl Pts',(-0.01199999999999,-0.0426400992552675,
-0.0130418786903524));
#49232=CARTESIAN_POINT('Ctrl Pts',(-0.0114999999999901,-0.0429287743898622,
-0.0127532035557576));
#49233=CARTESIAN_POINT('Origin',(-0.0115,-0.0417737743898722,-0.0127532035557477));
#49234=CARTESIAN_POINT('',(-0.0125,-0.0417737743898722,-0.0133305538249373));
#49235=CARTESIAN_POINT('',(-0.0115,-0.0417737743898722,-0.0127532035557477));
#49236=CARTESIAN_POINT('',(-0.01249999999999,-0.0417737743898622,-0.0133305538249473));
#49237=CARTESIAN_POINT('',(-0.0115,-0.0417737743898722,-0.0115985030173684));
#49238=CARTESIAN_POINT('',(-0.01149999999999,-0.0417737743898622,-0.0127532035557577));
#49239=CARTESIAN_POINT('',(-0.0125,-0.0417737743898721,-0.0110211527481788));
#49240=CARTESIAN_POINT('',(-0.01149999999999,-0.0417737743898622,-0.0115985030173584));
#49241=CARTESIAN_POINT('',(-0.0135,-0.0417737743898722,-0.0115985030173684));
#49242=CARTESIAN_POINT('',(-0.01250000000001,-0.0417737743898621,-0.0110211527481688));
#49243=CARTESIAN_POINT('',(-0.0135,-0.0417737743898722,-0.0127532035557477));
#49244=CARTESIAN_POINT('',(-0.01350000000001,-0.0417737743898622,-0.0115985030173584));
#49245=CARTESIAN_POINT('',(-0.01350000000001,-0.0417737743898622,-0.0127532035557577));
#49246=CARTESIAN_POINT('Origin',(-0.0115,-0.0417737743898722,-0.0127532035557477));
#49247=CARTESIAN_POINT('',(-0.01149999999999,-0.0417737743898622,-0.0127532035557577));
#49248=CARTESIAN_POINT('',(-0.01149999999999,-0.0417737743898622,-0.0115985030173584));
#49249=CARTESIAN_POINT('Origin',(-0.0115,-0.0417737743898722,-0.0115985030173684));
#49250=CARTESIAN_POINT('',(-0.01250000000001,-0.0417737743898621,-0.0110211527481688));
#49251=CARTESIAN_POINT('Origin',(-0.0125,-0.0417737743898721,-0.0110211527481788));
#49252=CARTESIAN_POINT('',(-0.01350000000001,-0.0417737743898622,-0.0115985030173584));
#49253=CARTESIAN_POINT('Origin',(-0.0135,-0.0417737743898722,-0.0115985030173684));
#49254=CARTESIAN_POINT('',(-0.01350000000001,-0.0417737743898622,-0.0127532035557577));
#49255=CARTESIAN_POINT('Origin',(-0.0135,-0.0417737743898722,-0.0127532035557477));
#49256=CARTESIAN_POINT('',(-0.01249999999999,-0.0417737743898622,-0.0133305538249473));
#49257=CARTESIAN_POINT('Origin',(-0.0125,-0.0417737743898722,-0.0133305538249373));
#50055=UNCERTAINTY_MEASURE_WITH_UNIT(LENGTH_MEASURE(1.E-5),#50082,
'DISTANCE_ACCURACY_VALUE',
'Maximum model space distance between geometric entities at asserted c
onnectivities');
#50059=UNCERTAINTY_MEASURE_WITH_UNIT(LENGTH_MEASURE(1.E-5),#50082,
'DISTANCE_ACCURACY_VALUE',
'Maximum model space distance between geometric entities at asserted c
onnectivities');
#50077=(
GEOMETRIC_REPRESENTATION_CONTEXT(3)
GLOBAL_UNCERTAINTY_ASSIGNED_CONTEXT((#50055))
GLOBAL_UNIT_ASSIGNED_CONTEXT((#50082,#50083,#50084))
REPRESENTATION_CONTEXT('','3D')
);
#50081=(
GEOMETRIC_REPRESENTATION_CONTEXT(3)
GLOBAL_UNCERTAINTY_ASSIGNED_CONTEXT((#50059))
GLOBAL_UNIT_ASSIGNED_CONTEXT((#50082,#50083,#50084))
REPRESENTATION_CONTEXT('','3D')
);
#50082=(
LENGTH_UNIT()
NAMED_UNIT(*)
SI_UNIT($,.METRE.)
);
#50083=(
NAMED_UNIT(*)
PLANE_ANGLE_UNIT()
SI_UNIT($,.RADIAN.)
);
#50084=(
NAMED_UNIT(*)
SI_UNIT($,.STERADIAN.)
SOLID_ANGLE_UNIT()
);
#50102=SHAPE_DEFINITION_REPRESENTATION(#50123,#50164);
#50123=PRODUCT_DEFINITION_SHAPE('',$,#50186);
#50164=SHAPE_REPRESENTATION('',(#10899),#50077);
#50168=PRODUCT_DEFINITION_CONTEXT('part definition',#50233,'design');
#50186=PRODUCT_DEFINITION('Screw','Screw',#50207,#50168);
#50207=PRODUCT_DEFINITION_FORMATION('',$,#50252);
#50233=APPLICATION_CONTEXT('Managed model based 3d engineering');
#50234=PRODUCT_CONTEXT('part definition',#50233,'mechanical');
#50252=PRODUCT('Screw','Screw',$,(#50234));
#50258=PRESENTATION_STYLE_ASSIGNMENT((#50265));
#50265=SURFACE_STYLE_USAGE(.BOTH.,#50272);
#50272=SURFACE_SIDE_STYLE('',(#50279));
#50279=SURFACE_STYLE_FILL_AREA(#50286);
#50286=FILL_AREA_STYLE('Opaque(89,149,218)',(#50293));
#50293=FILL_AREA_STYLE_COLOUR('Opaque(89,149,218)',#50300);
#50300=COLOUR_RGB('Opaque(89,149,218)',0.349019607843137,0.584313725490196,
0.854901960784314);
ENDSEC;
END-ISO-10303-21;
